ISO-10303-21;
HEADER;
/* Generated by software containing ST-Developer
 * from STEP Tools, Inc. (www.steptools.com) 
 */

FILE_DESCRIPTION(
/* description */ (''),
/* implementation_level */ '2;1');

FILE_NAME(
/* name */ 'Socket head cap screw M3x16.step',
/* time_stamp */ '2026-11-10T08:27:36-08:00',
/* author */ (''),
/* organization */ (''),
/* preprocessor_version */ 'ST-DEVELOPER v20.2',
/* originating_system */ 'Autodesk Translation Framework v15.17.0.0',
/* authorisation */ '');

FILE_SCHEMA (('AUTOMOTIVE_DESIGN { 1 0 10303 214 3 1 1 }'));
ENDSEC;

DATA;
#10=MECHANICAL_DESIGN_GEOMETRIC_PRESENTATION_REPRESENTATION('',(#573),#19090);
#75=CONICAL_SURFACE('',#7367,0.1,0.785398163397448);
#168=B_SPLINE_SURFACE_WITH_KNOTS('',3,3,((#16338,#16339,#16340,#16341,#16342,
#16343,#16344,#16345,#16346,#16347,#16348,#16349,#16350,#16351,#16352,#16353,
#16354,#16355,#16356,#16357,#16358,#16359,#16360,#16361,#16362,#16363,#16364,
#16365,#16366,#16367,#16368,#16369,#16370,#16371,#16372,#16373,#16374,#16375,
#16376,#16377,#16378,#16379,#16380,#16381,#16382,#16383,#16384,#16385,#16386,
#16387,#16388,#16389,#16390,#16391,#16392,#16393,#16394,#16395,#16396,#16397,
#16398,#16399,#16400,#16401,#16402,#16403,#16404,#16405,#16406,#16407,#16408,
#16409,#16410,#16411,#16412,#16413,#16414,#16415,#16416,#16417,#16418,#16419,
#16420,#16421,#16422,#16423,#16424,#16425,#16426,#16427,#16428,#16429,#16430,
#16431,#16432,#16433,#16434,#16435,#16436,#16437,#16438,#16439,#16440,#16441,
#16442,#16443,#16444,#16445,#16446,#16447,#16448,#16449,#16450,#16451,#16452,
#16453,#16454,#16455,#16456,#16457,#16458,#16459,#16460,#16461,#16462,#16463,
#16464,#16465,#16466,#16467,#16468,#16469,#16470,#16471,#16472,#16473,#16474,
#16475,#16476,#16477,#16478,#16479,#16480,#16481,#16482,#16483,#16484,#16485,
#16486,#16487,#16488,#16489,#16490,#16491,#16492,#16493,#16494,#16495,#16496,
#16497,#16498,#16499,#16500,#16501,#16502,#16503,#16504,#16505,#16506,#16507,
#16508,#16509,#16510,#16511,#16512,#16513,#16514,#16515,#16516,#16517,#16518,
#16519,#16520,#16521,#16522,#16523,#16524,#16525,#16526,#16527,#16528,#16529,
#16530,#16531,#16532,#16533),(#16534,#16535,#16536,#16537,#16538,#16539,
#16540,#16541,#16542,#16543,#16544,#16545,#16546,#16547,#16548,#16549,#16550,
#16551,#16552,#16553,#16554,#16555,#16556,#16557,#16558,#16559,#16560,#16561,
#16562,#16563,#16564,#16565,#16566,#16567,#16568,#16569,#16570,#16571,#16572,
#16573,#16574,#16575,#16576,#16577,#16578,#16579,#16580,#16581,#16582,#16583,
#16584,#16585,#16586,#16587,#16588,#16589,#16590,#16591,#16592,#16593,#16594,
#16595,#16596,#16597,#16598,#16599,#16600,#16601,#16602,#16603,#16604,#16605,
#16606,#16607,#16608,#16609,#16610,#16611,#16612,#16613,#16614,#16615,#16616,
#16617,#16618,#16619,#16620,#16621,#16622,#16623,#16624,#16625,#16626,#16627,
#16628,#16629,#16630,#16631,#16632,#16633,#16634,#16635,#16636,#16637,#16638,
#16639,#16640,#16641,#16642,#16643,#16644,#16645,#16646,#16647,#16648,#16649,
#16650,#16651,#16652,#16653,#16654,#16655,#16656,#16657,#16658,#16659,#16660,
#16661,#16662,#16663,#16664,#16665,#16666,#16667,#16668,#16669,#16670,#16671,
#16672,#16673,#16674,#16675,#16676,#16677,#16678,#16679,#16680,#16681,#16682,
#16683,#16684,#16685,#16686,#16687,#16688,#16689,#16690,#16691,#16692,#16693,
#16694,#16695,#16696,#16697,#16698,#16699,#16700,#16701,#16702,#16703,#16704,
#16705,#16706,#16707,#16708,#16709,#16710,#16711,#16712,#16713,#16714,#16715,
#16716,#16717,#16718,#16719,#16720,#16721,#16722,#16723,#16724,#16725,#16726,
#16727,#16728,#16729),(#16730,#16731,#16732,#16733,#16734,#16735,#16736,
#16737,#16738,#16739,#16740,#16741,#16742,#16743,#16744,#16745,#16746,#16747,
#16748,#16749,#16750,#16751,#16752,#16753,#16754,#16755,#16756,#16757,#16758,
#16759,#16760,#16761,#16762,#16763,#16764,#16765,#16766,#16767,#16768,#16769,
#16770,#16771,#16772,#16773,#16774,#16775,#16776,#16777,#16778,#16779,#16780,
#16781,#16782,#16783,#16784,#16785,#16786,#16787,#16788,#16789,#16790,#16791,
#16792,#16793,#16794,#16795,#16796,#16797,#16798,#16799,#16800,#16801,#16802,
#16803,#16804,#16805,#16806,#16807,#16808,#16809,#16810,#16811,#16812,#16813,
#16814,#16815,#16816,#16817,#16818,#16819,#16820,#16821,#16822,#16823,#16824,
#16825,#16826,#16827,#16828,#16829,#16830,#16831,#16832,#16833,#16834,#16835,
#16836,#16837,#16838,#16839,#16840,#16841,#16842,#16843,#16844,#16845,#16846,
#16847,#16848,#16849,#16850,#16851,#16852,#16853,#16854,#16855,#16856,#16857,
#16858,#16859,#16860,#16861,#16862,#16863,#16864,#16865,#16866,#16867,#16868,
#16869,#16870,#16871,#16872,#16873,#16874,#16875,#16876,#16877,#16878,#16879,
#16880,#16881,#16882,#16883,#16884,#16885,#16886,#16887,#16888,#16889,#16890,
#16891,#16892,#16893,#16894,#16895,#16896,#16897,#16898,#16899,#16900,#16901,
#16902,#16903,#16904,#16905,#16906,#16907,#16908,#16909,#16910,#16911,#16912,
#16913,#16914,#16915,#16916,#16917,#16918,#16919,#16920,#16921,#16922,#16923,
#16924,#16925),(#16926,#16927,#16928,#16929,#16930,#16931,#16932,#16933,
#16934,#16935,#16936,#16937,#16938,#16939,#16940,#16941,#16942,#16943,#16944,
#16945,#16946,#16947,#16948,#16949,#16950,#16951,#16952,#16953,#16954,#16955,
#16956,#16957,#16958,#16959,#16960,#16961,#16962,#16963,#16964,#16965,#16966,
#16967,#16968,#16969,#16970,#16971,#16972,#16973,#16974,#16975,#16976,#16977,
#16978,#16979,#16980,#16981,#16982,#16983,#16984,#16985,#16986,#16987,#16988,
#16989,#16990,#16991,#16992,#16993,#16994,#16995,#16996,#16997,#16998,#16999,
#17000,#17001,#17002,#17003,#17004,#17005,#17006,#17007,#17008,#17009,#17010,
#17011,#17012,#17013,#17014,#17015,#17016,#17017,#17018,#17019,#17020,#17021,
#17022,#17023,#17024,#17025,#17026,#17027,#17028,#17029,#17030,#17031,#17032,
#17033,#17034,#17035,#17036,#17037,#17038,#17039,#17040,#17041,#17042,#17043,
#17044,#17045,#17046,#17047,#17048,#17049,#17050,#17051,#17052,#17053,#17054,
#17055,#17056,#17057,#17058,#17059,#17060,#17061,#17062,#17063,#17064,#17065,
#17066,#17067,#17068,#17069,#17070,#17071,#17072,#17073,#17074,#17075,#17076,
#17077,#17078,#17079,#17080,#17081,#17082,#17083,#17084,#17085,#17086,#17087,
#17088,#17089,#17090,#17091,#17092,#17093,#17094,#17095,#17096,#17097,#17098,
#17099,#17100,#17101,#17102,#17103,#17104,#17105,#17106,#17107,#17108,#17109,
#17110,#17111,#17112,#17113,#17114,#17115,#17116,#17117,#17118,#17119,#17120,
#17121)),.UNSPECIFIED.,.F.,.F.,.F.,(4,4),(4,1,1,1,1,1,1,1,1,1,1,1,1,1,1,
1,1,1,1,1,1,1,1,1,1,1,1,1,1,1,1,1,1,1,1,1,1,1,1,1,1,1,1,1,1,1,1,1,1,1,1,
1,1,1,1,1,1,1,1,1,1,1,1,1,1,1,1,1,1,1,1,1,1,1,1,1,1,1,1,1,1,1,1,1,1,1,1,
1,1,1,1,1,1,1,1,1,1,1,1,1,1,1,1,1,1,1,1,1,1,1,1,1,1,1,1,1,1,1,1,1,1,1,1,
1,1,1,1,1,1,1,1,1,1,1,1,1,1,1,1,1,1,1,1,1,1,1,1,1,1,1,1,1,1,1,1,1,1,1,1,
1,1,1,1,1,1,1,1,1,1,1,1,1,1,1,1,1,1,1,1,1,1,1,1,1,1,1,1,1,1,1,1,1,1,4),
(0.,0.0329955678841871),(11.6159397475006,12.61358260836,13.6112254692194,
14.6088683300789,15.6065111909383,16.6041540517977,17.6017969126571,18.5994397735165,
19.5970826343759,20.5947254952353,21.5923683560947,22.5900112169541,23.5876540778135,
24.5852969386729,25.5829397995323,26.5805826603917,27.5782255212511,28.5758683821105,
29.5735112429699,30.5711541038294,31.5687969646888,32.5664398255482,33.5640826864076,
34.561725547267,35.5593684081264,36.5570112689858,37.5546541298452,38.5522969907046,
39.549939851564,40.5475827124234,41.5452255732828,42.5428684341422,43.5405112950016,
44.538154155861,45.5357970167204,46.5334398775799,47.5310827384393,48.5287255992987,
49.5263684601581,50.5240113210175,51.5216541818769,52.5192970427363,53.5169399035957,
54.5145827644551,55.5122256253145,56.5098684861739,57.5075113470333,58.5051542078927,
59.5027970687521,60.5004399296115,61.4980827904709,62.4957256513303,63.4933685121897,
64.4910113730492,65.4886542339086,66.486297094768,67.4839399556274,68.4815828164868,
69.4792256773462,70.4768685382056,71.474511399065,72.4721542599244,73.4697971207838,
74.4674399816432,75.4650828425026,76.462725703362,77.4603685642214,78.4580114250808,
79.4556542859402,80.4532971467996,81.4509400076591,82.4485828685185,83.4462257293779,
84.4438685902373,85.4415114510967,86.4391543119561,87.4367971728155,88.4344400336749,
89.4320828945343,90.4297257553937,91.4273686162531,92.4250114771125,93.4226543379719,
94.4202971988313,95.4179400596907,96.4155829205502,97.4132257814096,98.410868642269,
99.4085115031284,100.406154363988,101.403797224847,102.401440085707,103.399082946566,
104.396725807425,105.394368668285,106.392011529144,107.389654390004,108.387297250863,
109.384940111722,110.382582972582,111.380225833441,112.377868694301,113.37551155516,
114.373154416019,115.370797276879,116.368440137738,117.366082998598,118.363725859457,
119.361368720316,120.359011581176,121.356654442035,122.354297302895,123.351940163754,
124.349583024614,125.347225885473,126.344868746332,127.342511607192,128.340154468051,
129.337797328911,130.33544018977,131.333083050629,132.330725911489,133.328368772348,
134.326011633208,135.323654494067,136.321297354926,137.318940215786,138.316583076645,
139.314225937505,140.311868798364,141.309511659223,142.307154520083,143.304797380942,
144.302440241802,145.300083102661,146.29772596352,147.29536882438,148.293011685239,
149.290654546099,150.288297406958,151.285940267817,152.283583128677,153.281225989536,
154.278868850396,155.276511711255,156.274154572115,157.271797432974,158.269440293833,
159.267083154693,160.264726015552,161.262368876412,162.260011737271,163.25765459813,
164.25529745899,165.252940319849,166.250583180709,167.248226041568,168.245868902427,
169.243511763287,170.241154624146,171.238797485006,172.236440345865,173.234083206724,
174.231726067584,175.229368928443,176.227011789303,177.224654650162,178.222297511021,
179.219940371881,180.21758323274,181.2152260936,182.212868954459,183.210511815318,
184.208154676178,185.205797537037,186.203440397897,187.201083258756,188.198726119616,
189.196368980475,190.194011841334,191.191654702194,192.189297563053,193.186940423913,
194.184583284772,195.182226145631,196.179869006491,197.17751186735,198.17515472821,
199.172797589069,200.170440449928,201.168083310788,202.165726171647,203.163369032507,
204.161011893366),.UNSPECIFIED.);
#169=B_SPLINE_SURFACE_WITH_KNOTS('',3,3,((#17211,#17212,#17213,#17214,#17215,
#17216,#17217,#17218,#17219,#17220,#17221,#17222,#17223,#17224,#17225,#17226,
#17227,#17228,#17229,#17230,#17231,#17232,#17233,#17234,#17235,#17236,#17237,
#17238,#17239,#17240,#17241,#17242,#17243,#17244,#17245,#17246,#17247,#17248,
#17249,#17250,#17251,#17252,#17253,#17254,#17255,#17256,#17257,#17258,#17259,
#17260,#17261,#17262,#17263,#17264,#17265,#17266,#17267,#17268,#17269,#17270,
#17271,#17272,#17273,#17274,#17275,#17276,#17277,#17278,#17279,#17280,#17281,
#17282,#17283,#17284,#17285,#17286,#17287,#17288,#17289,#17290,#17291,#17292,
#17293,#17294,#17295,#17296,#17297,#17298,#17299,#17300,#17301,#17302,#17303,
#17304,#17305,#17306,#17307,#17308,#17309,#17310,#17311,#17312,#17313,#17314,
#17315,#17316,#17317,#17318,#17319,#17320,#17321,#17322,#17323,#17324,#17325,
#17326,#17327,#17328,#17329,#17330,#17331,#17332,#17333,#17334,#17335,#17336,
#17337,#17338,#17339,#17340,#17341,#17342,#17343,#17344,#17345,#17346,#17347,
#17348,#17349,#17350,#17351,#17352,#17353,#17354,#17355,#17356,#17357,#17358,
#17359,#17360,#17361,#17362,#17363,#17364,#17365,#17366,#17367,#17368,#17369,
#17370,#17371,#17372,#17373,#17374,#17375,#17376,#17377,#17378,#17379,#17380,
#17381,#17382,#17383,#17384,#17385,#17386,#17387,#17388,#17389,#17390,#17391,
#17392,#17393,#17394,#17395,#17396,#17397,#17398,#17399,#17400,#17401,#17402,
#17403,#17404,#17405,#17406,#17407,#17408),(#17409,#17410,#17411,#17412,
#17413,#17414,#17415,#17416,#17417,#17418,#17419,#17420,#17421,#17422,#17423,
#17424,#17425,#17426,#17427,#17428,#17429,#17430,#17431,#17432,#17433,#17434,
#17435,#17436,#17437,#17438,#17439,#17440,#17441,#17442,#17443,#17444,#17445,
#17446,#17447,#17448,#17449,#17450,#17451,#17452,#17453,#17454,#17455,#17456,
#17457,#17458,#17459,#17460,#17461,#17462,#17463,#17464,#17465,#17466,#17467,
#17468,#17469,#17470,#17471,#17472,#17473,#17474,#17475,#17476,#17477,#17478,
#17479,#17480,#17481,#17482,#17483,#17484,#17485,#17486,#17487,#17488,#17489,
#17490,#17491,#17492,#17493,#17494,#17495,#17496,#17497,#17498,#17499,#17500,
#17501,#17502,#17503,#17504,#17505,#17506,#17507,#17508,#17509,#17510,#17511,
#17512,#17513,#17514,#17515,#17516,#17517,#17518,#17519,#17520,#17521,#17522,
#17523,#17524,#17525,#17526,#17527,#17528,#17529,#17530,#17531,#17532,#17533,
#17534,#17535,#17536,#17537,#17538,#17539,#17540,#17541,#17542,#17543,#17544,
#17545,#17546,#17547,#17548,#17549,#17550,#17551,#17552,#17553,#17554,#17555,
#17556,#17557,#17558,#17559,#17560,#17561,#17562,#17563,#17564,#17565,#17566,
#17567,#17568,#17569,#17570,#17571,#17572,#17573,#17574,#17575,#17576,#17577,
#17578,#17579,#17580,#17581,#17582,#17583,#17584,#17585,#17586,#17587,#17588,
#17589,#17590,#17591,#17592,#17593,#17594,#17595,#17596,#17597,#17598,#17599,
#17600,#17601,#17602,#17603,#17604,#17605,#17606),(#17607,#17608,#17609,
#17610,#17611,#17612,#17613,#17614,#17615,#17616,#17617,#17618,#17619,#17620,
#17621,#17622,#17623,#17624,#17625,#17626,#17627,#17628,#17629,#17630,#17631,
#17632,#17633,#17634,#17635,#17636,#17637,#17638,#17639,#17640,#17641,#17642,
#17643,#17644,#17645,#17646,#17647,#17648,#17649,#17650,#17651,#17652,#17653,
#17654,#17655,#17656,#17657,#17658,#17659,#17660,#17661,#17662,#17663,#17664,
#17665,#17666,#17667,#17668,#17669,#17670,#17671,#17672,#17673,#17674,#17675,
#17676,#17677,#17678,#17679,#17680,#17681,#17682,#17683,#17684,#17685,#17686,
#17687,#17688,#17689,#17690,#17691,#17692,#17693,#17694,#17695,#17696,#17697,
#17698,#17699,#17700,#17701,#17702,#17703,#17704,#17705,#17706,#17707,#17708,
#17709,#17710,#17711,#17712,#17713,#17714,#17715,#17716,#17717,#17718,#17719,
#17720,#17721,#17722,#17723,#17724,#17725,#17726,#17727,#17728,#17729,#17730,
#17731,#17732,#17733,#17734,#17735,#17736,#17737,#17738,#17739,#17740,#17741,
#17742,#17743,#17744,#17745,#17746,#17747,#17748,#17749,#17750,#17751,#17752,
#17753,#17754,#17755,#17756,#17757,#17758,#17759,#17760,#17761,#17762,#17763,
#17764,#17765,#17766,#17767,#17768,#17769,#17770,#17771,#17772,#17773,#17774,
#17775,#17776,#17777,#17778,#17779,#17780,#17781,#17782,#17783,#17784,#17785,
#17786,#17787,#17788,#17789,#17790,#17791,#17792,#17793,#17794,#17795,#17796,
#17797,#17798,#17799,#17800,#17801,#17802,#17803,#17804),(#17805,#17806,
#17807,#17808,#17809,#17810,#17811,#17812,#17813,#17814,#17815,#17816,#17817,
#17818,#17819,#17820,#17821,#17822,#17823,#17824,#17825,#17826,#17827,#17828,
#17829,#17830,#17831,#17832,#17833,#17834,#17835,#17836,#17837,#17838,#17839,
#17840,#17841,#17842,#17843,#17844,#17845,#17846,#17847,#17848,#17849,#17850,
#17851,#17852,#17853,#17854,#17855,#17856,#17857,#17858,#17859,#17860,#17861,
#17862,#17863,#17864,#17865,#17866,#17867,#17868,#17869,#17870,#17871,#17872,
#17873,#17874,#17875,#17876,#17877,#17878,#17879,#17880,#17881,#17882,#17883,
#17884,#17885,#17886,#17887,#17888,#17889,#17890,#17891,#17892,#17893,#17894,
#17895,#17896,#17897,#17898,#17899,#17900,#17901,#17902,#17903,#17904,#17905,
#17906,#17907,#17908,#17909,#17910,#17911,#17912,#17913,#17914,#17915,#17916,
#17917,#17918,#17919,#17920,#17921,#17922,#17923,#17924,#17925,#17926,#17927,
#17928,#17929,#17930,#17931,#17932,#17933,#17934,#17935,#17936,#17937,#17938,
#17939,#17940,#17941,#17942,#17943,#17944,#17945,#17946,#17947,#17948,#17949,
#17950,#17951,#17952,#17953,#17954,#17955,#17956,#17957,#17958,#17959,#17960,
#17961,#17962,#17963,#17964,#17965,#17966,#17967,#17968,#17969,#17970,#17971,
#17972,#17973,#17974,#17975,#17976,#17977,#17978,#17979,#17980,#17981,#17982,
#17983,#17984,#17985,#17986,#17987,#17988,#17989,#17990,#17991,#17992,#17993,
#17994,#17995,#17996,#17997,#17998,#17999,#18000,#18001,#18002)),
 .UNSPECIFIED.,.F.,.F.,.F.,(4,4),(4,1,1,1,1,1,1,1,1,1,1,1,1,1,1,1,1,1,1,
1,1,1,1,1,1,1,1,1,1,1,1,1,1,1,1,1,1,1,1,1,1,1,1,1,1,1,1,1,1,1,1,1,1,1,1,
1,1,1,1,1,1,1,1,1,1,1,1,1,1,1,1,1,1,1,1,1,1,1,1,1,1,1,1,1,1,1,1,1,1,1,1,
1,1,1,1,1,1,1,1,1,1,1,1,1,1,1,1,1,1,1,1,1,1,1,1,1,1,1,1,1,1,1,1,1,1,1,1,
1,1,1,1,1,1,1,1,1,1,1,1,1,1,1,1,1,1,1,1,1,1,1,1,1,1,1,1,1,1,1,1,1,1,1,1,
1,1,1,1,1,1,1,1,1,1,1,1,1,1,1,1,1,1,1,1,1,1,1,1,1,1,1,1,1,1,1,1,4),(0.,
0.0329955678841871),(8.30203615430855,9.30007843543257,10.2981207165566,
11.2961629976806,12.2942052788047,13.2922475599287,14.2902898410527,15.2883321221767,
16.2863744033008,17.2844166844248,18.2824589655488,19.2805012466728,20.2785435277969,
21.2765858089209,22.2746280900449,23.272670371169,24.270712652293,25.268754933417,
26.266797214541,27.2648394956651,28.2628817767891,29.2609240579131,30.2589663390371,
31.2570086201612,32.2550509012852,33.2530931824092,34.2511354635333,35.2491777446573,
36.2472200257813,37.2452623069053,38.2433045880294,39.2413468691534,40.2393891502774,
41.2374314314014,42.2354737125255,43.2335159936495,44.2315582747735,45.2296005558975,
46.2276428370216,47.2256851181456,48.2237273992696,49.2217696803937,50.2198119615177,
51.2178542426417,52.2158965237657,53.2139388048898,54.2119810860138,55.2100233671378,
56.2080656482619,57.2061079293859,58.2041502105099,59.2021924916339,60.200234772758,
61.198277053882,62.196319335006,63.19436161613,64.1924038972541,65.1904461783781,
66.1884884595021,67.1865307406262,68.1845730217502,69.1826153028742,70.1806575839982,
71.1786998651223,72.1767421462463,73.1747844273703,74.1728267084943,75.1708689896184,
76.1689112707424,77.1669535518664,78.1649958329905,79.1630381141145,80.1610803952385,
81.1591226763625,82.1571649574865,83.1552072386106,84.1532495197346,85.1512918008586,
86.1493340819827,87.1473763631067,88.1454186442307,89.1434609253548,90.1415032064788,
91.1395454876028,92.1375877687268,93.1356300498508,94.1336723309749,95.1317146120989,
96.1297568932229,97.127799174347,98.125841455471,99.123883736595,100.121926017719,
101.119968298843,102.118010579967,103.116052861091,104.114095142215,105.112137423339,
106.110179704463,107.108221985587,108.106264266711,109.104306547835,110.102348828959,
111.100391110083,112.098433391207,113.096475672331,114.094517953455,115.092560234579,
116.090602515703,117.088644796828,118.086687077952,119.084729359076,120.0827716402,
121.080813921324,122.078856202448,123.076898483572,124.074940764696,125.07298304582,
126.071025326944,127.069067608068,128.067109889192,129.065152170316,130.06319445144,
131.061236732564,132.059279013688,133.057321294812,134.055363575936,135.05340585706,
136.051448138184,137.049490419308,138.047532700432,139.045574981556,140.04361726268,
141.041659543804,142.039701824928,143.037744106052,144.035786387176,145.0338286683,
146.031870949424,147.029913230548,148.027955511672,149.025997792796,150.02404007392,
151.022082355044,152.020124636168,153.018166917292,154.016209198417,155.014251479541,
156.012293760665,157.010336041789,158.008378322913,159.006420604037,160.004462885161,
161.002505166285,162.000547447409,162.998589728533,163.996632009657,164.994674290781,
165.992716571905,166.990758853029,167.988801134153,168.986843415277,169.984885696401,
170.982927977525,171.980970258649,172.979012539773,173.977054820897,174.975097102021,
175.973139383145,176.971181664269,177.969223945393,178.967266226517,179.965308507641,
180.963350788765,181.961393069889,182.959435351013,183.957477632137,184.955519913261,
185.953562194385,186.951604475509,187.949646756633,188.947689037757,189.945731318881,
190.943773600006,191.94181588113,192.939858162254,193.937900443378,194.935942724502,
195.933985005626,196.93202728675,197.930069567874,198.928111848998,199.926154130122,
200.924196411246,201.92223869237,202.920280973494),.UNSPECIFIED.);
#390=B_SPLINE_CURVE_WITH_KNOTS('',3,(#13962,#13963,#13964,#13965,#13966,
#13967,#13968,#13969,#13970,#13971),.UNSPECIFIED.,.F.,.F.,(4,3,3,4),(-4.09202352044852,
-3.99057144343763,-2.99292858257822,-2.07317267331971),.UNSPECIFIED.);
#391=B_SPLINE_CURVE_WITH_KNOTS('',3,(#13974,#13975,#13976,#13977,#13978,
#13979,#13980),.UNSPECIFIED.,.F.,.F.,(4,3,4),(0.,0.998042281124014,1.12274180646116),
 .UNSPECIFIED.);
#392=B_SPLINE_CURVE_WITH_KNOTS('',3,(#13985,#13986,#13987,#13988,#13989,
#13990,#13991,#13992,#13993,#13994,#13995,#13996,#13997,#13998,#13999,#14000,
#14001,#14002,#14003,#14004,#14005,#14006),.UNSPECIFIED.,.F.,.F.,(4,3,3,
3,3,3,3,4),(-10.3752088276281,-9.97642860859406,-8.97878574773466,-7.98114288687525,
-6.98350002601584,-5.98585716515644,-4.98821430429703,-4.09202352044852),
 .UNSPECIFIED.);
#393=B_SPLINE_CURVE_WITH_KNOTS('',3,(#14007,#14008,#14009,#14010,#14011,
#14012,#14013,#14014,#14015,#14016,#14017,#14018,#14019,#14020,#14021,#14022,
#14023,#14024,#14025,#14026,#14027,#14028),.UNSPECIFIED.,.F.,.F.,(4,3,3,
3,3,3,3,4),(1.12274180646116,1.99608456224804,2.99412684337208,3.99216912449611,
4.99021140562014,5.98825368674417,6.98629596786821,7.40592711364074),
 .UNSPECIFIED.);
#394=B_SPLINE_CURVE_WITH_KNOTS('',3,(#14033,#14034,#14035,#14036,#14037,
#14038,#14039,#14040,#14041,#14042,#14043,#14044,#14045,#14046,#14047,#14048,
#14049,#14050,#14051,#14052,#14053,#14054),.UNSPECIFIED.,.F.,.F.,(4,3,3,
3,3,3,3,4),(-16.6583941348077,-15.9622857737505,-14.9646429128911,-13.9670000520317,
-12.9693571911723,-11.9717143303129,-10.9740714694535,-10.3752088276281),
 .UNSPECIFIED.);
#395=B_SPLINE_CURVE_WITH_KNOTS('',3,(#14055,#14056,#14057,#14058,#14059,
#14060,#14061,#14062,#14063,#14064,#14065,#14066,#14067,#14068,#14069,#14070,
#14071,#14072,#14073,#14074,#14075,#14076),.UNSPECIFIED.,.F.,.F.,(4,3,3,
3,3,3,3,4),(7.40592711364074,7.98433824899223,8.98238053011626,9.98042281124028,
10.9784650923643,11.9765073734883,12.9745496546124,13.6891124208203),
 .UNSPECIFIED.);
#396=B_SPLINE_CURVE_WITH_KNOTS('',3,(#14081,#14082,#14083,#14084,#14085,
#14086,#14087,#14088,#14089,#14090,#14091,#14092,#14093,#14094,#14095,#14096,
#14097,#14098,#14099,#14100,#14101,#14102),.UNSPECIFIED.,.F.,.F.,(4,3,3,
3,3,3,3,4),(-22.9415794419873,-21.9481429389069,-20.9505000780475,-19.9528572171881,
-18.9552143563287,-17.9575714954693,-16.9599286346099,-16.6583941348077),
 .UNSPECIFIED.);
#397=B_SPLINE_CURVE_WITH_KNOTS('',3,(#14103,#14104,#14105,#14106,#14107,
#14108,#14109,#14110,#14111,#14112,#14113,#14114,#14115,#14116,#14117,#14118,
#14119,#14120,#14121,#14122,#14123,#14124,#14125,#14126,#14127),
 .UNSPECIFIED.,.F.,.F.,(4,3,3,3,3,3,3,3,4),(13.6891124208203,13.9725919357364,
14.9706342168604,15.9686764979844,16.9667187791085,17.9647610602325,18.9628033413565,
19.9608456224805,19.9722977279999),.UNSPECIFIED.);
#398=B_SPLINE_CURVE_WITH_KNOTS('',3,(#14132,#14133,#14134,#14135,#14136,
#14137,#14138,#14139,#14140,#14141,#14142,#14143,#14144,#14145,#14146,#14147,
#14148,#14149,#14150,#14151,#14152,#14153),.UNSPECIFIED.,.F.,.F.,(4,3,3,
3,3,3,3,4),(-29.2247647491669,-28.9316429649228,-27.9340001040634,-26.936357243204,
-25.9387143823446,-24.9410715214852,-23.9434286606257,-22.9415794419873),
 .UNSPECIFIED.);
#399=B_SPLINE_CURVE_WITH_KNOTS('',3,(#14154,#14155,#14156,#14157,#14158,
#14159,#14160,#14161,#14162,#14163,#14164,#14165,#14166,#14167,#14168,#14169,
#14170,#14171,#14172,#14173,#14174,#14175),.UNSPECIFIED.,.F.,.F.,(4,3,3,
3,3,3,3,4),(19.9722977279999,20.9588879036046,21.9569301847286,22.9549724658526,
23.9530147469767,24.9510570281007,25.9490993092247,26.2554830351795),
 .UNSPECIFIED.);
#400=B_SPLINE_CURVE_WITH_KNOTS('',3,(#14180,#14181,#14182,#14183,#14184,
#14185,#14186,#14187,#14188,#14189,#14190,#14191,#14192,#14193,#14194,#14195,
#14196,#14197,#14198,#14199,#14200,#14201),.UNSPECIFIED.,.F.,.F.,(4,3,3,
3,3,3,3,4),(-35.5079500563465,-34.9175001300792,-33.9198572692198,-32.9222144083604,
-31.924571547501,-30.9269286866416,-29.9292858257822,-29.2247647491669),
 .UNSPECIFIED.);
#401=B_SPLINE_CURVE_WITH_KNOTS('',3,(#14202,#14203,#14204,#14205,#14206,
#14207,#14208,#14209,#14210,#14211,#14212,#14213,#14214,#14215,#14216,#14217,
#14218,#14219,#14220,#14221,#14222,#14223),.UNSPECIFIED.,.F.,.F.,(4,3,3,
3,3,3,3,4),(26.2554830351795,26.9471415903487,27.9451838714728,28.9432261525968,
29.9412684337208,30.9393107148448,31.9373529959689,32.5386683423591),
 .UNSPECIFIED.);
#402=B_SPLINE_CURVE_WITH_KNOTS('',3,(#14228,#14229,#14230,#14231,#14232,
#14233,#14234,#14235,#14236,#14237,#14238,#14239,#14240,#14241,#14242,#14243,
#14244,#14245,#14246,#14247,#14248,#14249),.UNSPECIFIED.,.F.,.F.,(4,3,3,
3,3,3,3,4),(-41.791135363526,-40.9033572952357,-39.9057144343762,-38.9080715735168,
-37.9104287126574,-36.912785851798,-35.9151429909386,-35.5079500563465),
 .UNSPECIFIED.);
#403=B_SPLINE_CURVE_WITH_KNOTS('',3,(#14250,#14251,#14252,#14253,#14254,
#14255,#14256,#14257,#14258,#14259,#14260,#14261,#14262,#14263,#14264,#14265,
#14266,#14267,#14268,#14269,#14270,#14271),.UNSPECIFIED.,.F.,.F.,(4,3,3,
3,3,3,3,4),(32.5386683423591,32.9353952770929,33.9334375582169,34.931479839341,
35.929522120465,36.927564401589,37.9256066827131,38.8218536495387),
 .UNSPECIFIED.);
#404=B_SPLINE_CURVE_WITH_KNOTS('',3,(#14276,#14277,#14278,#14279,#14280,
#14281,#14282,#14283,#14284,#14285,#14286,#14287,#14288,#14289,#14290,#14291,
#14292,#14293,#14294,#14295,#14296,#14297,#14298,#14299,#14300),
 .UNSPECIFIED.,.F.,.F.,(4,3,3,3,3,3,3,3,4),(-48.0743206707056,-47.8868573212515,
-46.8892144603921,-45.8915715995327,-44.8939287386733,-43.8962858778139,
-42.8986430169545,-41.9010001560951,-41.791135363526),.UNSPECIFIED.);
#405=B_SPLINE_CURVE_WITH_KNOTS('',3,(#14301,#14302,#14303,#14304,#14305,
#14306,#14307,#14308,#14309,#14310,#14311,#14312,#14313,#14314,#14315,#14316,
#14317,#14318,#14319,#14320,#14321,#14322,#14323,#14324,#14325),
 .UNSPECIFIED.,.F.,.F.,(4,3,3,3,3,3,3,3,4),(38.8218536495387,38.9236489638371,
39.9216912449611,40.9197335260851,41.9177758072091,42.9158180883332,43.9138603694572,
44.9119026505812,45.1050389567183),.UNSPECIFIED.);
#406=B_SPLINE_CURVE_WITH_KNOTS('',3,(#14330,#14331,#14332,#14333,#14334,
#14335,#14336,#14337,#14338,#14339,#14340,#14341,#14342,#14343,#14344,#14345,
#14346,#14347,#14348,#14349,#14350,#14351),.UNSPECIFIED.,.F.,.F.,(4,3,3,
3,3,3,3,4),(-54.3575059778852,-53.8727144864079,-52.8750716255485,-51.8774287646891,
-50.8797859038297,-49.8821430429703,-48.8845001821109,-48.0743206707056),
 .UNSPECIFIED.);
#407=B_SPLINE_CURVE_WITH_KNOTS('',3,(#14352,#14353,#14354,#14355,#14356,
#14357,#14358,#14359,#14360,#14361,#14362,#14363,#14364,#14365,#14366,#14367,
#14368,#14369,#14370,#14371,#14372,#14373),.UNSPECIFIED.,.F.,.F.,(4,3,3,
3,3,3,3,4),(45.1050389567183,45.9099449317052,46.9079872128293,47.9060294939533,
48.9040717750773,49.9021140562014,50.9001563373254,51.3882242638979),
 .UNSPECIFIED.);
#408=B_SPLINE_CURVE_WITH_KNOTS('',3,(#14378,#14379,#14380,#14381,#14382,
#14383,#14384,#14385,#14386,#14387,#14388,#14389,#14390,#14391,#14392,#14393,
#14394,#14395,#14396,#14397,#14398,#14399),.UNSPECIFIED.,.F.,.F.,(4,3,3,
3,3,3,3,4),(-60.6406912850648,-59.8585716515644,-58.860928790705,-57.8632859298455,
-56.8656430689861,-55.8680002081267,-54.8703573472673,-54.3575059778852),
 .UNSPECIFIED.);
#409=B_SPLINE_CURVE_WITH_KNOTS('',3,(#14400,#14401,#14402,#14403,#14404,
#14405,#14406,#14407,#14408,#14409,#14410,#14411,#14412,#14413,#14414,#14415,
#14416,#14417,#14418,#14419,#14420,#14421),.UNSPECIFIED.,.F.,.F.,(4,3,3,
3,3,3,3,4),(51.3882242638979,51.8981986184494,52.8962408995734,53.8942831806975,
54.8923254618215,55.8903677429455,56.8884100240695,57.6714095710775),
 .UNSPECIFIED.);
#410=B_SPLINE_CURVE_WITH_KNOTS('',3,(#14426,#14427,#14428,#14429,#14430,
#14431,#14432,#14433,#14434,#14435,#14436,#14437,#14438,#14439,#14440,#14441,
#14442,#14443,#14444,#14445,#14446,#14447,#14448,#14449,#14450),
 .UNSPECIFIED.,.F.,.F.,(4,3,3,3,3,3,3,3,4),(-66.9238765922444,-66.8420716775802,
-65.8444288167208,-64.8467859558614,-63.849143095002,-62.8515002341426,
-61.8538573732832,-60.8562145124238,-60.6406912850648),.UNSPECIFIED.);
#411=B_SPLINE_CURVE_WITH_KNOTS('',3,(#14451,#14452,#14453,#14454,#14455,
#14456,#14457,#14458,#14459,#14460,#14461,#14462,#14463,#14464,#14465,#14466,
#14467,#14468,#14469,#14470,#14471,#14472,#14473,#14474,#14475),
 .UNSPECIFIED.,.F.,.F.,(4,3,3,3,3,3,3,3,4),(57.6714095710775,57.8864523051936,
58.8844945863176,59.8825368674416,60.8805791485657,61.8786214296897,62.8766637108137,
63.8747059919378,63.9545948782571),.UNSPECIFIED.);
#412=B_SPLINE_CURVE_WITH_KNOTS('',3,(#14480,#14481,#14482,#14483,#14484,
#14485,#14486,#14487,#14488,#14489,#14490,#14491,#14492,#14493,#14494,#14495,
#14496,#14497,#14498,#14499,#14500,#14501),.UNSPECIFIED.,.F.,.F.,(4,3,3,
3,3,3,3,4),(-73.207061899424,-72.8279288427366,-71.8302859818773,-70.8326431210178,
-69.8350002601584,-68.837357399299,-67.8397145384396,-66.9238765922444),
 .UNSPECIFIED.);
#413=B_SPLINE_CURVE_WITH_KNOTS('',3,(#14502,#14503,#14504,#14505,#14506,
#14507,#14508,#14509,#14510,#14511,#14512,#14513,#14514,#14515,#14516,#14517,
#14518,#14519,#14520,#14521,#14522,#14523),.UNSPECIFIED.,.F.,.F.,(4,3,3,
3,3,3,3,4),(63.9545948782571,64.8727482730618,65.8707905541858,66.8688328353098,
67.8668751164338,68.8649173975579,69.8629596786819,70.2377801854366),
 .UNSPECIFIED.);
#414=B_SPLINE_CURVE_WITH_KNOTS('',3,(#14528,#14529,#14530,#14531,#14532,
#14533,#14534,#14535,#14536,#14537,#14538,#14539,#14540,#14541,#14542,#14543,
#14544,#14545,#14546,#14547,#14548,#14549),.UNSPECIFIED.,.F.,.F.,(4,3,3,
3,3,3,3,4),(-79.4902472066036,-78.8137860078931,-77.8161431470337,-76.8185002861743,
-75.8208574253149,-74.8232145644555,-73.825571703596,-73.207061899424),
 .UNSPECIFIED.);
#415=B_SPLINE_CURVE_WITH_KNOTS('',3,(#14550,#14551,#14552,#14553,#14554,
#14555,#14556,#14557,#14558,#14559,#14560,#14561,#14562,#14563,#14564,#14565,
#14566,#14567,#14568,#14569,#14570,#14571),.UNSPECIFIED.,.F.,.F.,(4,3,3,
3,3,3,3,4),(70.2377801854366,70.8610019598059,71.85904424093,72.857086522054,
73.855128803178,74.853171084302,75.8512133654261,76.5209654926162),
 .UNSPECIFIED.);
#416=B_SPLINE_CURVE_WITH_KNOTS('',3,(#14576,#14577,#14578,#14579,#14580,
#14581,#14582,#14583,#14584,#14585,#14586,#14587,#14588,#14589,#14590,#14591,
#14592,#14593,#14594,#14595,#14596,#14597),.UNSPECIFIED.,.F.,.F.,(4,3,3,
3,3,3,3,4),(-85.7734325137832,-84.7996431730495,-83.8020003121901,-82.8043574513307,
-81.8067145904713,-80.8090717296119,-79.8114288687525,-79.4902472066036),
 .UNSPECIFIED.);
#417=B_SPLINE_CURVE_WITH_KNOTS('',3,(#14598,#14599,#14600,#14601,#14602,
#14603,#14604,#14605,#14606,#14607,#14608,#14609,#14610,#14611,#14612,#14613,
#14614,#14615,#14616,#14617,#14618,#14619),.UNSPECIFIED.,.F.,.F.,(4,3,3,
3,3,3,3,4),(76.5209654926162,76.8492556465501,77.8472979276741,78.8453402087982,
79.8433824899222,80.8414247710462,81.8394670521702,82.8041507997958),
 .UNSPECIFIED.);
#418=B_SPLINE_CURVE_WITH_KNOTS('',3,(#14624,#14625,#14626,#14627,#14628,
#14629,#14630,#14631,#14632,#14633,#14634,#14635,#14636,#14637,#14638,#14639,
#14640,#14641,#14642,#14643,#14644,#14645,#14646,#14647,#14648),
 .UNSPECIFIED.,.F.,.F.,(4,3,3,3,3,3,3,3,4),(-92.0566178209628,-91.7831431990654,
-90.7855003382059,-89.7878574773465,-88.7902146164871,-87.7925717556277,
-86.7949288947683,-85.7972860339089,-85.7734325137832),.UNSPECIFIED.);
#419=B_SPLINE_CURVE_WITH_KNOTS('',3,(#14649,#14650,#14651,#14652,#14653,
#14654,#14655,#14656,#14657,#14658,#14659,#14660,#14661,#14662,#14663,#14664,
#14665,#14666,#14667,#14668,#14669,#14670,#14671,#14672,#14673),
 .UNSPECIFIED.,.F.,.F.,(4,3,3,3,3,3,3,3,4),(82.8041507997958,82.8375093332942,
83.8355516144183,84.8335938955423,85.8316361766664,86.8296784577904,87.8277207389144,
88.8257630200384,89.0873361069754),.UNSPECIFIED.);
#420=B_SPLINE_CURVE_WITH_KNOTS('',3,(#14678,#14679,#14680,#14681,#14682,
#14683,#14684,#14685,#14686,#14687,#14688,#14689,#14690,#14691,#14692,#14693,
#14694,#14695,#14696,#14697,#14698,#14699),.UNSPECIFIED.,.F.,.F.,(4,3,3,
3,3,3,3,4),(-98.3398031281424,-97.7690003642218,-96.7713575033624,-95.773714642503,
-94.7760717816436,-93.7784289207842,-92.7807860599248,-92.0566178209628),
 .UNSPECIFIED.);
#421=B_SPLINE_CURVE_WITH_KNOTS('',3,(#14700,#14701,#14702,#14703,#14704,
#14705,#14706,#14707,#14708,#14709,#14710,#14711,#14712,#14713,#14714,#14715,
#14716,#14717,#14718,#14719,#14720,#14721),.UNSPECIFIED.,.F.,.F.,(4,3,3,
3,3,3,3,4),(89.0873361069754,89.8238053011624,90.8218475822865,91.8198898634105,
92.8179321445345,93.8159744256585,94.8140167067826,95.370521414155),
 .UNSPECIFIED.);
#422=B_SPLINE_CURVE_WITH_KNOTS('',3,(#14726,#14727,#14728,#14729,#14730,
#14731,#14732,#14733,#14734,#14735,#14736,#14737,#14738,#14739,#14740,#14741,
#14742,#14743,#14744,#14745,#14746,#14747),.UNSPECIFIED.,.F.,.F.,(4,3,3,
3,3,3,3,4),(-104.622988435322,-103.754857529378,-102.757214668519,-101.759571807659,
-100.7619289468,-99.7642860859406,-98.7666432250812,-98.3398031281424),
 .UNSPECIFIED.);
#423=B_SPLINE_CURVE_WITH_KNOTS('',3,(#14748,#14749,#14750,#14751,#14752,
#14753,#14754,#14755,#14756,#14757,#14758,#14759,#14760,#14761,#14762,#14763,
#14764,#14765,#14766,#14767,#14768,#14769),.UNSPECIFIED.,.F.,.F.,(4,3,3,
3,3,3,3,4),(95.370521414155,95.8120589879066,96.8101012690306,97.8081435501546,
98.8061858312787,99.8042281124027,100.802270393527,101.653706721335),
 .UNSPECIFIED.);
#424=B_SPLINE_CURVE_WITH_KNOTS('',3,(#14774,#14775,#14776,#14777,#14778,
#14779,#14780,#14781,#14782,#14783,#14784,#14785,#14786,#14787,#14788,#14789,
#14790,#14791,#14792,#14793,#14794,#14795,#14796,#14797,#14798),
 .UNSPECIFIED.,.F.,.F.,(4,3,3,3,3,3,3,3,4),(-110.906173742502,-110.738357555394,
-109.740714694535,-108.743071833675,-107.745428972816,-106.747786111956,
-105.750143251097,-104.752500390238,-104.622988435322),.UNSPECIFIED.);
#425=B_SPLINE_CURVE_WITH_KNOTS('',3,(#14799,#14800,#14801,#14802,#14803,
#14804,#14805,#14806,#14807,#14808,#14809,#14810,#14811,#14812,#14813,#14814,
#14815,#14816,#14817,#14818,#14819,#14820,#14821,#14822,#14823),
 .UNSPECIFIED.,.F.,.F.,(4,3,3,3,3,3,3,3,4),(101.653706721335,101.800312674651,
102.798354955775,103.796397236899,104.794439518023,105.792481799147,106.790524080271,
107.788566361395,107.936892028514),.UNSPECIFIED.);
#426=B_SPLINE_CURVE_WITH_KNOTS('',3,(#14828,#14829,#14830,#14831,#14832,
#14833,#14834,#14835,#14836,#14837,#14838,#14839,#14840,#14841,#14842,#14843,
#14844,#14845,#14846,#14847,#14848,#14849),.UNSPECIFIED.,.F.,.F.,(4,3,3,
3,3,3,3,4),(-117.189359049681,-116.724214720551,-115.726571859691,-114.728928998832,
-113.731286137972,-112.733643277113,-111.736000416253,-110.906173742502),
 .UNSPECIFIED.);
#427=B_SPLINE_CURVE_WITH_KNOTS('',3,(#14850,#14851,#14852,#14853,#14854,
#14855,#14856,#14857,#14858,#14859,#14860,#14861,#14862,#14863,#14864,#14865,
#14866,#14867,#14868,#14869,#14870,#14871),.UNSPECIFIED.,.F.,.F.,(4,3,3,
3,3,3,3,4),(107.936892028514,108.786608642519,109.784650923643,110.782693204767,
111.780735485891,112.778777767015,113.776820048139,114.220077335694),
 .UNSPECIFIED.);
#428=B_SPLINE_CURVE_WITH_KNOTS('',3,(#14876,#14877,#14878,#14879,#14880,
#14881,#14882,#14883,#14884,#14885,#14886,#14887,#14888,#14889,#14890,#14891,
#14892,#14893,#14894,#14895,#14896,#14897),.UNSPECIFIED.,.F.,.F.,(4,3,3,
3,3,3,3,4),(-123.472544356861,-122.710071885707,-121.712429024848,-120.714786163988,
-119.717143303129,-118.719500442269,-117.72185758141,-117.189359049681),
 .UNSPECIFIED.);
#429=B_SPLINE_CURVE_WITH_KNOTS('',3,(#14898,#14899,#14900,#14901,#14902,
#14903,#14904,#14905,#14906,#14907,#14908,#14909,#14910,#14911,#14912,#14913,
#14914,#14915,#14916,#14917,#14918,#14919),.UNSPECIFIED.,.F.,.F.,(4,3,3,
3,3,3,3,4),(114.220077335694,114.774862329263,115.772904610387,116.770946891511,
117.768989172635,118.767031453759,119.765073734883,120.503262642873),
 .UNSPECIFIED.);
#430=B_SPLINE_CURVE_WITH_KNOTS('',3,(#14924,#14925,#14926,#14927,#14928,
#14929,#14930,#14931,#14932,#14933,#14934,#14935,#14936,#14937,#14938,#14939,
#14940,#14941,#14942,#14943,#14944,#14945,#14946,#14947,#14948),
 .UNSPECIFIED.,.F.,.F.,(4,3,3,3,3,3,3,3,4),(-129.75572966404,-129.693571911723,
-128.695929050863,-127.698286190004,-126.700643329145,-125.703000468285,
-124.705357607426,-123.707714746566,-123.472544356861),.UNSPECIFIED.);
#431=B_SPLINE_CURVE_WITH_KNOTS('',3,(#14949,#14950,#14951,#14952,#14953,
#14954,#14955,#14956,#14957,#14958,#14959,#14960,#14961,#14962,#14963,#14964,
#14965,#14966,#14967,#14968,#14969,#14970,#14971,#14972,#14973),
 .UNSPECIFIED.,.F.,.F.,(4,3,3,3,3,3,3,3,4),(120.503262642873,120.763116016007,
121.761158297131,122.759200578255,123.757242859379,124.755285140503,125.753327421627,
126.751369702751,126.786447950053),.UNSPECIFIED.);
#432=B_SPLINE_CURVE_WITH_KNOTS('',3,(#14978,#14979,#14980,#14981,#14982,
#14983,#14984,#14985,#14986,#14987,#14988,#14989,#14990,#14991,#14992,#14993,
#14994,#14995,#14996,#14997,#14998,#14999),.UNSPECIFIED.,.F.,.F.,(4,3,3,
3,3,3,3,4),(-136.03891497122,-135.679429076879,-134.68178621602,-133.68414335516,
-132.686500494301,-131.688857633442,-130.691214772582,-129.75572966404),
 .UNSPECIFIED.);
#433=B_SPLINE_CURVE_WITH_KNOTS('',3,(#15000,#15001,#15002,#15003,#15004,
#15005,#15006,#15007,#15008,#15009,#15010,#15011,#15012,#15013,#15014,#15015,
#15016,#15017,#15018,#15019,#15020,#15021),.UNSPECIFIED.,.F.,.F.,(4,3,3,
3,3,3,3,4),(126.786447950053,127.749411983875,128.747454265,129.745496546124,
130.743538827248,131.741581108372,132.739623389496,133.069633257233),
 .UNSPECIFIED.);
#434=B_SPLINE_CURVE_WITH_KNOTS('',3,(#15026,#15027,#15028,#15029,#15030,
#15031,#15032,#15033,#15034,#15035,#15036,#15037,#15038,#15039,#15040,#15041,
#15042,#15043,#15044,#15045,#15046,#15047),.UNSPECIFIED.,.F.,.F.,(4,3,3,
3,3,3,3,4),(-142.322100278399,-141.665286242036,-140.667643381176,-139.670000520317,
-138.672357659457,-137.674714798598,-136.677071937739,-136.03891497122),
 .UNSPECIFIED.);
#435=B_SPLINE_CURVE_WITH_KNOTS('',3,(#15048,#15049,#15050,#15051,#15052,
#15053,#15054,#15055,#15056,#15057,#15058,#15059,#15060,#15061,#15062,#15063,
#15064,#15065,#15066,#15067,#15068,#15069),.UNSPECIFIED.,.F.,.F.,(4,3,3,
3,3,3,3,4),(133.069633257233,133.73766567062,134.735707951744,135.733750232868,
136.731792513992,137.729834795116,138.72787707624,139.352818564412),
 .UNSPECIFIED.);
#436=B_SPLINE_CURVE_WITH_KNOTS('',3,(#15074,#15075,#15076,#15077,#15078,
#15079,#15080,#15081,#15082,#15083,#15084,#15085,#15086,#15087,#15088,#15089,
#15090,#15091,#15092,#15093,#15094,#15095),.UNSPECIFIED.,.F.,.F.,(4,3,3,
3,3,3,3,4),(-148.605285585579,-147.651143407192,-146.653500546333,-145.655857685473,
-144.658214824614,-143.660571963754,-142.662929102895,-142.322100278399),
 .UNSPECIFIED.);
#437=B_SPLINE_CURVE_WITH_KNOTS('',3,(#15096,#15097,#15098,#15099,#15100,
#15101,#15102,#15103,#15104,#15105,#15106,#15107,#15108,#15109,#15110,#15111,
#15112,#15113,#15114,#15115,#15116,#15117),.UNSPECIFIED.,.F.,.F.,(4,3,3,
3,3,3,3,4),(139.352818564412,139.725919357364,140.723961638488,141.722003919612,
142.720046200736,143.71808848186,144.716130762984,145.636003871592),
 .UNSPECIFIED.);
#438=B_SPLINE_CURVE_WITH_KNOTS('',3,(#15122,#15123,#15124,#15125,#15126,
#15127,#15128,#15129,#15130,#15131,#15132,#15133,#15134,#15135,#15136,#15137,
#15138,#15139,#15140,#15141,#15142,#15143,#15144,#15145,#15146),
 .UNSPECIFIED.,.F.,.F.,(4,3,3,3,3,3,3,3,4),(-154.888470892759,-154.634643433208,
-153.637000572349,-152.639357711489,-151.64171485063,-150.64407198977,-149.646429128911,
-148.648786268052,-148.605285585579),.UNSPECIFIED.);
#439=B_SPLINE_CURVE_WITH_KNOTS('',3,(#15147,#15148,#15149,#15150,#15151,
#15152,#15153,#15154,#15155,#15156,#15157,#15158,#15159,#15160,#15161,#15162,
#15163,#15164,#15165,#15166,#15167,#15168,#15169,#15170,#15171),
 .UNSPECIFIED.,.F.,.F.,(4,3,3,3,3,3,3,3,4),(145.636003871592,145.714173044108,
146.712215325232,147.710257606356,148.70829988748,149.706342168604,150.704384449728,
151.702426730852,151.919189178771),.UNSPECIFIED.);
#440=B_SPLINE_CURVE_WITH_KNOTS('',3,(#15176,#15177,#15178,#15179,#15180,
#15181,#15182,#15183,#15184,#15185,#15186,#15187,#15188,#15189,#15190,#15191,
#15192,#15193,#15194,#15195,#15196,#15197),.UNSPECIFIED.,.F.,.F.,(4,3,3,
3,3,3,3,4),(-161.171656199938,-160.620500598364,-159.622857737505,-158.625214876646,
-157.627572015786,-156.629929154927,-155.632286294067,-154.888470892759),
 .UNSPECIFIED.);
#441=B_SPLINE_CURVE_WITH_KNOTS('',3,(#15198,#15199,#15200,#15201,#15202,
#15203,#15204,#15205,#15206,#15207,#15208,#15209,#15210,#15211,#15212,#15213,
#15214,#15215,#15216,#15217,#15218,#15219),.UNSPECIFIED.,.F.,.F.,(4,3,3,
3,3,3,3,4),(151.919189178771,152.700469011976,153.6985112931,154.696553574224,
155.694595855348,156.692638136472,157.690680417596,158.202374485951),
 .UNSPECIFIED.);
#442=B_SPLINE_CURVE_WITH_KNOTS('',3,(#15224,#15225,#15226,#15227,#15228,
#15229,#15230,#15231,#15232,#15233,#15234,#15235,#15236,#15237,#15238,#15239,
#15240,#15241,#15242,#15243,#15244,#15245),.UNSPECIFIED.,.F.,.F.,(4,3,3,
3,3,3,3,4),(-167.454841507118,-166.606357763521,-165.608714902661,-164.611072041802,
-163.613429180943,-162.615786320083,-161.618143459224,-161.171656199938),
 .UNSPECIFIED.);
#443=B_SPLINE_CURVE_WITH_KNOTS('',3,(#15246,#15247,#15248,#15249,#15250,
#15251,#15252,#15253,#15254,#15255,#15256,#15257,#15258,#15259,#15260,#15261,
#15262,#15263,#15264,#15265,#15266,#15267),.UNSPECIFIED.,.F.,.F.,(4,3,3,
3,3,3,3,4),(158.202374485951,158.68872269872,159.686764979844,160.684807260968,
161.682849542092,162.680891823216,163.67893410434,164.48555979313),
 .UNSPECIFIED.);
#444=B_SPLINE_CURVE_WITH_KNOTS('',3,(#15272,#15273,#15274,#15275,#15276,
#15277,#15278,#15279,#15280,#15281,#15282,#15283,#15284,#15285,#15286,#15287,
#15288,#15289,#15290,#15291,#15292,#15293,#15294,#15295,#15296),
 .UNSPECIFIED.,.F.,.F.,(4,3,3,3,3,3,3,3,4),(-173.738026814297,-173.589857789537,
-172.592214928677,-171.594572067818,-170.596929206958,-169.599286346099,
-168.60164348524,-167.60400062438,-167.454841507118),.UNSPECIFIED.);
#445=B_SPLINE_CURVE_WITH_KNOTS('',3,(#15297,#15298,#15299,#15300,#15301,
#15302,#15303,#15304,#15305,#15306,#15307,#15308,#15309,#15310,#15311,#15312,
#15313,#15314,#15315,#15316,#15317,#15318,#15319,#15320,#15321),
 .UNSPECIFIED.,.F.,.F.,(4,3,3,3,3,3,3,3,4),(164.48555979313,164.676976385465,
165.675018666588,166.673060947713,167.671103228837,168.669145509961,169.667187791085,
170.665230072209,170.76874510031),.UNSPECIFIED.);
#446=B_SPLINE_CURVE_WITH_KNOTS('',3,(#15326,#15327,#15328,#15329,#15330,
#15331,#15332,#15333,#15334,#15335,#15336,#15337,#15338,#15339,#15340,#15341,
#15342,#15343,#15344,#15345,#15346,#15347),.UNSPECIFIED.,.F.,.F.,(4,3,3,
3,3,3,3,4),(-180.021212121477,-179.575714954693,-178.578072093834,-177.580429232974,
-176.582786372115,-175.585143511255,-174.587500650396,-173.738026814297),
 .UNSPECIFIED.);
#447=B_SPLINE_CURVE_WITH_KNOTS('',3,(#15348,#15349,#15350,#15351,#15352,
#15353,#15354,#15355,#15356,#15357,#15358,#15359,#15360,#15361,#15362,#15363,
#15364,#15365,#15366,#15367,#15368,#15369),.UNSPECIFIED.,.F.,.F.,(4,3,3,
3,3,3,3,4),(170.76874510031,171.663272353333,172.661314634457,173.659356915581,
174.657399196705,175.655441477829,176.653483758953,177.051930407489),
 .UNSPECIFIED.);
#448=B_SPLINE_CURVE_WITH_KNOTS('',3,(#15374,#15375,#15376,#15377,#15378,
#15379,#15380,#15381,#15382,#15383,#15384,#15385,#15386,#15387,#15388,#15389,
#15390,#15391,#15392,#15393,#15394,#15395),.UNSPECIFIED.,.F.,.F.,(4,3,3,
3,3,3,3,4),(-186.304397428656,-185.56157211985,-184.56392925899,-183.566286398131,
-182.568643537271,-181.571000676412,-180.573357815553,-180.021212121477),
 .UNSPECIFIED.);
#449=B_SPLINE_CURVE_WITH_KNOTS('',3,(#15396,#15397,#15398,#15399,#15400,
#15401,#15402,#15403,#15404,#15405,#15406,#15407,#15408,#15409,#15410,#15411,
#15412,#15413,#15414,#15415,#15416,#15417),.UNSPECIFIED.,.F.,.F.,(4,3,3,
3,3,3,3,4),(177.051930407489,177.651526040077,178.649568321201,179.647610602325,
180.645652883449,181.643695164573,182.641737445697,183.335115714669),
 .UNSPECIFIED.);
#450=B_SPLINE_CURVE_WITH_KNOTS('',3,(#15423,#15424,#15425,#15426,#15427,
#15428,#15429,#15430,#15431,#15432),.UNSPECIFIED.,.F.,.F.,(4,1,1,1,1,1,
1,4),(197.920337176157,198.17515472821,199.172797589069,200.170440449928,
201.168083310788,202.165726171647,203.163369032507,204.161011893366),
 .UNSPECIFIED.);
#451=B_SPLINE_CURVE_WITH_KNOTS('',3,(#15435,#15436,#15437,#15438,#15439,
#15440,#15441,#15442,#15443),.UNSPECIFIED.,.F.,.F.,(4,1,1,1,1,1,4),(197.920337176157,
197.930069567874,198.928111848998,199.926154130122,200.924196411246,201.92223869237,
202.920280973494),.UNSPECIFIED.);
#452=B_SPLINE_CURVE_WITH_KNOTS('',3,(#15448,#15449,#15450,#15451,#15452,
#15453,#15454,#15455,#15456,#15457),.UNSPECIFIED.,.F.,.F.,(4,1,1,1,1,1,
1,4),(191.637151868977,192.189297563053,193.186940423913,194.184583284772,
195.182226145631,196.179869006491,197.17751186735,197.920337176157),
 .UNSPECIFIED.);
#453=B_SPLINE_CURVE_WITH_KNOTS('',3,(#15458,#15459,#15460,#15461,#15462,
#15463,#15464,#15465,#15466,#15467),.UNSPECIFIED.,.F.,.F.,(4,1,1,1,1,1,
1,4),(191.637151868977,191.94181588113,192.939858162254,193.937900443378,
194.935942724502,195.933985005626,196.93202728675,197.920337176157),
 .UNSPECIFIED.);
#454=B_SPLINE_CURVE_WITH_KNOTS('',3,(#15472,#15473,#15474,#15475,#15476,
#15477,#15478,#15479,#15480,#15481),.UNSPECIFIED.,.F.,.F.,(4,1,1,1,1,1,
1,4),(185.353966561798,186.203440397897,187.201083258756,188.198726119616,
189.196368980475,190.194011841334,191.191654702194,191.637151868977),
 .UNSPECIFIED.);
#455=B_SPLINE_CURVE_WITH_KNOTS('',3,(#15482,#15483,#15484,#15485,#15486,
#15487,#15488,#15489,#15490,#15491),.UNSPECIFIED.,.F.,.F.,(4,1,1,1,1,1,
1,4),(185.353966561798,185.953562194385,186.951604475509,187.949646756633,
188.947689037757,189.945731318881,190.943773600006,191.637151868977),
 .UNSPECIFIED.);
#456=B_SPLINE_CURVE_WITH_KNOTS('',3,(#15496,#15497,#15498,#15499,#15500,
#15501,#15502,#15503,#15504,#15505,#15506),.UNSPECIFIED.,.F.,.F.,(4,1,1,
1,1,1,1,1,4),(179.070781254618,179.219940371881,180.21758323274,181.2152260936,
182.212868954459,183.210511815318,184.208154676178,185.205797537037,185.353966561798),
 .UNSPECIFIED.);
#457=B_SPLINE_CURVE_WITH_KNOTS('',3,(#15507,#15508,#15509,#15510,#15511,
#15512,#15513,#15514,#15515,#15516),.UNSPECIFIED.,.F.,.F.,(4,1,1,1,1,1,
1,4),(179.070781254618,179.965308507641,180.963350788765,181.961393069889,
182.959435351013,183.957477632137,184.955519913261,185.353966561798),
 .UNSPECIFIED.);
#458=B_SPLINE_CURVE_WITH_KNOTS('',3,(#15521,#15522,#15523,#15524,#15525,
#15526,#15527,#15528,#15529,#15530),.UNSPECIFIED.,.F.,.F.,(4,1,1,1,1,1,
1,4),(172.787595947439,173.234083206724,174.231726067584,175.229368928443,
176.227011789303,177.224654650162,178.222297511021,179.070781254618),
 .UNSPECIFIED.);
#459=B_SPLINE_CURVE_WITH_KNOTS('',3,(#15531,#15532,#15533,#15534,#15535,
#15536,#15537,#15538,#15539,#15540,#15541),.UNSPECIFIED.,.F.,.F.,(4,1,1,
1,1,1,1,1,4),(172.787595947439,172.979012539773,173.977054820897,174.975097102021,
175.973139383145,176.971181664269,177.969223945393,178.967266226517,179.070781254618),
 .UNSPECIFIED.);
#460=B_SPLINE_CURVE_WITH_KNOTS('',3,(#15546,#15547,#15548,#15549,#15550,
#15551,#15552,#15553,#15554,#15555),.UNSPECIFIED.,.F.,.F.,(4,1,1,1,1,1,
1,4),(166.504410640259,167.248226041568,168.245868902427,169.243511763287,
170.241154624146,171.238797485006,172.236440345865,172.787595947439),
 .UNSPECIFIED.);
#461=B_SPLINE_CURVE_WITH_KNOTS('',3,(#15556,#15557,#15558,#15559,#15560,
#15561,#15562,#15563,#15564,#15565),.UNSPECIFIED.,.F.,.F.,(4,1,1,1,1,1,
1,4),(166.504410640259,166.990758853029,167.988801134153,168.986843415277,
169.984885696401,170.982927977525,171.980970258649,172.787595947439),
 .UNSPECIFIED.);
#462=B_SPLINE_CURVE_WITH_KNOTS('',3,(#15570,#15571,#15572,#15573,#15574,
#15575,#15576,#15577,#15578,#15579,#15580),.UNSPECIFIED.,.F.,.F.,(4,1,1,
1,1,1,1,1,4),(160.22122533308,160.264726015552,161.262368876412,162.260011737271,
163.25765459813,164.25529745899,165.252940319849,166.250583180709,166.504410640259),
 .UNSPECIFIED.);
#463=B_SPLINE_CURVE_WITH_KNOTS('',3,(#15581,#15582,#15583,#15584,#15585,
#15586,#15587,#15588,#15589,#15590),.UNSPECIFIED.,.F.,.F.,(4,1,1,1,1,1,
1,4),(160.22122533308,161.002505166285,162.000547447409,162.998589728533,
163.996632009657,164.994674290781,165.992716571905,166.504410640259),
 .UNSPECIFIED.);
#464=B_SPLINE_CURVE_WITH_KNOTS('',3,(#15595,#15596,#15597,#15598,#15599,
#15600,#15601,#15602,#15603,#15604),.UNSPECIFIED.,.F.,.F.,(4,1,1,1,1,1,
1,4),(153.9380400259,154.278868850396,155.276511711255,156.274154572115,
157.271797432974,158.269440293833,159.267083154693,160.22122533308),
 .UNSPECIFIED.);
#465=B_SPLINE_CURVE_WITH_KNOTS('',3,(#15605,#15606,#15607,#15608,#15609,
#15610,#15611,#15612,#15613,#15614,#15615),.UNSPECIFIED.,.F.,.F.,(4,1,1,
1,1,1,1,1,4),(153.9380400259,154.016209198417,155.014251479541,156.012293760665,
157.010336041789,158.008378322913,159.006420604037,160.004462885161,160.22122533308),
 .UNSPECIFIED.);
#466=B_SPLINE_CURVE_WITH_KNOTS('',3,(#15620,#15621,#15622,#15623,#15624,
#15625,#15626,#15627,#15628,#15629),.UNSPECIFIED.,.F.,.F.,(4,1,1,1,1,1,
1,4),(147.65485471872,148.293011685239,149.290654546099,150.288297406958,
151.285940267817,152.283583128677,153.281225989536,153.9380400259),
 .UNSPECIFIED.);
#467=B_SPLINE_CURVE_WITH_KNOTS('',3,(#15630,#15631,#15632,#15633,#15634,
#15635,#15636,#15637,#15638,#15639),.UNSPECIFIED.,.F.,.F.,(4,1,1,1,1,1,
1,4),(147.65485471872,148.027955511672,149.025997792796,150.02404007392,
151.022082355044,152.020124636168,153.018166917292,153.9380400259),
 .UNSPECIFIED.);
#468=B_SPLINE_CURVE_WITH_KNOTS('',3,(#15644,#15645,#15646,#15647,#15648,
#15649,#15650,#15651,#15652,#15653),.UNSPECIFIED.,.F.,.F.,(4,1,1,1,1,1,
1,4),(141.371669411541,142.307154520083,143.304797380942,144.302440241802,
145.300083102661,146.29772596352,147.29536882438,147.65485471872),
 .UNSPECIFIED.);
#469=B_SPLINE_CURVE_WITH_KNOTS('',3,(#15654,#15655,#15656,#15657,#15658,
#15659,#15660,#15661,#15662,#15663),.UNSPECIFIED.,.F.,.F.,(4,1,1,1,1,1,
1,4),(141.371669411541,142.039701824928,143.037744106052,144.035786387176,
145.0338286683,146.031870949424,147.029913230548,147.65485471872),
 .UNSPECIFIED.);
#470=B_SPLINE_CURVE_WITH_KNOTS('',3,(#15668,#15669,#15670,#15671,#15672,
#15673,#15674,#15675,#15676,#15677,#15678),.UNSPECIFIED.,.F.,.F.,(4,1,1,
1,1,1,1,1,4),(135.088484104361,135.323654494067,136.321297354926,137.318940215786,
138.316583076645,139.314225937505,140.311868798364,141.309511659223,141.371669411541),
 .UNSPECIFIED.);
#471=B_SPLINE_CURVE_WITH_KNOTS('',3,(#15679,#15680,#15681,#15682,#15683,
#15684,#15685,#15686,#15687,#15688),.UNSPECIFIED.,.F.,.F.,(4,1,1,1,1,1,
1,4),(135.088484104361,136.051448138184,137.049490419308,138.047532700432,
139.045574981556,140.04361726268,141.041659543804,141.371669411541),
 .UNSPECIFIED.);
#472=B_SPLINE_CURVE_WITH_KNOTS('',3,(#15693,#15694,#15695,#15696,#15697,
#15698,#15699,#15700,#15701,#15702),.UNSPECIFIED.,.F.,.F.,(4,1,1,1,1,1,
1,4),(128.805298797182,129.337797328911,130.33544018977,131.333083050629,
132.330725911489,133.328368772348,134.326011633208,135.088484104361),
 .UNSPECIFIED.);
#473=B_SPLINE_CURVE_WITH_KNOTS('',3,(#15703,#15704,#15705,#15706,#15707,
#15708,#15709,#15710,#15711,#15712,#15713),.UNSPECIFIED.,.F.,.F.,(4,1,1,
1,1,1,1,1,4),(128.805298797182,129.065152170316,130.06319445144,131.061236732564,
132.059279013688,133.057321294812,134.055363575936,135.05340585706,135.088484104361),
 .UNSPECIFIED.);
#474=B_SPLINE_CURVE_WITH_KNOTS('',3,(#15718,#15719,#15720,#15721,#15722,
#15723,#15724,#15725,#15726,#15727),.UNSPECIFIED.,.F.,.F.,(4,1,1,1,1,1,
1,4),(122.522113490002,123.351940163754,124.349583024614,125.347225885473,
126.344868746332,127.342511607192,128.340154468051,128.805298797182),
 .UNSPECIFIED.);
#475=B_SPLINE_CURVE_WITH_KNOTS('',3,(#15728,#15729,#15730,#15731,#15732,
#15733,#15734,#15735,#15736,#15737),.UNSPECIFIED.,.F.,.F.,(4,1,1,1,1,1,
1,4),(122.522113490002,123.076898483572,124.074940764696,125.07298304582,
126.071025326944,127.069067608068,128.067109889192,128.805298797182),
 .UNSPECIFIED.);
#476=B_SPLINE_CURVE_WITH_KNOTS('',3,(#15742,#15743,#15744,#15745,#15746,
#15747,#15748,#15749,#15750,#15751,#15752),.UNSPECIFIED.,.F.,.F.,(4,1,1,
1,1,1,1,1,4),(116.238928182823,116.368440137738,117.366082998598,118.363725859457,
119.361368720316,120.359011581176,121.356654442035,122.354297302895,122.522113490002),
 .UNSPECIFIED.);
#477=B_SPLINE_CURVE_WITH_KNOTS('',3,(#15753,#15754,#15755,#15756,#15757,
#15758,#15759,#15760,#15761,#15762),.UNSPECIFIED.,.F.,.F.,(4,1,1,1,1,1,
1,4),(116.238928182823,117.088644796828,118.086687077952,119.084729359076,
120.0827716402,121.080813921324,122.078856202448,122.522113490002),
 .UNSPECIFIED.);
#478=B_SPLINE_CURVE_WITH_KNOTS('',3,(#15767,#15768,#15769,#15770,#15771,
#15772,#15773,#15774,#15775,#15776),.UNSPECIFIED.,.F.,.F.,(4,1,1,1,1,1,
1,4),(109.955742875643,110.382582972582,111.380225833441,112.377868694301,
113.37551155516,114.373154416019,115.370797276879,116.238928182823),
 .UNSPECIFIED.);
#479=B_SPLINE_CURVE_WITH_KNOTS('',3,(#15777,#15778,#15779,#15780,#15781,
#15782,#15783,#15784,#15785,#15786,#15787),.UNSPECIFIED.,.F.,.F.,(4,1,1,
1,1,1,1,1,4),(109.955742875643,110.102348828959,111.100391110083,112.098433391207,
113.096475672331,114.094517953455,115.092560234579,116.090602515703,116.238928182823),
 .UNSPECIFIED.);
#480=B_SPLINE_CURVE_WITH_KNOTS('',3,(#15792,#15793,#15794,#15795,#15796,
#15797,#15798,#15799,#15800,#15801),.UNSPECIFIED.,.F.,.F.,(4,1,1,1,1,1,
1,4),(103.672557568463,104.396725807425,105.394368668285,106.392011529144,
107.389654390004,108.387297250863,109.384940111722,109.955742875643),
 .UNSPECIFIED.);
#481=B_SPLINE_CURVE_WITH_KNOTS('',3,(#15802,#15803,#15804,#15805,#15806,
#15807,#15808,#15809,#15810,#15811),.UNSPECIFIED.,.F.,.F.,(4,1,1,1,1,1,
1,4),(103.672557568463,104.114095142215,105.112137423339,106.110179704463,
107.108221985587,108.106264266711,109.104306547835,109.955742875643),
 .UNSPECIFIED.);
#482=B_SPLINE_CURVE_WITH_KNOTS('',3,(#15816,#15817,#15818,#15819,#15820,
#15821,#15822,#15823,#15824,#15825,#15826),.UNSPECIFIED.,.F.,.F.,(4,1,1,
1,1,1,1,1,4),(97.3893722612837,97.4132257814096,98.410868642269,99.4085115031284,
100.406154363988,101.403797224847,102.401440085707,103.399082946566,103.672557568463),
 .UNSPECIFIED.);
#483=B_SPLINE_CURVE_WITH_KNOTS('',3,(#15827,#15828,#15829,#15830,#15831,
#15832,#15833,#15834,#15835,#15836),.UNSPECIFIED.,.F.,.F.,(4,1,1,1,1,1,
1,4),(97.3893722612838,98.125841455471,99.123883736595,100.121926017719,
101.119968298843,102.118010579967,103.116052861091,103.672557568463),
 .UNSPECIFIED.);
#484=B_SPLINE_CURVE_WITH_KNOTS('',3,(#15841,#15842,#15843,#15844,#15845,
#15846,#15847,#15848,#15849,#15850),.UNSPECIFIED.,.F.,.F.,(4,1,1,1,1,1,
1,4),(91.1061869541041,91.4273686162531,92.4250114771125,93.4226543379719,
94.4202971988313,95.4179400596907,96.4155829205502,97.3893722612837),
 .UNSPECIFIED.);
#485=B_SPLINE_CURVE_WITH_KNOTS('',3,(#15851,#15852,#15853,#15854,#15855,
#15856,#15857,#15858,#15859,#15860,#15861),.UNSPECIFIED.,.F.,.F.,(4,1,1,
1,1,1,1,1,4),(91.1061869541042,91.1395454876028,92.1375877687268,93.1356300498508,
94.1336723309749,95.1317146120989,96.1297568932229,97.127799174347,97.3893722612838),
 .UNSPECIFIED.);
#486=B_SPLINE_CURVE_WITH_KNOTS('',3,(#15866,#15867,#15868,#15869,#15870,
#15871,#15872,#15873,#15874,#15875),.UNSPECIFIED.,.F.,.F.,(4,1,1,1,1,1,
1,4),(84.8230016469245,85.4415114510967,86.4391543119561,87.4367971728155,
88.4344400336749,89.4320828945343,90.4297257553937,91.1061869541041),
 .UNSPECIFIED.);
#487=B_SPLINE_CURVE_WITH_KNOTS('',3,(#15876,#15877,#15878,#15879,#15880,
#15881,#15882,#15883,#15884,#15885),.UNSPECIFIED.,.F.,.F.,(4,1,1,1,1,1,
1,4),(84.8230016469246,85.1512918008586,86.1493340819827,87.1473763631067,
88.1454186442307,89.1434609253548,90.1415032064788,91.1061869541042),
 .UNSPECIFIED.);
#488=B_SPLINE_CURVE_WITH_KNOTS('',3,(#15890,#15891,#15892,#15893,#15894,
#15895,#15896,#15897,#15898,#15899),.UNSPECIFIED.,.F.,.F.,(4,1,1,1,1,1,
1,4),(78.539816339745,79.4556542859402,80.4532971467996,81.4509400076591,
82.4485828685185,83.4462257293779,84.4438685902373,84.8230016469245),
 .UNSPECIFIED.);
#489=B_SPLINE_CURVE_WITH_KNOTS('',3,(#15900,#15901,#15902,#15903,#15904,
#15905,#15906,#15907,#15908,#15909),.UNSPECIFIED.,.F.,.F.,(4,1,1,1,1,1,
1,4),(78.539816339745,79.1630381141145,80.1610803952385,81.1591226763625,
82.1571649574865,83.1552072386106,84.1532495197346,84.8230016469246),
 .UNSPECIFIED.);
#490=B_SPLINE_CURVE_WITH_KNOTS('',3,(#15914,#15915,#15916,#15917,#15918,
#15919,#15920,#15921,#15922,#15923,#15924),.UNSPECIFIED.,.F.,.F.,(4,1,1,
1,1,1,1,1,4),(72.2566310325654,72.4721542599244,73.4697971207838,74.4674399816432,
75.4650828425026,76.462725703362,77.4603685642214,78.4580114250808,78.539816339745),
 .UNSPECIFIED.);
#491=B_SPLINE_CURVE_WITH_KNOTS('',3,(#15925,#15926,#15927,#15928,#15929,
#15930,#15931,#15932,#15933,#15934),.UNSPECIFIED.,.F.,.F.,(4,1,1,1,1,1,
1,4),(72.2566310325654,73.1747844273703,74.1728267084943,75.1708689896184,
76.1689112707424,77.1669535518664,78.1649958329905,78.539816339745),
 .UNSPECIFIED.);
#492=B_SPLINE_CURVE_WITH_KNOTS('',3,(#15939,#15940,#15941,#15942,#15943,
#15944,#15945,#15946,#15947,#15948),.UNSPECIFIED.,.F.,.F.,(4,1,1,1,1,1,
1,4),(65.9734457253858,66.486297094768,67.4839399556274,68.4815828164868,
69.4792256773462,70.4768685382056,71.474511399065,72.2566310325654),
 .UNSPECIFIED.);
#493=B_SPLINE_CURVE_WITH_KNOTS('',3,(#15949,#15950,#15951,#15952,#15953,
#15954,#15955,#15956,#15957,#15958,#15959),.UNSPECIFIED.,.F.,.F.,(4,1,1,
1,1,1,1,1,4),(65.9734457253858,66.1884884595021,67.1865307406262,68.1845730217502,
69.1826153028742,70.1806575839982,71.1786998651223,72.1767421462463,72.2566310325654),
 .UNSPECIFIED.);
#494=B_SPLINE_CURVE_WITH_KNOTS('',3,(#15964,#15965,#15966,#15967,#15968,
#15969,#15970,#15971,#15972,#15973),.UNSPECIFIED.,.F.,.F.,(4,1,1,1,1,1,
1,4),(59.6902604182062,60.5004399296115,61.4980827904709,62.4957256513303,
63.4933685121897,64.4910113730492,65.4886542339086,65.9734457253858),
 .UNSPECIFIED.);
#495=B_SPLINE_CURVE_WITH_KNOTS('',3,(#15974,#15975,#15976,#15977,#15978,
#15979,#15980,#15981,#15982,#15983),.UNSPECIFIED.,.F.,.F.,(4,1,1,1,1,1,
1,4),(59.6902604182062,60.200234772758,61.198277053882,62.196319335006,
63.19436161613,64.1924038972541,65.1904461783781,65.9734457253858),
 .UNSPECIFIED.);
#496=B_SPLINE_CURVE_WITH_KNOTS('',3,(#15988,#15989,#15990,#15991,#15992,
#15993,#15994,#15995,#15996,#15997,#15998),.UNSPECIFIED.,.F.,.F.,(4,1,1,
1,1,1,1,1,4),(53.4070751110266,53.5169399035957,54.5145827644551,55.5122256253145,
56.5098684861739,57.5075113470333,58.5051542078927,59.5027970687521,59.6902604182062),
 .UNSPECIFIED.);
#497=B_SPLINE_CURVE_WITH_KNOTS('',3,(#15999,#16000,#16001,#16002,#16003,
#16004,#16005,#16006,#16007,#16008),.UNSPECIFIED.,.F.,.F.,(4,1,1,1,1,1,
1,4),(53.4070751110266,54.2119810860138,55.2100233671378,56.2080656482619,
57.2061079293859,58.2041502105099,59.2021924916339,59.6902604182062),
 .UNSPECIFIED.);
#498=B_SPLINE_CURVE_WITH_KNOTS('',3,(#16013,#16014,#16015,#16016,#16017,
#16018,#16019,#16020,#16021,#16022),.UNSPECIFIED.,.F.,.F.,(4,1,1,1,1,1,
1,4),(47.123889803847,47.5310827384393,48.5287255992987,49.5263684601581,
50.5240113210175,51.5216541818769,52.5192970427363,53.4070751110266),
 .UNSPECIFIED.);
#499=B_SPLINE_CURVE_WITH_KNOTS('',3,(#16023,#16024,#16025,#16026,#16027,
#16028,#16029,#16030,#16031,#16032,#16033),.UNSPECIFIED.,.F.,.F.,(4,1,1,
1,1,1,1,1,4),(47.123889803847,47.2256851181456,48.2237273992696,49.2217696803937,
50.2198119615177,51.2178542426417,52.2158965237657,53.2139388048898,53.4070751110266),
 .UNSPECIFIED.);
#500=B_SPLINE_CURVE_WITH_KNOTS('',3,(#16038,#16039,#16040,#16041,#16042,
#16043,#16044,#16045,#16046,#16047),.UNSPECIFIED.,.F.,.F.,(4,1,1,1,1,1,
1,4),(40.8407044966674,41.5452255732828,42.5428684341422,43.5405112950016,
44.538154155861,45.5357970167204,46.5334398775799,47.123889803847),
 .UNSPECIFIED.);
#501=B_SPLINE_CURVE_WITH_KNOTS('',3,(#16048,#16049,#16050,#16051,#16052,
#16053,#16054,#16055,#16056,#16057),.UNSPECIFIED.,.F.,.F.,(4,1,1,1,1,1,
1,4),(40.8407044966675,41.2374314314014,42.2354737125255,43.2335159936495,
44.2315582747735,45.2296005558975,46.2276428370216,47.123889803847),
 .UNSPECIFIED.);
#502=B_SPLINE_CURVE_WITH_KNOTS('',3,(#16062,#16063,#16064,#16065,#16066,
#16067,#16068,#16069,#16070,#16071,#16072),.UNSPECIFIED.,.F.,.F.,(4,1,1,
1,1,1,1,1,4),(34.5575191894878,34.561725547267,35.5593684081264,36.5570112689858,
37.5546541298452,38.5522969907046,39.549939851564,40.5475827124234,40.8407044966674),
 .UNSPECIFIED.);
#503=B_SPLINE_CURVE_WITH_KNOTS('',3,(#16073,#16074,#16075,#16076,#16077,
#16078,#16079,#16080,#16081,#16082),.UNSPECIFIED.,.F.,.F.,(4,1,1,1,1,1,
1,4),(34.5575191894879,35.2491777446573,36.2472200257813,37.2452623069053,
38.2433045880294,39.2413468691534,40.2393891502774,40.8407044966675),
 .UNSPECIFIED.);
#504=B_SPLINE_CURVE_WITH_KNOTS('',3,(#16087,#16088,#16089,#16090,#16091,
#16092,#16093,#16094,#16095,#16096),.UNSPECIFIED.,.F.,.F.,(4,1,1,1,1,1,
1,4),(28.2743338823082,28.5758683821105,29.5735112429699,30.5711541038294,
31.5687969646888,32.5664398255482,33.5640826864076,34.5575191894878),
 .UNSPECIFIED.);
#505=B_SPLINE_CURVE_WITH_KNOTS('',3,(#16097,#16098,#16099,#16100,#16101,
#16102,#16103,#16104,#16105,#16106),.UNSPECIFIED.,.F.,.F.,(4,1,1,1,1,1,
1,4),(28.2743338823083,29.2609240579131,30.2589663390371,31.2570086201612,
32.2550509012852,33.2530931824092,34.2511354635333,34.5575191894879),
 .UNSPECIFIED.);
#506=B_SPLINE_CURVE_WITH_KNOTS('',3,(#16111,#16112,#16113,#16114,#16115,
#16116,#16117,#16118,#16119,#16120),.UNSPECIFIED.,.F.,.F.,(4,1,1,1,1,1,
1,4),(21.9911485751286,22.5900112169541,23.5876540778135,24.5852969386729,
25.5829397995323,26.5805826603917,27.5782255212511,28.2743338823082),
 .UNSPECIFIED.);
#507=B_SPLINE_CURVE_WITH_KNOTS('',3,(#16121,#16122,#16123,#16124,#16125,
#16126,#16127,#16128,#16129,#16130,#16131),.UNSPECIFIED.,.F.,.F.,(4,1,1,
1,1,1,1,1,4),(21.9911485751287,22.2746280900449,23.272670371169,24.270712652293,
25.268754933417,26.266797214541,27.2648394956651,28.2628817767891,28.2743338823083),
 .UNSPECIFIED.);
#508=B_SPLINE_CURVE_WITH_KNOTS('',3,(#16136,#16137,#16138,#16139,#16140,
#16141,#16142,#16143,#16144,#16145),.UNSPECIFIED.,.F.,.F.,(4,1,1,1,1,1,
1,4),(15.707963267949,16.6041540517977,17.6017969126571,18.5994397735165,
19.5970826343759,20.5947254952353,21.5923683560947,21.9911485751286),
 .UNSPECIFIED.);
#509=B_SPLINE_CURVE_WITH_KNOTS('',3,(#16146,#16147,#16148,#16149,#16150,
#16151,#16152,#16153,#16154,#16155),.UNSPECIFIED.,.F.,.F.,(4,1,1,1,1,1,
1,4),(15.7079632679491,16.2863744033008,17.2844166844248,18.2824589655488,
19.2805012466728,20.2785435277969,21.2765858089209,21.9911485751287),
 .UNSPECIFIED.);
#510=B_SPLINE_CURVE_WITH_KNOTS('',3,(#16158,#16159,#16160,#16161,#16162,
#16163,#16164,#16165,#16166,#16167,#16168,#16169,#16170,#16171,#16172,#16173,
#16174,#16175,#16176,#16177,#16178,#16179,#16180,#16181,#16182,#16183,#16184,
#16185,#16186,#16187,#16188,#16189,#16190,#16191,#16192,#16193,#16194,#16195,
#16196,#16197,#16198,#16199,#16200,#16201,#16202,#16203,#16204,#16205,#16206,
#16207,#16208,#16209,#16210,#16211,#16212,#16213,#16214,#16215,#16216,#16217,
#16218,#16219,#16220,#16221,#16222,#16223,#16224,#16225,#16226,#16227,#16228,
#16229,#16230,#16231,#16232,#16233,#16234,#16235,#16236,#16237,#16238,#16239,
#16240,#16241,#16242,#16243,#16244,#16245,#16246,#16247,#16248,#16249,#16250,
#16251,#16252,#16253,#16254,#16255,#16256,#16257,#16258,#16259,#16260,#16261,
#16262,#16263,#16264,#16265,#16266,#16267,#16268,#16269,#16270,#16271,#16272,
#16273,#16274,#16275,#16276,#16277,#16278),.UNSPECIFIED.,.F.,.F.,(4,3,3,
3,3,3,3,3,3,3,3,3,3,3,3,3,3,3,3,3,3,3,3,3,3,3,3,3,3,3,3,3,3,3,3,3,3,3,3,
3,4),(-0.753008129282056,-0.726412283548368,-0.715911613874471,-0.694893371653716,
-0.683361029549332,-0.673826434412814,-0.652889016486892,-0.639679181765185,
-0.63195159856097,-0.60480408471638,-0.59150990338668,-0.582561183693184,
-0.554067746128576,-0.540494882749548,-0.528208608719221,-0.505843484121927,
-0.4921308028701,-0.483102814228457,-0.456032674248847,-0.436199115577779,
-0.427073928162626,-0.400948091236321,-0.382860905241332,-0.374822254310016,
-0.34584221065474,-0.333939649620793,-0.324058619604945,-0.29393738163796,
-0.278576588250954,-0.269234263278142,-0.238815915606663,-0.225742435796944,
-0.216239773488962,-0.18666367230127,-0.170750005528772,-0.161294486761502,
-0.129614927749849,-0.114924930935507,-0.106250072717365,-0.0979353687381955,
-0.0965360155478562),.UNSPECIFIED.);
#511=B_SPLINE_CURVE_WITH_KNOTS('',3,(#16280,#16281,#16282,#16283,#16284,
#16285,#16286,#16287,#16288,#16289,#16290,#16291,#16292,#16293,#16294,#16295,
#16296,#16297,#16298,#16299,#16300,#16301,#16302,#16303,#16304,#16305,#16306,
#16307,#16308,#16309,#16310,#16311,#16312,#16313,#16314,#16315,#16316),
 .UNSPECIFIED.,.F.,.F.,(4,3,3,3,3,3,3,3,3,3,3,3,4),(-0.204609524178132,
-0.173922074105667,-0.152149392827302,-0.142793959810126,-0.12983323009626,
-0.11308637627832,-0.0998536142809363,-0.090547498816978,-0.0679106241127335,
-0.0514558350659385,-0.042025593252969,-0.0155529233063705,0.),
 .UNSPECIFIED.);
#512=B_SPLINE_CURVE_WITH_KNOTS('',3,(#16319,#16320,#16321,#16322,#16323,
#16324,#16325,#16326,#16327,#16328,#16329,#16330,#16331,#16332,#16333,#16334),
 .UNSPECIFIED.,.F.,.F.,(4,3,3,3,3,4),(-0.0965360155478562,-0.0724020116608921,
-0.0590232605257019,-0.050388474335024,-0.0186937936910934,0.),
 .UNSPECIFIED.);
#513=B_SPLINE_CURVE_WITH_KNOTS('',3,(#17123,#17124,#17125,#17126,#17127,
#17128,#17129,#17130),.UNSPECIFIED.,.F.,.F.,(4,1,1,1,1,4),(11.6159397475006,
12.61358260836,13.6112254692194,14.6088683300789,15.6065111909383,15.707963267949),
 .UNSPECIFIED.);
#514=B_SPLINE_CURVE_WITH_KNOTS('',3,(#17131,#17132,#17133,#17134,#17135,
#17136,#17137,#17138,#17139,#17140,#17141,#17142,#17143,#17144,#17145,#17146,
#17147,#17148,#17149,#17150,#17151,#17152,#17153,#17154,#17155,#17156,#17157,
#17158,#17159,#17160,#17161,#17162,#17163,#17164,#17165,#17166,#17167,#17168,
#17169,#17170,#17171,#17172,#17173,#17174,#17175,#17176,#17177,#17178,#17179),
 .UNSPECIFIED.,.F.,.F.,(4,3,3,3,3,3,3,3,3,3,3,3,3,3,3,3,4),(-0.275362278356892,
-0.263988733943187,-0.242277787653762,-0.228409792083558,-0.208856161945484,
-0.197709057767663,-0.168075464588018,-0.150222803571495,-0.140083955862437,
-0.125365894046572,-0.0997819296507484,-0.0889593225835958,-0.0667194919376969,
-0.0511923416312717,-0.0404361839568205,-0.0141940669149386,0.),
 .UNSPECIFIED.);
#515=B_SPLINE_CURVE_WITH_KNOTS('',3,(#17180,#17181,#17182,#17183,#17184,
#17185,#17186,#17187,#17188,#17189,#17190,#17191,#17192,#17193,#17194,#17195,
#17196,#17197,#17198),.UNSPECIFIED.,.F.,.F.,(4,3,3,3,3,3,4),(-191.027404416132,
-190.549786424147,-189.552143563287,-188.554500702428,-187.556857841568,
-186.559214980709,-186.304397428656),.UNSPECIFIED.);
#516=B_SPLINE_CURVE_WITH_KNOTS('',3,(#17201,#17202,#17203,#17204,#17205,
#17206,#17207,#17208,#17209),.UNSPECIFIED.,.F.,.F.,(4,1,1,1,1,1,4),(10.3752088276283,
11.2961629976806,12.2942052788047,13.2922475599287,14.2902898410527,15.2883321221767,
15.7079632679491),.UNSPECIFIED.);
#517=B_SPLINE_CURVE_WITH_KNOTS('',3,(#18003,#18004,#18005,#18006,#18007,
#18008,#18009,#18010,#18011,#18012,#18013,#18014,#18015,#18016,#18017,#18018,
#18019,#18020,#18021,#18022,#18023,#18024),.UNSPECIFIED.,.F.,.F.,(4,3,3,
3,3,3,3,4),(183.335115714669,183.639779726821,184.637822007945,185.635864289069,
186.633906570193,187.631948851317,188.629991132441,188.954231742812),
 .UNSPECIFIED.);
#518=B_SPLINE_CURVE_WITH_KNOTS('',3,(#18025,#18026,#18027,#18028,#18029,
#18030,#18031,#18032,#18033,#18034,#18035,#18036,#18037,#18038,#18039,#18040,
#18041,#18042,#18043,#18044,#18045,#18046,#18047,#18048,#18049,#18050,#18051,
#18052,#18053,#18054,#18055,#18056,#18057,#18058,#18059,#18060,#18061,#18062,
#18063,#18064,#18065,#18066,#18067,#18068,#18069,#18070,#18071,#18072,#18073,
#18074,#18075,#18076),.UNSPECIFIED.,.F.,.F.,(4,3,3,3,3,3,3,3,3,3,3,3,3,
3,3,3,3,4),(-0.276631791712714,-0.267404104599176,-0.245529112929484,-0.233826742508505,
-0.212230201958684,-0.201819484750363,-0.173281546649687,-0.162756755581661,
-0.152537502224722,-0.140478169692516,-0.120739781640826,-0.110641775261762,
-0.100726383882944,-0.0755447879122082,-0.0587891884452614,-0.0493012364577666,
-0.0182848522583483,0.),.UNSPECIFIED.);
#553=SHAPE_REPRESENTATION_RELATIONSHIP('SRR','None',#19144,#563);
#563=ADVANCED_BREP_SHAPE_REPRESENTATION('',(#583),#19087);
#573=STYLED_ITEM('',(#19202),#583);
#583=MANIFOLD_SOLID_BREP('Body1',#6827);
#647=FACE_BOUND('',#1621,.T.);
#648=FACE_BOUND('',#1624,.T.);
#793=PLANE('',#7373);
#794=PLANE('',#7374);
#795=PLANE('',#7375);
#796=PLANE('',#7376);
#797=PLANE('',#7377);
#798=PLANE('',#7378);
#799=PLANE('',#7379);
#800=PLANE('',#7380);
#801=PLANE('',#7384);
#802=PLANE('',#7385);
#1099=FACE_OUTER_BOUND('',#1548,.T.);
#1100=FACE_OUTER_BOUND('',#1549,.T.);
#1101=FACE_OUTER_BOUND('',#1550,.T.);
#1102=FACE_OUTER_BOUND('',#1551,.T.);
#1103=FACE_OUTER_BOUND('',#1552,.T.);
#1104=FACE_OUTER_BOUND('',#1553,.T.);
#1105=FACE_OUTER_BOUND('',#1554,.T.);
#1106=FACE_OUTER_BOUND('',#1555,.T.);
#1107=FACE_OUTER_BOUND('',#1556,.T.);
#1108=FACE_OUTER_BOUND('',#1557,.T.);
#1109=FACE_OUTER_BOUND('',#1558,.T.);
#1110=FACE_OUTER_BOUND('',#1559,.T.);
#1111=FACE_OUTER_BOUND('',#1560,.T.);
#1112=FACE_OUTER_BOUND('',#1561,.T.);
#1113=FACE_OUTER_BOUND('',#1562,.T.);
#1114=FACE_OUTER_BOUND('',#1563,.T.);
#1115=FACE_OUTER_BOUND('',#1564,.T.);
#1116=FACE_OUTER_BOUND('',#1565,.T.);
#1117=FACE_OUTER_BOUND('',#1566,.T.);
#1118=FACE_OUTER_BOUND('',#1567,.T.);
#1119=FACE_OUTER_BOUND('',#1568,.T.);
#1120=FACE_OUTER_BOUND('',#1569,.T.);
#1121=FACE_OUTER_BOUND('',#1570,.T.);
#1122=FACE_OUTER_BOUND('',#1571,.T.);
#1123=FACE_OUTER_BOUND('',#1572,.T.);
#1124=FACE_OUTER_BOUND('',#1573,.T.);
#1125=FACE_OUTER_BOUND('',#1574,.T.);
#1126=FACE_OUTER_BOUND('',#1575,.T.);
#1127=FACE_OUTER_BOUND('',#1576,.T.);
#1128=FACE_OUTER_BOUND('',#1577,.T.);
#1129=FACE_OUTER_BOUND('',#1578,.T.);
#1130=FACE_OUTER_BOUND('',#1579,.T.);
#1131=FACE_OUTER_BOUND('',#1580,.T.);
#1132=FACE_OUTER_BOUND('',#1581,.T.);
#1133=FACE_OUTER_BOUND('',#1582,.T.);
#1134=FACE_OUTER_BOUND('',#1583,.T.);
#1135=FACE_OUTER_BOUND('',#1584,.T.);
#1136=FACE_OUTER_BOUND('',#1585,.T.);
#1137=FACE_OUTER_BOUND('',#1586,.T.);
#1138=FACE_OUTER_BOUND('',#1587,.T.);
#1139=FACE_OUTER_BOUND('',#1588,.T.);
#1140=FACE_OUTER_BOUND('',#1589,.T.);
#1141=FACE_OUTER_BOUND('',#1590,.T.);
#1142=FACE_OUTER_BOUND('',#1591,.T.);
#1143=FACE_OUTER_BOUND('',#1592,.T.);
#1144=FACE_OUTER_BOUND('',#1593,.T.);
#1145=FACE_OUTER_BOUND('',#1594,.T.);
#1146=FACE_OUTER_BOUND('',#1595,.T.);
#1147=FACE_OUTER_BOUND('',#1596,.T.);
#1148=FACE_OUTER_BOUND('',#1597,.T.);
#1149=FACE_OUTER_BOUND('',#1598,.T.);
#1150=FACE_OUTER_BOUND('',#1599,.T.);
#1151=FACE_OUTER_BOUND('',#1600,.T.);
#1152=FACE_OUTER_BOUND('',#1601,.T.);
#1153=FACE_OUTER_BOUND('',#1602,.T.);
#1154=FACE_OUTER_BOUND('',#1603,.T.);
#1155=FACE_OUTER_BOUND('',#1604,.T.);
#1156=FACE_OUTER_BOUND('',#1605,.T.);
#1157=FACE_OUTER_BOUND('',#1606,.T.);
#1158=FACE_OUTER_BOUND('',#1607,.T.);
#1159=FACE_OUTER_BOUND('',#1608,.T.);
#1160=FACE_OUTER_BOUND('',#1609,.T.);
#1161=FACE_OUTER_BOUND('',#1610,.T.);
#1162=FACE_OUTER_BOUND('',#1611,.T.);
#1163=FACE_OUTER_BOUND('',#1612,.T.);
#1164=FACE_OUTER_BOUND('',#1613,.T.);
#1165=FACE_OUTER_BOUND('',#1614,.T.);
#1166=FACE_OUTER_BOUND('',#1615,.T.);
#1167=FACE_OUTER_BOUND('',#1616,.T.);
#1168=FACE_OUTER_BOUND('',#1617,.T.);
#1169=FACE_OUTER_BOUND('',#1618,.T.);
#1170=FACE_OUTER_BOUND('',#1619,.T.);
#1171=FACE_OUTER_BOUND('',#1620,.T.);
#1172=FACE_OUTER_BOUND('',#1622,.T.);
#1173=FACE_OUTER_BOUND('',#1623,.T.);
#1174=FACE_OUTER_BOUND('',#1625,.T.);
#1548=EDGE_LOOP('',(#5737,#5738,#5739,#5740));
#1549=EDGE_LOOP('',(#5741,#5742,#5743,#5744));
#1550=EDGE_LOOP('',(#5745,#5746,#5747,#5748));
#1551=EDGE_LOOP('',(#5749,#5750,#5751,#5752));
#1552=EDGE_LOOP('',(#5753,#5754,#5755,#5756));
#1553=EDGE_LOOP('',(#5757,#5758,#5759,#5760));
#1554=EDGE_LOOP('',(#5761,#5762,#5763,#5764));
#1555=EDGE_LOOP('',(#5765,#5766,#5767,#5768));
#1556=EDGE_LOOP('',(#5769,#5770,#5771,#5772));
#1557=EDGE_LOOP('',(#5773,#5774,#5775,#5776));
#1558=EDGE_LOOP('',(#5777,#5778,#5779,#5780));
#1559=EDGE_LOOP('',(#5781,#5782,#5783,#5784));
#1560=EDGE_LOOP('',(#5785,#5786,#5787,#5788));
#1561=EDGE_LOOP('',(#5789,#5790,#5791,#5792));
#1562=EDGE_LOOP('',(#5793,#5794,#5795,#5796));
#1563=EDGE_LOOP('',(#5797,#5798,#5799,#5800));
#1564=EDGE_LOOP('',(#5801,#5802,#5803,#5804));
#1565=EDGE_LOOP('',(#5805,#5806,#5807,#5808));
#1566=EDGE_LOOP('',(#5809,#5810,#5811,#5812));
#1567=EDGE_LOOP('',(#5813,#5814,#5815,#5816));
#1568=EDGE_LOOP('',(#5817,#5818,#5819,#5820));
#1569=EDGE_LOOP('',(#5821,#5822,#5823,#5824));
#1570=EDGE_LOOP('',(#5825,#5826,#5827,#5828));
#1571=EDGE_LOOP('',(#5829,#5830,#5831,#5832));
#1572=EDGE_LOOP('',(#5833,#5834,#5835,#5836));
#1573=EDGE_LOOP('',(#5837,#5838,#5839,#5840));
#1574=EDGE_LOOP('',(#5841,#5842,#5843,#5844));
#1575=EDGE_LOOP('',(#5845,#5846,#5847,#5848));
#1576=EDGE_LOOP('',(#5849,#5850,#5851,#5852));
#1577=EDGE_LOOP('',(#5853,#5854,#5855,#5856));
#1578=EDGE_LOOP('',(#5857,#5858,#5859,#5860));
#1579=EDGE_LOOP('',(#5861,#5862,#5863,#5864));
#1580=EDGE_LOOP('',(#5865,#5866,#5867,#5868));
#1581=EDGE_LOOP('',(#5869,#5870,#5871,#5872));
#1582=EDGE_LOOP('',(#5873,#5874,#5875,#5876));
#1583=EDGE_LOOP('',(#5877,#5878,#5879,#5880));
#1584=EDGE_LOOP('',(#5881,#5882,#5883,#5884));
#1585=EDGE_LOOP('',(#5885,#5886,#5887,#5888));
#1586=EDGE_LOOP('',(#5889,#5890,#5891,#5892));
#1587=EDGE_LOOP('',(#5893,#5894,#5895,#5896));
#1588=EDGE_LOOP('',(#5897,#5898,#5899,#5900));
#1589=EDGE_LOOP('',(#5901,#5902,#5903,#5904));
#1590=EDGE_LOOP('',(#5905,#5906,#5907,#5908));
#1591=EDGE_LOOP('',(#5909,#5910,#5911,#5912));
#1592=EDGE_LOOP('',(#5913,#5914,#5915,#5916));
#1593=EDGE_LOOP('',(#5917,#5918,#5919,#5920));
#1594=EDGE_LOOP('',(#5921,#5922,#5923,#5924));
#1595=EDGE_LOOP('',(#5925,#5926,#5927,#5928));
#1596=EDGE_LOOP('',(#5929,#5930,#5931,#5932));
#1597=EDGE_LOOP('',(#5933,#5934,#5935,#5936));
#1598=EDGE_LOOP('',(#5937,#5938,#5939,#5940));
#1599=EDGE_LOOP('',(#5941,#5942,#5943,#5944));
#1600=EDGE_LOOP('',(#5945,#5946,#5947,#5948));
#1601=EDGE_LOOP('',(#5949,#5950,#5951,#5952));
#1602=EDGE_LOOP('',(#5953,#5954,#5955,#5956));
#1603=EDGE_LOOP('',(#5957,#5958,#5959,#5960));
#1604=EDGE_LOOP('',(#5961,#5962,#5963,#5964));
#1605=EDGE_LOOP('',(#5965,#5966,#5967,#5968));
#1606=EDGE_LOOP('',(#5969,#5970,#5971,#5972));
#1607=EDGE_LOOP('',(#5973,#5974,#5975,#5976));
#1608=EDGE_LOOP('',(#5977,#5978,#5979,#5980,#5981,#5982,#5983,#5984));
#1609=EDGE_LOOP('',(#5985,#5986,#5987,#5988,#5989,#5990,#5991,#5992,#5993,
#5994,#5995,#5996,#5997,#5998,#5999,#6000,#6001,#6002,#6003,#6004,#6005,
#6006,#6007,#6008,#6009,#6010,#6011,#6012,#6013,#6014,#6015,#6016,#6017,
#6018,#6019,#6020,#6021,#6022,#6023,#6024,#6025,#6026,#6027,#6028,#6029,
#6030,#6031,#6032,#6033,#6034,#6035,#6036,#6037,#6038,#6039,#6040,#6041,
#6042,#6043,#6044,#6045,#6046,#6047,#6048));
#1610=EDGE_LOOP('',(#6049,#6050,#6051,#6052));
#1611=EDGE_LOOP('',(#6053,#6054,#6055,#6056,#6057,#6058,#6059,#6060,#6061,
#6062,#6063,#6064,#6065,#6066,#6067,#6068,#6069,#6070,#6071,#6072,#6073,
#6074,#6075,#6076,#6077,#6078,#6079,#6080,#6081,#6082,#6083,#6084,#6085,
#6086,#6087,#6088,#6089,#6090,#6091,#6092,#6093,#6094,#6095,#6096,#6097,
#6098,#6099,#6100,#6101,#6102,#6103,#6104,#6105,#6106,#6107,#6108,#6109,
#6110,#6111,#6112,#6113,#6114,#6115,#6116,#6117));
#1612=EDGE_LOOP('',(#6118,#6119,#6120,#6121));
#1613=EDGE_LOOP('',(#6122,#6123,#6124,#6125));
#1614=EDGE_LOOP('',(#6126,#6127,#6128,#6129));
#1615=EDGE_LOOP('',(#6130,#6131,#6132,#6133));
#1616=EDGE_LOOP('',(#6134,#6135,#6136,#6137));
#1617=EDGE_LOOP('',(#6138,#6139,#6140,#6141));
#1618=EDGE_LOOP('',(#6142,#6143,#6144,#6145));
#1619=EDGE_LOOP('',(#6146,#6147,#6148,#6149,#6150,#6151));
#1620=EDGE_LOOP('',(#6152));
#1621=EDGE_LOOP('',(#6153,#6154,#6155,#6156));
#1622=EDGE_LOOP('',(#6157,#6158,#6159,#6160));
#1623=EDGE_LOOP('',(#6161));
#1624=EDGE_LOOP('',(#6162,#6163,#6164,#6165,#6166,#6167));
#1625=EDGE_LOOP('',(#6168));
#1995=LINE('',#13960,#2444);
#1996=LINE('',#13984,#2445);
#1997=LINE('',#14032,#2446);
#1998=LINE('',#14080,#2447);
#1999=LINE('',#14131,#2448);
#2000=LINE('',#14179,#2449);
#2001=LINE('',#14227,#2450);
#2002=LINE('',#14275,#2451);
#2003=LINE('',#14329,#2452);
#2004=LINE('',#14377,#2453);
#2005=LINE('',#14425,#2454);
#2006=LINE('',#14479,#2455);
#2007=LINE('',#14527,#2456);
#2008=LINE('',#14575,#2457);
#2009=LINE('',#14623,#2458);
#2010=LINE('',#14677,#2459);
#2011=LINE('',#14725,#2460);
#2012=LINE('',#14773,#2461);
#2013=LINE('',#14827,#2462);
#2014=LINE('',#14875,#2463);
#2015=LINE('',#14923,#2464);
#2016=LINE('',#14977,#2465);
#2017=LINE('',#15025,#2466);
#2018=LINE('',#15073,#2467);
#2019=LINE('',#15121,#2468);
#2020=LINE('',#15175,#2469);
#2021=LINE('',#15223,#2470);
#2022=LINE('',#15271,#2471);
#2023=LINE('',#15325,#2472);
#2024=LINE('',#15373,#2473);
#2025=LINE('',#15421,#2474);
#2026=LINE('',#15447,#2475);
#2027=LINE('',#15471,#2476);
#2028=LINE('',#15495,#2477);
#2029=LINE('',#15520,#2478);
#2030=LINE('',#15545,#2479);
#2031=LINE('',#15569,#2480);
#2032=LINE('',#15594,#2481);
#2033=LINE('',#15619,#2482);
#2034=LINE('',#15643,#2483);
#2035=LINE('',#15667,#2484);
#2036=LINE('',#15692,#2485);
#2037=LINE('',#15717,#2486);
#2038=LINE('',#15741,#2487);
#2039=LINE('',#15766,#2488);
#2040=LINE('',#15791,#2489);
#2041=LINE('',#15815,#2490);
#2042=LINE('',#15840,#2491);
#2043=LINE('',#15865,#2492);
#2044=LINE('',#15889,#2493);
#2045=LINE('',#15913,#2494);
#2046=LINE('',#15938,#2495);
#2047=LINE('',#15963,#2496);
#2048=LINE('',#15987,#2497);
#2049=LINE('',#16012,#2498);
#2050=LINE('',#16037,#2499);
#2051=LINE('',#16061,#2500);
#2052=LINE('',#16086,#2501);
#2053=LINE('',#16110,#2502);
#2054=LINE('',#16135,#2503);
#2055=LINE('',#16336,#2504);
#2056=LINE('',#18081,#2505);
#2057=LINE('',#18083,#2506);
#2058=LINE('',#18085,#2507);
#2059=LINE('',#18086,#2508);
#2060=LINE('',#18089,#2509);
#2061=LINE('',#18091,#2510);
#2062=LINE('',#18092,#2511);
#2063=LINE('',#18095,#2512);
#2064=LINE('',#18097,#2513);
#2065=LINE('',#18098,#2514);
#2066=LINE('',#18101,#2515);
#2067=LINE('',#18103,#2516);
#2068=LINE('',#18104,#2517);
#2069=LINE('',#18107,#2518);
#2070=LINE('',#18109,#2519);
#2071=LINE('',#18110,#2520);
#2072=LINE('',#18112,#2521);
#2073=LINE('',#18113,#2522);
#2074=LINE('',#18120,#2523);
#2444=VECTOR('',#8506,0.15);
#2445=VECTOR('',#8511,0.15);
#2446=VECTOR('',#8514,0.15);
#2447=VECTOR('',#8517,0.15);
#2448=VECTOR('',#8520,0.15);
#2449=VECTOR('',#8523,0.15);
#2450=VECTOR('',#8526,0.15);
#2451=VECTOR('',#8529,0.15);
#2452=VECTOR('',#8532,0.15);
#2453=VECTOR('',#8535,0.15);
#2454=VECTOR('',#8538,0.15);
#2455=VECTOR('',#8541,0.15);
#2456=VECTOR('',#8544,0.15);
#2457=VECTOR('',#8547,0.15);
#2458=VECTOR('',#8550,0.15);
#2459=VECTOR('',#8553,0.15);
#2460=VECTOR('',#8556,0.15);
#2461=VECTOR('',#8559,0.15);
#2462=VECTOR('',#8562,0.15);
#2463=VECTOR('',#8565,0.15);
#2464=VECTOR('',#8568,0.15);
#2465=VECTOR('',#8571,0.15);
#2466=VECTOR('',#8574,0.15);
#2467=VECTOR('',#8577,0.15);
#2468=VECTOR('',#8580,0.15);
#2469=VECTOR('',#8583,0.15);
#2470=VECTOR('',#8586,0.15);
#2471=VECTOR('',#8589,0.15);
#2472=VECTOR('',#8592,0.15);
#2473=VECTOR('',#8595,0.15);
#2474=VECTOR('',#8598,0.117775);
#2475=VECTOR('',#8603,0.117775);
#2476=VECTOR('',#8606,0.117775);
#2477=VECTOR('',#8609,0.117775);
#2478=VECTOR('',#8612,0.117775);
#2479=VECTOR('',#8615,0.117775);
#2480=VECTOR('',#8618,0.117775);
#2481=VECTOR('',#8621,0.117775);
#2482=VECTOR('',#8624,0.117775);
#2483=VECTOR('',#8627,0.117775);
#2484=VECTOR('',#8630,0.117775);
#2485=VECTOR('',#8633,0.117775);
#2486=VECTOR('',#8636,0.117775);
#2487=VECTOR('',#8639,0.117775);
#2488=VECTOR('',#8642,0.117775);
#2489=VECTOR('',#8645,0.117775);
#2490=VECTOR('',#8648,0.117775);
#2491=VECTOR('',#8651,0.117775);
#2492=VECTOR('',#8654,0.117775);
#2493=VECTOR('',#8657,0.117775);
#2494=VECTOR('',#8660,0.117775);
#2495=VECTOR('',#8663,0.117775);
#2496=VECTOR('',#8666,0.117775);
#2497=VECTOR('',#8669,0.117775);
#2498=VECTOR('',#8672,0.117775);
#2499=VECTOR('',#8675,0.117775);
#2500=VECTOR('',#8678,0.117775);
#2501=VECTOR('',#8681,0.117775);
#2502=VECTOR('',#8684,0.117775);
#2503=VECTOR('',#8687,0.117775);
#2504=VECTOR('',#8692,0.1);
#2505=VECTOR('',#8703,1.);
#2506=VECTOR('',#8704,1.);
#2507=VECTOR('',#8705,1.);
#2508=VECTOR('',#8706,1.);
#2509=VECTOR('',#8709,1.);
#2510=VECTOR('',#8710,1.);
#2511=VECTOR('',#8711,1.);
#2512=VECTOR('',#8714,1.);
#2513=VECTOR('',#8715,1.);
#2514=VECTOR('',#8716,1.);
#2515=VECTOR('',#8719,1.);
#2516=VECTOR('',#8720,1.);
#2517=VECTOR('',#8721,1.);
#2518=VECTOR('',#8724,1.);
#2519=VECTOR('',#8725,1.);
#2520=VECTOR('',#8726,1.);
#2521=VECTOR('',#8729,1.);
#2522=VECTOR('',#8730,1.);
#2523=VECTOR('',#8739,0.275);
#2698=CIRCLE('',#7306,0.14635);
#2699=CIRCLE('',#7337,0.117775);
#2700=CIRCLE('',#7368,0.14635);
#2701=CIRCLE('',#7369,0.05);
#2702=CIRCLE('',#7371,0.117775);
#2703=CIRCLE('',#7381,0.275);
#2704=CIRCLE('',#7383,0.275);
#3164=VERTEX_POINT('',#13958);
#3165=VERTEX_POINT('',#13959);
#3166=VERTEX_POINT('',#13961);
#3167=VERTEX_POINT('',#13972);
#3168=VERTEX_POINT('',#13982);
#3169=VERTEX_POINT('',#13983);
#3170=VERTEX_POINT('',#14030);
#3171=VERTEX_POINT('',#14031);
#3172=VERTEX_POINT('',#14078);
#3173=VERTEX_POINT('',#14079);
#3174=VERTEX_POINT('',#14129);
#3175=VERTEX_POINT('',#14130);
#3176=VERTEX_POINT('',#14177);
#3177=VERTEX_POINT('',#14178);
#3178=VERTEX_POINT('',#14225);
#3179=VERTEX_POINT('',#14226);
#3180=VERTEX_POINT('',#14273);
#3181=VERTEX_POINT('',#14274);
#3182=VERTEX_POINT('',#14327);
#3183=VERTEX_POINT('',#14328);
#3184=VERTEX_POINT('',#14375);
#3185=VERTEX_POINT('',#14376);
#3186=VERTEX_POINT('',#14423);
#3187=VERTEX_POINT('',#14424);
#3188=VERTEX_POINT('',#14477);
#3189=VERTEX_POINT('',#14478);
#3190=VERTEX_POINT('',#14525);
#3191=VERTEX_POINT('',#14526);
#3192=VERTEX_POINT('',#14573);
#3193=VERTEX_POINT('',#14574);
#3194=VERTEX_POINT('',#14621);
#3195=VERTEX_POINT('',#14622);
#3196=VERTEX_POINT('',#14675);
#3197=VERTEX_POINT('',#14676);
#3198=VERTEX_POINT('',#14723);
#3199=VERTEX_POINT('',#14724);
#3200=VERTEX_POINT('',#14771);
#3201=VERTEX_POINT('',#14772);
#3202=VERTEX_POINT('',#14825);
#3203=VERTEX_POINT('',#14826);
#3204=VERTEX_POINT('',#14873);
#3205=VERTEX_POINT('',#14874);
#3206=VERTEX_POINT('',#14921);
#3207=VERTEX_POINT('',#14922);
#3208=VERTEX_POINT('',#14975);
#3209=VERTEX_POINT('',#14976);
#3210=VERTEX_POINT('',#15023);
#3211=VERTEX_POINT('',#15024);
#3212=VERTEX_POINT('',#15071);
#3213=VERTEX_POINT('',#15072);
#3214=VERTEX_POINT('',#15119);
#3215=VERTEX_POINT('',#15120);
#3216=VERTEX_POINT('',#15173);
#3217=VERTEX_POINT('',#15174);
#3218=VERTEX_POINT('',#15221);
#3219=VERTEX_POINT('',#15222);
#3220=VERTEX_POINT('',#15269);
#3221=VERTEX_POINT('',#15270);
#3222=VERTEX_POINT('',#15323);
#3223=VERTEX_POINT('',#15324);
#3224=VERTEX_POINT('',#15371);
#3225=VERTEX_POINT('',#15372);
#3226=VERTEX_POINT('',#15419);
#3227=VERTEX_POINT('',#15420);
#3228=VERTEX_POINT('',#15422);
#3229=VERTEX_POINT('',#15433);
#3230=VERTEX_POINT('',#15445);
#3231=VERTEX_POINT('',#15446);
#3232=VERTEX_POINT('',#15469);
#3233=VERTEX_POINT('',#15470);
#3234=VERTEX_POINT('',#15493);
#3235=VERTEX_POINT('',#15494);
#3236=VERTEX_POINT('',#15518);
#3237=VERTEX_POINT('',#15519);
#3238=VERTEX_POINT('',#15543);
#3239=VERTEX_POINT('',#15544);
#3240=VERTEX_POINT('',#15567);
#3241=VERTEX_POINT('',#15568);
#3242=VERTEX_POINT('',#15592);
#3243=VERTEX_POINT('',#15593);
#3244=VERTEX_POINT('',#15617);
#3245=VERTEX_POINT('',#15618);
#3246=VERTEX_POINT('',#15641);
#3247=VERTEX_POINT('',#15642);
#3248=VERTEX_POINT('',#15665);
#3249=VERTEX_POINT('',#15666);
#3250=VERTEX_POINT('',#15690);
#3251=VERTEX_POINT('',#15691);
#3252=VERTEX_POINT('',#15715);
#3253=VERTEX_POINT('',#15716);
#3254=VERTEX_POINT('',#15739);
#3255=VERTEX_POINT('',#15740);
#3256=VERTEX_POINT('',#15764);
#3257=VERTEX_POINT('',#15765);
#3258=VERTEX_POINT('',#15789);
#3259=VERTEX_POINT('',#15790);
#3260=VERTEX_POINT('',#15813);
#3261=VERTEX_POINT('',#15814);
#3262=VERTEX_POINT('',#15838);
#3263=VERTEX_POINT('',#15839);
#3264=VERTEX_POINT('',#15863);
#3265=VERTEX_POINT('',#15864);
#3266=VERTEX_POINT('',#15887);
#3267=VERTEX_POINT('',#15888);
#3268=VERTEX_POINT('',#15911);
#3269=VERTEX_POINT('',#15912);
#3270=VERTEX_POINT('',#15936);
#3271=VERTEX_POINT('',#15937);
#3272=VERTEX_POINT('',#15961);
#3273=VERTEX_POINT('',#15962);
#3274=VERTEX_POINT('',#15985);
#3275=VERTEX_POINT('',#15986);
#3276=VERTEX_POINT('',#16010);
#3277=VERTEX_POINT('',#16011);
#3278=VERTEX_POINT('',#16035);
#3279=VERTEX_POINT('',#16036);
#3280=VERTEX_POINT('',#16059);
#3281=VERTEX_POINT('',#16060);
#3282=VERTEX_POINT('',#16084);
#3283=VERTEX_POINT('',#16085);
#3284=VERTEX_POINT('',#16108);
#3285=VERTEX_POINT('',#16109);
#3286=VERTEX_POINT('',#16133);
#3287=VERTEX_POINT('',#16134);
#3288=VERTEX_POINT('',#16157);
#3289=VERTEX_POINT('',#16279);
#3290=VERTEX_POINT('',#16317);
#3291=VERTEX_POINT('',#16335);
#3292=VERTEX_POINT('',#17122);
#3293=VERTEX_POINT('',#17200);
#3294=VERTEX_POINT('',#18079);
#3295=VERTEX_POINT('',#18080);
#3296=VERTEX_POINT('',#18082);
#3297=VERTEX_POINT('',#18084);
#3298=VERTEX_POINT('',#18088);
#3299=VERTEX_POINT('',#18090);
#3300=VERTEX_POINT('',#18094);
#3301=VERTEX_POINT('',#18096);
#3302=VERTEX_POINT('',#18100);
#3303=VERTEX_POINT('',#18102);
#3304=VERTEX_POINT('',#18106);
#3305=VERTEX_POINT('',#18108);
#3306=VERTEX_POINT('',#18116);
#3307=VERTEX_POINT('',#18119);
#4053=EDGE_CURVE('',#3164,#3165,#1995,.T.);
#4054=EDGE_CURVE('',#3164,#3166,#390,.T.);
#4055=EDGE_CURVE('',#3166,#3167,#2698,.F.);
#4056=EDGE_CURVE('',#3167,#3165,#391,.T.);
#4057=EDGE_CURVE('',#3168,#3169,#1996,.T.);
#4058=EDGE_CURVE('',#3168,#3164,#392,.T.);
#4059=EDGE_CURVE('',#3165,#3169,#393,.T.);
#4060=EDGE_CURVE('',#3170,#3171,#1997,.T.);
#4061=EDGE_CURVE('',#3170,#3168,#394,.T.);
#4062=EDGE_CURVE('',#3169,#3171,#395,.T.);
#4063=EDGE_CURVE('',#3172,#3173,#1998,.T.);
#4064=EDGE_CURVE('',#3172,#3170,#396,.T.);
#4065=EDGE_CURVE('',#3171,#3173,#397,.T.);
#4066=EDGE_CURVE('',#3174,#3175,#1999,.T.);
#4067=EDGE_CURVE('',#3174,#3172,#398,.T.);
#4068=EDGE_CURVE('',#3173,#3175,#399,.T.);
#4069=EDGE_CURVE('',#3176,#3177,#2000,.T.);
#4070=EDGE_CURVE('',#3176,#3174,#400,.T.);
#4071=EDGE_CURVE('',#3175,#3177,#401,.T.);
#4072=EDGE_CURVE('',#3178,#3179,#2001,.T.);
#4073=EDGE_CURVE('',#3178,#3176,#402,.T.);
#4074=EDGE_CURVE('',#3177,#3179,#403,.T.);
#4075=EDGE_CURVE('',#3180,#3181,#2002,.T.);
#4076=EDGE_CURVE('',#3180,#3178,#404,.T.);
#4077=EDGE_CURVE('',#3179,#3181,#405,.T.);
#4078=EDGE_CURVE('',#3182,#3183,#2003,.T.);
#4079=EDGE_CURVE('',#3182,#3180,#406,.T.);
#4080=EDGE_CURVE('',#3181,#3183,#407,.T.);
#4081=EDGE_CURVE('',#3184,#3185,#2004,.T.);
#4082=EDGE_CURVE('',#3184,#3182,#408,.T.);
#4083=EDGE_CURVE('',#3183,#3185,#409,.T.);
#4084=EDGE_CURVE('',#3186,#3187,#2005,.T.);
#4085=EDGE_CURVE('',#3186,#3184,#410,.T.);
#4086=EDGE_CURVE('',#3185,#3187,#411,.T.);
#4087=EDGE_CURVE('',#3188,#3189,#2006,.T.);
#4088=EDGE_CURVE('',#3188,#3186,#412,.T.);
#4089=EDGE_CURVE('',#3187,#3189,#413,.T.);
#4090=EDGE_CURVE('',#3190,#3191,#2007,.T.);
#4091=EDGE_CURVE('',#3190,#3188,#414,.T.);
#4092=EDGE_CURVE('',#3189,#3191,#415,.T.);
#4093=EDGE_CURVE('',#3192,#3193,#2008,.T.);
#4094=EDGE_CURVE('',#3192,#3190,#416,.T.);
#4095=EDGE_CURVE('',#3191,#3193,#417,.T.);
#4096=EDGE_CURVE('',#3194,#3195,#2009,.T.);
#4097=EDGE_CURVE('',#3194,#3192,#418,.T.);
#4098=EDGE_CURVE('',#3193,#3195,#419,.T.);
#4099=EDGE_CURVE('',#3196,#3197,#2010,.T.);
#4100=EDGE_CURVE('',#3196,#3194,#420,.T.);
#4101=EDGE_CURVE('',#3195,#3197,#421,.T.);
#4102=EDGE_CURVE('',#3198,#3199,#2011,.T.);
#4103=EDGE_CURVE('',#3198,#3196,#422,.T.);
#4104=EDGE_CURVE('',#3197,#3199,#423,.T.);
#4105=EDGE_CURVE('',#3200,#3201,#2012,.T.);
#4106=EDGE_CURVE('',#3200,#3198,#424,.T.);
#4107=EDGE_CURVE('',#3199,#3201,#425,.T.);
#4108=EDGE_CURVE('',#3202,#3203,#2013,.T.);
#4109=EDGE_CURVE('',#3202,#3200,#426,.T.);
#4110=EDGE_CURVE('',#3201,#3203,#427,.T.);
#4111=EDGE_CURVE('',#3204,#3205,#2014,.T.);
#4112=EDGE_CURVE('',#3204,#3202,#428,.T.);
#4113=EDGE_CURVE('',#3203,#3205,#429,.T.);
#4114=EDGE_CURVE('',#3206,#3207,#2015,.T.);
#4115=EDGE_CURVE('',#3206,#3204,#430,.T.);
#4116=EDGE_CURVE('',#3205,#3207,#431,.T.);
#4117=EDGE_CURVE('',#3208,#3209,#2016,.T.);
#4118=EDGE_CURVE('',#3208,#3206,#432,.T.);
#4119=EDGE_CURVE('',#3207,#3209,#433,.T.);
#4120=EDGE_CURVE('',#3210,#3211,#2017,.T.);
#4121=EDGE_CURVE('',#3210,#3208,#434,.T.);
#4122=EDGE_CURVE('',#3209,#3211,#435,.T.);
#4123=EDGE_CURVE('',#3212,#3213,#2018,.T.);
#4124=EDGE_CURVE('',#3212,#3210,#436,.T.);
#4125=EDGE_CURVE('',#3211,#3213,#437,.T.);
#4126=EDGE_CURVE('',#3214,#3215,#2019,.T.);
#4127=EDGE_CURVE('',#3214,#3212,#438,.T.);
#4128=EDGE_CURVE('',#3213,#3215,#439,.T.);
#4129=EDGE_CURVE('',#3216,#3217,#2020,.T.);
#4130=EDGE_CURVE('',#3216,#3214,#440,.T.);
#4131=EDGE_CURVE('',#3215,#3217,#441,.T.);
#4132=EDGE_CURVE('',#3218,#3219,#2021,.T.);
#4133=EDGE_CURVE('',#3218,#3216,#442,.T.);
#4134=EDGE_CURVE('',#3217,#3219,#443,.T.);
#4135=EDGE_CURVE('',#3220,#3221,#2022,.T.);
#4136=EDGE_CURVE('',#3220,#3218,#444,.T.);
#4137=EDGE_CURVE('',#3219,#3221,#445,.T.);
#4138=EDGE_CURVE('',#3222,#3223,#2023,.T.);
#4139=EDGE_CURVE('',#3222,#3220,#446,.T.);
#4140=EDGE_CURVE('',#3221,#3223,#447,.T.);
#4141=EDGE_CURVE('',#3224,#3225,#2024,.T.);
#4142=EDGE_CURVE('',#3224,#3222,#448,.T.);
#4143=EDGE_CURVE('',#3223,#3225,#449,.T.);
#4144=EDGE_CURVE('',#3226,#3227,#2025,.T.);
#4145=EDGE_CURVE('',#3226,#3228,#450,.T.);
#4146=EDGE_CURVE('',#3228,#3229,#2699,.T.);
#4147=EDGE_CURVE('',#3227,#3229,#451,.T.);
#4148=EDGE_CURVE('',#3230,#3231,#2026,.T.);
#4149=EDGE_CURVE('',#3230,#3226,#452,.T.);
#4150=EDGE_CURVE('',#3231,#3227,#453,.T.);
#4151=EDGE_CURVE('',#3232,#3233,#2027,.T.);
#4152=EDGE_CURVE('',#3232,#3230,#454,.T.);
#4153=EDGE_CURVE('',#3233,#3231,#455,.T.);
#4154=EDGE_CURVE('',#3234,#3235,#2028,.T.);
#4155=EDGE_CURVE('',#3234,#3232,#456,.T.);
#4156=EDGE_CURVE('',#3235,#3233,#457,.T.);
#4157=EDGE_CURVE('',#3236,#3237,#2029,.T.);
#4158=EDGE_CURVE('',#3236,#3234,#458,.T.);
#4159=EDGE_CURVE('',#3237,#3235,#459,.T.);
#4160=EDGE_CURVE('',#3238,#3239,#2030,.T.);
#4161=EDGE_CURVE('',#3238,#3236,#460,.T.);
#4162=EDGE_CURVE('',#3239,#3237,#461,.T.);
#4163=EDGE_CURVE('',#3240,#3241,#2031,.T.);
#4164=EDGE_CURVE('',#3240,#3238,#462,.T.);
#4165=EDGE_CURVE('',#3241,#3239,#463,.T.);
#4166=EDGE_CURVE('',#3242,#3243,#2032,.T.);
#4167=EDGE_CURVE('',#3242,#3240,#464,.T.);
#4168=EDGE_CURVE('',#3243,#3241,#465,.T.);
#4169=EDGE_CURVE('',#3244,#3245,#2033,.T.);
#4170=EDGE_CURVE('',#3244,#3242,#466,.T.);
#4171=EDGE_CURVE('',#3245,#3243,#467,.T.);
#4172=EDGE_CURVE('',#3246,#3247,#2034,.T.);
#4173=EDGE_CURVE('',#3246,#3244,#468,.T.);
#4174=EDGE_CURVE('',#3247,#3245,#469,.T.);
#4175=EDGE_CURVE('',#3248,#3249,#2035,.T.);
#4176=EDGE_CURVE('',#3248,#3246,#470,.T.);
#4177=EDGE_CURVE('',#3249,#3247,#471,.T.);
#4178=EDGE_CURVE('',#3250,#3251,#2036,.T.);
#4179=EDGE_CURVE('',#3250,#3248,#472,.T.);
#4180=EDGE_CURVE('',#3251,#3249,#473,.T.);
#4181=EDGE_CURVE('',#3252,#3253,#2037,.T.);
#4182=EDGE_CURVE('',#3252,#3250,#474,.T.);
#4183=EDGE_CURVE('',#3253,#3251,#475,.T.);
#4184=EDGE_CURVE('',#3254,#3255,#2038,.T.);
#4185=EDGE_CURVE('',#3254,#3252,#476,.T.);
#4186=EDGE_CURVE('',#3255,#3253,#477,.T.);
#4187=EDGE_CURVE('',#3256,#3257,#2039,.T.);
#4188=EDGE_CURVE('',#3256,#3254,#478,.T.);
#4189=EDGE_CURVE('',#3257,#3255,#479,.T.);
#4190=EDGE_CURVE('',#3258,#3259,#2040,.T.);
#4191=EDGE_CURVE('',#3258,#3256,#480,.T.);
#4192=EDGE_CURVE('',#3259,#3257,#481,.T.);
#4193=EDGE_CURVE('',#3260,#3261,#2041,.T.);
#4194=EDGE_CURVE('',#3260,#3258,#482,.T.);
#4195=EDGE_CURVE('',#3261,#3259,#483,.T.);
#4196=EDGE_CURVE('',#3262,#3263,#2042,.T.);
#4197=EDGE_CURVE('',#3262,#3260,#484,.T.);
#4198=EDGE_CURVE('',#3263,#3261,#485,.T.);
#4199=EDGE_CURVE('',#3264,#3265,#2043,.T.);
#4200=EDGE_CURVE('',#3264,#3262,#486,.T.);
#4201=EDGE_CURVE('',#3265,#3263,#487,.T.);
#4202=EDGE_CURVE('',#3266,#3267,#2044,.T.);
#4203=EDGE_CURVE('',#3266,#3264,#488,.T.);
#4204=EDGE_CURVE('',#3267,#3265,#489,.T.);
#4205=EDGE_CURVE('',#3268,#3269,#2045,.T.);
#4206=EDGE_CURVE('',#3268,#3266,#490,.T.);
#4207=EDGE_CURVE('',#3269,#3267,#491,.T.);
#4208=EDGE_CURVE('',#3270,#3271,#2046,.T.);
#4209=EDGE_CURVE('',#3270,#3268,#492,.T.);
#4210=EDGE_CURVE('',#3271,#3269,#493,.T.);
#4211=EDGE_CURVE('',#3272,#3273,#2047,.T.);
#4212=EDGE_CURVE('',#3272,#3270,#494,.T.);
#4213=EDGE_CURVE('',#3273,#3271,#495,.T.);
#4214=EDGE_CURVE('',#3274,#3275,#2048,.T.);
#4215=EDGE_CURVE('',#3274,#3272,#496,.T.);
#4216=EDGE_CURVE('',#3275,#3273,#497,.T.);
#4217=EDGE_CURVE('',#3276,#3277,#2049,.T.);
#4218=EDGE_CURVE('',#3276,#3274,#498,.T.);
#4219=EDGE_CURVE('',#3277,#3275,#499,.T.);
#4220=EDGE_CURVE('',#3278,#3279,#2050,.T.);
#4221=EDGE_CURVE('',#3278,#3276,#500,.T.);
#4222=EDGE_CURVE('',#3279,#3277,#501,.T.);
#4223=EDGE_CURVE('',#3280,#3281,#2051,.T.);
#4224=EDGE_CURVE('',#3280,#3278,#502,.T.);
#4225=EDGE_CURVE('',#3281,#3279,#503,.T.);
#4226=EDGE_CURVE('',#3282,#3283,#2052,.T.);
#4227=EDGE_CURVE('',#3282,#3280,#504,.T.);
#4228=EDGE_CURVE('',#3283,#3281,#505,.T.);
#4229=EDGE_CURVE('',#3284,#3285,#2053,.T.);
#4230=EDGE_CURVE('',#3284,#3282,#506,.T.);
#4231=EDGE_CURVE('',#3285,#3283,#507,.T.);
#4232=EDGE_CURVE('',#3286,#3287,#2054,.T.);
#4233=EDGE_CURVE('',#3286,#3284,#508,.T.);
#4234=EDGE_CURVE('',#3287,#3285,#509,.T.);
#4235=EDGE_CURVE('',#3229,#3288,#510,.T.);
#4236=EDGE_CURVE('',#3289,#3228,#511,.T.);
#4237=EDGE_CURVE('',#3290,#3289,#2700,.T.);
#4238=EDGE_CURVE('',#3288,#3290,#512,.T.);
#4239=EDGE_CURVE('',#3288,#3291,#2055,.T.);
#4240=EDGE_CURVE('',#3291,#3291,#2701,.T.);
#4241=EDGE_CURVE('',#3292,#3286,#513,.T.);
#4242=EDGE_CURVE('',#3166,#3292,#514,.T.);
#4243=EDGE_CURVE('',#3289,#3224,#515,.T.);
#4244=EDGE_CURVE('',#3293,#3287,#516,.T.);
#4245=EDGE_CURVE('',#3292,#3293,#2702,.T.);
#4246=EDGE_CURVE('',#3225,#3290,#517,.T.);
#4247=EDGE_CURVE('',#3293,#3167,#518,.T.);
#4248=EDGE_CURVE('',#3294,#3295,#2056,.T.);
#4249=EDGE_CURVE('',#3294,#3296,#2057,.T.);
#4250=EDGE_CURVE('',#3296,#3297,#2058,.T.);
#4251=EDGE_CURVE('',#3295,#3297,#2059,.T.);
#4252=EDGE_CURVE('',#3298,#3294,#2060,.T.);
#4253=EDGE_CURVE('',#3298,#3299,#2061,.T.);
#4254=EDGE_CURVE('',#3299,#3296,#2062,.T.);
#4255=EDGE_CURVE('',#3300,#3298,#2063,.T.);
#4256=EDGE_CURVE('',#3300,#3301,#2064,.T.);
#4257=EDGE_CURVE('',#3301,#3299,#2065,.T.);
#4258=EDGE_CURVE('',#3302,#3300,#2066,.T.);
#4259=EDGE_CURVE('',#3302,#3303,#2067,.T.);
#4260=EDGE_CURVE('',#3303,#3301,#2068,.T.);
#4261=EDGE_CURVE('',#3304,#3302,#2069,.T.);
#4262=EDGE_CURVE('',#3304,#3305,#2070,.T.);
#4263=EDGE_CURVE('',#3305,#3303,#2071,.T.);
#4264=EDGE_CURVE('',#3295,#3304,#2072,.T.);
#4265=EDGE_CURVE('',#3297,#3305,#2073,.T.);
#4266=EDGE_CURVE('',#3306,#3306,#2703,.T.);
#4267=EDGE_CURVE('',#3306,#3307,#2074,.T.);
#4268=EDGE_CURVE('',#3307,#3307,#2704,.T.);
#5737=ORIENTED_EDGE('',*,*,#4053,.F.);
#5738=ORIENTED_EDGE('',*,*,#4054,.T.);
#5739=ORIENTED_EDGE('',*,*,#4055,.T.);
#5740=ORIENTED_EDGE('',*,*,#4056,.T.);
#5741=ORIENTED_EDGE('',*,*,#4057,.F.);
#5742=ORIENTED_EDGE('',*,*,#4058,.T.);
#5743=ORIENTED_EDGE('',*,*,#4053,.T.);
#5744=ORIENTED_EDGE('',*,*,#4059,.T.);
#5745=ORIENTED_EDGE('',*,*,#4060,.F.);
#5746=ORIENTED_EDGE('',*,*,#4061,.T.);
#5747=ORIENTED_EDGE('',*,*,#4057,.T.);
#5748=ORIENTED_EDGE('',*,*,#4062,.T.);
#5749=ORIENTED_EDGE('',*,*,#4063,.F.);
#5750=ORIENTED_EDGE('',*,*,#4064,.T.);
#5751=ORIENTED_EDGE('',*,*,#4060,.T.);
#5752=ORIENTED_EDGE('',*,*,#4065,.T.);
#5753=ORIENTED_EDGE('',*,*,#4066,.F.);
#5754=ORIENTED_EDGE('',*,*,#4067,.T.);
#5755=ORIENTED_EDGE('',*,*,#4063,.T.);
#5756=ORIENTED_EDGE('',*,*,#4068,.T.);
#5757=ORIENTED_EDGE('',*,*,#4069,.F.);
#5758=ORIENTED_EDGE('',*,*,#4070,.T.);
#5759=ORIENTED_EDGE('',*,*,#4066,.T.);
#5760=ORIENTED_EDGE('',*,*,#4071,.T.);
#5761=ORIENTED_EDGE('',*,*,#4072,.F.);
#5762=ORIENTED_EDGE('',*,*,#4073,.T.);
#5763=ORIENTED_EDGE('',*,*,#4069,.T.);
#5764=ORIENTED_EDGE('',*,*,#4074,.T.);
#5765=ORIENTED_EDGE('',*,*,#4075,.F.);
#5766=ORIENTED_EDGE('',*,*,#4076,.T.);
#5767=ORIENTED_EDGE('',*,*,#4072,.T.);
#5768=ORIENTED_EDGE('',*,*,#4077,.T.);
#5769=ORIENTED_EDGE('',*,*,#4078,.F.);
#5770=ORIENTED_EDGE('',*,*,#4079,.T.);
#5771=ORIENTED_EDGE('',*,*,#4075,.T.);
#5772=ORIENTED_EDGE('',*,*,#4080,.T.);
#5773=ORIENTED_EDGE('',*,*,#4081,.F.);
#5774=ORIENTED_EDGE('',*,*,#4082,.T.);
#5775=ORIENTED_EDGE('',*,*,#4078,.T.);
#5776=ORIENTED_EDGE('',*,*,#4083,.T.);
#5777=ORIENTED_EDGE('',*,*,#4084,.F.);
#5778=ORIENTED_EDGE('',*,*,#4085,.T.);
#5779=ORIENTED_EDGE('',*,*,#4081,.T.);
#5780=ORIENTED_EDGE('',*,*,#4086,.T.);
#5781=ORIENTED_EDGE('',*,*,#4087,.F.);
#5782=ORIENTED_EDGE('',*,*,#4088,.T.);
#5783=ORIENTED_EDGE('',*,*,#4084,.T.);
#5784=ORIENTED_EDGE('',*,*,#4089,.T.);
#5785=ORIENTED_EDGE('',*,*,#4090,.F.);
#5786=ORIENTED_EDGE('',*,*,#4091,.T.);
#5787=ORIENTED_EDGE('',*,*,#4087,.T.);
#5788=ORIENTED_EDGE('',*,*,#4092,.T.);
#5789=ORIENTED_EDGE('',*,*,#4093,.F.);
#5790=ORIENTED_EDGE('',*,*,#4094,.T.);
#5791=ORIENTED_EDGE('',*,*,#4090,.T.);
#5792=ORIENTED_EDGE('',*,*,#4095,.T.);
#5793=ORIENTED_EDGE('',*,*,#4096,.F.);
#5794=ORIENTED_EDGE('',*,*,#4097,.T.);
#5795=ORIENTED_EDGE('',*,*,#4093,.T.);
#5796=ORIENTED_EDGE('',*,*,#4098,.T.);
#5797=ORIENTED_EDGE('',*,*,#4099,.F.);
#5798=ORIENTED_EDGE('',*,*,#4100,.T.);
#5799=ORIENTED_EDGE('',*,*,#4096,.T.);
#5800=ORIENTED_EDGE('',*,*,#4101,.T.);
#5801=ORIENTED_EDGE('',*,*,#4102,.F.);
#5802=ORIENTED_EDGE('',*,*,#4103,.T.);
#5803=ORIENTED_EDGE('',*,*,#4099,.T.);
#5804=ORIENTED_EDGE('',*,*,#4104,.T.);
#5805=ORIENTED_EDGE('',*,*,#4105,.F.);
#5806=ORIENTED_EDGE('',*,*,#4106,.T.);
#5807=ORIENTED_EDGE('',*,*,#4102,.T.);
#5808=ORIENTED_EDGE('',*,*,#4107,.T.);
#5809=ORIENTED_EDGE('',*,*,#4108,.F.);
#5810=ORIENTED_EDGE('',*,*,#4109,.T.);
#5811=ORIENTED_EDGE('',*,*,#4105,.T.);
#5812=ORIENTED_EDGE('',*,*,#4110,.T.);
#5813=ORIENTED_EDGE('',*,*,#4111,.F.);
#5814=ORIENTED_EDGE('',*,*,#4112,.T.);
#5815=ORIENTED_EDGE('',*,*,#4108,.T.);
#5816=ORIENTED_EDGE('',*,*,#4113,.T.);
#5817=ORIENTED_EDGE('',*,*,#4114,.F.);
#5818=ORIENTED_EDGE('',*,*,#4115,.T.);
#5819=ORIENTED_EDGE('',*,*,#4111,.T.);
#5820=ORIENTED_EDGE('',*,*,#4116,.T.);
#5821=ORIENTED_EDGE('',*,*,#4117,.F.);
#5822=ORIENTED_EDGE('',*,*,#4118,.T.);
#5823=ORIENTED_EDGE('',*,*,#4114,.T.);
#5824=ORIENTED_EDGE('',*,*,#4119,.T.);
#5825=ORIENTED_EDGE('',*,*,#4120,.F.);
#5826=ORIENTED_EDGE('',*,*,#4121,.T.);
#5827=ORIENTED_EDGE('',*,*,#4117,.T.);
#5828=ORIENTED_EDGE('',*,*,#4122,.T.);
#5829=ORIENTED_EDGE('',*,*,#4123,.F.);
#5830=ORIENTED_EDGE('',*,*,#4124,.T.);
#5831=ORIENTED_EDGE('',*,*,#4120,.T.);
#5832=ORIENTED_EDGE('',*,*,#4125,.T.);
#5833=ORIENTED_EDGE('',*,*,#4126,.F.);
#5834=ORIENTED_EDGE('',*,*,#4127,.T.);
#5835=ORIENTED_EDGE('',*,*,#4123,.T.);
#5836=ORIENTED_EDGE('',*,*,#4128,.T.);
#5837=ORIENTED_EDGE('',*,*,#4129,.F.);
#5838=ORIENTED_EDGE('',*,*,#4130,.T.);
#5839=ORIENTED_EDGE('',*,*,#4126,.T.);
#5840=ORIENTED_EDGE('',*,*,#4131,.T.);
#5841=ORIENTED_EDGE('',*,*,#4132,.F.);
#5842=ORIENTED_EDGE('',*,*,#4133,.T.);
#5843=ORIENTED_EDGE('',*,*,#4129,.T.);
#5844=ORIENTED_EDGE('',*,*,#4134,.T.);
#5845=ORIENTED_EDGE('',*,*,#4135,.F.);
#5846=ORIENTED_EDGE('',*,*,#4136,.T.);
#5847=ORIENTED_EDGE('',*,*,#4132,.T.);
#5848=ORIENTED_EDGE('',*,*,#4137,.T.);
#5849=ORIENTED_EDGE('',*,*,#4138,.F.);
#5850=ORIENTED_EDGE('',*,*,#4139,.T.);
#5851=ORIENTED_EDGE('',*,*,#4135,.T.);
#5852=ORIENTED_EDGE('',*,*,#4140,.T.);
#5853=ORIENTED_EDGE('',*,*,#4141,.F.);
#5854=ORIENTED_EDGE('',*,*,#4142,.T.);
#5855=ORIENTED_EDGE('',*,*,#4138,.T.);
#5856=ORIENTED_EDGE('',*,*,#4143,.T.);
#5857=ORIENTED_EDGE('',*,*,#4144,.F.);
#5858=ORIENTED_EDGE('',*,*,#4145,.T.);
#5859=ORIENTED_EDGE('',*,*,#4146,.T.);
#5860=ORIENTED_EDGE('',*,*,#4147,.F.);
#5861=ORIENTED_EDGE('',*,*,#4148,.F.);
#5862=ORIENTED_EDGE('',*,*,#4149,.T.);
#5863=ORIENTED_EDGE('',*,*,#4144,.T.);
#5864=ORIENTED_EDGE('',*,*,#4150,.F.);
#5865=ORIENTED_EDGE('',*,*,#4151,.F.);
#5866=ORIENTED_EDGE('',*,*,#4152,.T.);
#5867=ORIENTED_EDGE('',*,*,#4148,.T.);
#5868=ORIENTED_EDGE('',*,*,#4153,.F.);
#5869=ORIENTED_EDGE('',*,*,#4154,.F.);
#5870=ORIENTED_EDGE('',*,*,#4155,.T.);
#5871=ORIENTED_EDGE('',*,*,#4151,.T.);
#5872=ORIENTED_EDGE('',*,*,#4156,.F.);
#5873=ORIENTED_EDGE('',*,*,#4157,.F.);
#5874=ORIENTED_EDGE('',*,*,#4158,.T.);
#5875=ORIENTED_EDGE('',*,*,#4154,.T.);
#5876=ORIENTED_EDGE('',*,*,#4159,.F.);
#5877=ORIENTED_EDGE('',*,*,#4160,.F.);
#5878=ORIENTED_EDGE('',*,*,#4161,.T.);
#5879=ORIENTED_EDGE('',*,*,#4157,.T.);
#5880=ORIENTED_EDGE('',*,*,#4162,.F.);
#5881=ORIENTED_EDGE('',*,*,#4163,.F.);
#5882=ORIENTED_EDGE('',*,*,#4164,.T.);
#5883=ORIENTED_EDGE('',*,*,#4160,.T.);
#5884=ORIENTED_EDGE('',*,*,#4165,.F.);
#5885=ORIENTED_EDGE('',*,*,#4166,.F.);
#5886=ORIENTED_EDGE('',*,*,#4167,.T.);
#5887=ORIENTED_EDGE('',*,*,#4163,.T.);
#5888=ORIENTED_EDGE('',*,*,#4168,.F.);
#5889=ORIENTED_EDGE('',*,*,#4169,.F.);
#5890=ORIENTED_EDGE('',*,*,#4170,.T.);
#5891=ORIENTED_EDGE('',*,*,#4166,.T.);
#5892=ORIENTED_EDGE('',*,*,#4171,.F.);
#5893=ORIENTED_EDGE('',*,*,#4172,.F.);
#5894=ORIENTED_EDGE('',*,*,#4173,.T.);
#5895=ORIENTED_EDGE('',*,*,#4169,.T.);
#5896=ORIENTED_EDGE('',*,*,#4174,.F.);
#5897=ORIENTED_EDGE('',*,*,#4175,.F.);
#5898=ORIENTED_EDGE('',*,*,#4176,.T.);
#5899=ORIENTED_EDGE('',*,*,#4172,.T.);
#5900=ORIENTED_EDGE('',*,*,#4177,.F.);
#5901=ORIENTED_EDGE('',*,*,#4178,.F.);
#5902=ORIENTED_EDGE('',*,*,#4179,.T.);
#5903=ORIENTED_EDGE('',*,*,#4175,.T.);
#5904=ORIENTED_EDGE('',*,*,#4180,.F.);
#5905=ORIENTED_EDGE('',*,*,#4181,.F.);
#5906=ORIENTED_EDGE('',*,*,#4182,.T.);
#5907=ORIENTED_EDGE('',*,*,#4178,.T.);
#5908=ORIENTED_EDGE('',*,*,#4183,.F.);
#5909=ORIENTED_EDGE('',*,*,#4184,.F.);
#5910=ORIENTED_EDGE('',*,*,#4185,.T.);
#5911=ORIENTED_EDGE('',*,*,#4181,.T.);
#5912=ORIENTED_EDGE('',*,*,#4186,.F.);
#5913=ORIENTED_EDGE('',*,*,#4187,.F.);
#5914=ORIENTED_EDGE('',*,*,#4188,.T.);
#5915=ORIENTED_EDGE('',*,*,#4184,.T.);
#5916=ORIENTED_EDGE('',*,*,#4189,.F.);
#5917=ORIENTED_EDGE('',*,*,#4190,.F.);
#5918=ORIENTED_EDGE('',*,*,#4191,.T.);
#5919=ORIENTED_EDGE('',*,*,#4187,.T.);
#5920=ORIENTED_EDGE('',*,*,#4192,.F.);
#5921=ORIENTED_EDGE('',*,*,#4193,.F.);
#5922=ORIENTED_EDGE('',*,*,#4194,.T.);
#5923=ORIENTED_EDGE('',*,*,#4190,.T.);
#5924=ORIENTED_EDGE('',*,*,#4195,.F.);
#5925=ORIENTED_EDGE('',*,*,#4196,.F.);
#5926=ORIENTED_EDGE('',*,*,#4197,.T.);
#5927=ORIENTED_EDGE('',*,*,#4193,.T.);
#5928=ORIENTED_EDGE('',*,*,#4198,.F.);
#5929=ORIENTED_EDGE('',*,*,#4199,.F.);
#5930=ORIENTED_EDGE('',*,*,#4200,.T.);
#5931=ORIENTED_EDGE('',*,*,#4196,.T.);
#5932=ORIENTED_EDGE('',*,*,#4201,.F.);
#5933=ORIENTED_EDGE('',*,*,#4202,.F.);
#5934=ORIENTED_EDGE('',*,*,#4203,.T.);
#5935=ORIENTED_EDGE('',*,*,#4199,.T.);
#5936=ORIENTED_EDGE('',*,*,#4204,.F.);
#5937=ORIENTED_EDGE('',*,*,#4205,.F.);
#5938=ORIENTED_EDGE('',*,*,#4206,.T.);
#5939=ORIENTED_EDGE('',*,*,#4202,.T.);
#5940=ORIENTED_EDGE('',*,*,#4207,.F.);
#5941=ORIENTED_EDGE('',*,*,#4208,.F.);
#5942=ORIENTED_EDGE('',*,*,#4209,.T.);
#5943=ORIENTED_EDGE('',*,*,#4205,.T.);
#5944=ORIENTED_EDGE('',*,*,#4210,.F.);
#5945=ORIENTED_EDGE('',*,*,#4211,.F.);
#5946=ORIENTED_EDGE('',*,*,#4212,.T.);
#5947=ORIENTED_EDGE('',*,*,#4208,.T.);
#5948=ORIENTED_EDGE('',*,*,#4213,.F.);
#5949=ORIENTED_EDGE('',*,*,#4214,.F.);
#5950=ORIENTED_EDGE('',*,*,#4215,.T.);
#5951=ORIENTED_EDGE('',*,*,#4211,.T.);
#5952=ORIENTED_EDGE('',*,*,#4216,.F.);
#5953=ORIENTED_EDGE('',*,*,#4217,.F.);
#5954=ORIENTED_EDGE('',*,*,#4218,.T.);
#5955=ORIENTED_EDGE('',*,*,#4214,.T.);
#5956=ORIENTED_EDGE('',*,*,#4219,.F.);
#5957=ORIENTED_EDGE('',*,*,#4220,.F.);
#5958=ORIENTED_EDGE('',*,*,#4221,.T.);
#5959=ORIENTED_EDGE('',*,*,#4217,.T.);
#5960=ORIENTED_EDGE('',*,*,#4222,.F.);
#5961=ORIENTED_EDGE('',*,*,#4223,.F.);
#5962=ORIENTED_EDGE('',*,*,#4224,.T.);
#5963=ORIENTED_EDGE('',*,*,#4220,.T.);
#5964=ORIENTED_EDGE('',*,*,#4225,.F.);
#5965=ORIENTED_EDGE('',*,*,#4226,.F.);
#5966=ORIENTED_EDGE('',*,*,#4227,.T.);
#5967=ORIENTED_EDGE('',*,*,#4223,.T.);
#5968=ORIENTED_EDGE('',*,*,#4228,.F.);
#5969=ORIENTED_EDGE('',*,*,#4229,.F.);
#5970=ORIENTED_EDGE('',*,*,#4230,.T.);
#5971=ORIENTED_EDGE('',*,*,#4226,.T.);
#5972=ORIENTED_EDGE('',*,*,#4231,.F.);
#5973=ORIENTED_EDGE('',*,*,#4232,.F.);
#5974=ORIENTED_EDGE('',*,*,#4233,.T.);
#5975=ORIENTED_EDGE('',*,*,#4229,.T.);
#5976=ORIENTED_EDGE('',*,*,#4234,.F.);
#5977=ORIENTED_EDGE('',*,*,#4235,.F.);
#5978=ORIENTED_EDGE('',*,*,#4146,.F.);
#5979=ORIENTED_EDGE('',*,*,#4236,.F.);
#5980=ORIENTED_EDGE('',*,*,#4237,.F.);
#5981=ORIENTED_EDGE('',*,*,#4238,.F.);
#5982=ORIENTED_EDGE('',*,*,#4239,.T.);
#5983=ORIENTED_EDGE('',*,*,#4240,.F.);
#5984=ORIENTED_EDGE('',*,*,#4239,.F.);
#5985=ORIENTED_EDGE('',*,*,#4236,.T.);
#5986=ORIENTED_EDGE('',*,*,#4145,.F.);
#5987=ORIENTED_EDGE('',*,*,#4149,.F.);
#5988=ORIENTED_EDGE('',*,*,#4152,.F.);
#5989=ORIENTED_EDGE('',*,*,#4155,.F.);
#5990=ORIENTED_EDGE('',*,*,#4158,.F.);
#5991=ORIENTED_EDGE('',*,*,#4161,.F.);
#5992=ORIENTED_EDGE('',*,*,#4164,.F.);
#5993=ORIENTED_EDGE('',*,*,#4167,.F.);
#5994=ORIENTED_EDGE('',*,*,#4170,.F.);
#5995=ORIENTED_EDGE('',*,*,#4173,.F.);
#5996=ORIENTED_EDGE('',*,*,#4176,.F.);
#5997=ORIENTED_EDGE('',*,*,#4179,.F.);
#5998=ORIENTED_EDGE('',*,*,#4182,.F.);
#5999=ORIENTED_EDGE('',*,*,#4185,.F.);
#6000=ORIENTED_EDGE('',*,*,#4188,.F.);
#6001=ORIENTED_EDGE('',*,*,#4191,.F.);
#6002=ORIENTED_EDGE('',*,*,#4194,.F.);
#6003=ORIENTED_EDGE('',*,*,#4197,.F.);
#6004=ORIENTED_EDGE('',*,*,#4200,.F.);
#6005=ORIENTED_EDGE('',*,*,#4203,.F.);
#6006=ORIENTED_EDGE('',*,*,#4206,.F.);
#6007=ORIENTED_EDGE('',*,*,#4209,.F.);
#6008=ORIENTED_EDGE('',*,*,#4212,.F.);
#6009=ORIENTED_EDGE('',*,*,#4215,.F.);
#6010=ORIENTED_EDGE('',*,*,#4218,.F.);
#6011=ORIENTED_EDGE('',*,*,#4221,.F.);
#6012=ORIENTED_EDGE('',*,*,#4224,.F.);
#6013=ORIENTED_EDGE('',*,*,#4227,.F.);
#6014=ORIENTED_EDGE('',*,*,#4230,.F.);
#6015=ORIENTED_EDGE('',*,*,#4233,.F.);
#6016=ORIENTED_EDGE('',*,*,#4241,.F.);
#6017=ORIENTED_EDGE('',*,*,#4242,.F.);
#6018=ORIENTED_EDGE('',*,*,#4054,.F.);
#6019=ORIENTED_EDGE('',*,*,#4058,.F.);
#6020=ORIENTED_EDGE('',*,*,#4061,.F.);
#6021=ORIENTED_EDGE('',*,*,#4064,.F.);
#6022=ORIENTED_EDGE('',*,*,#4067,.F.);
#6023=ORIENTED_EDGE('',*,*,#4070,.F.);
#6024=ORIENTED_EDGE('',*,*,#4073,.F.);
#6025=ORIENTED_EDGE('',*,*,#4076,.F.);
#6026=ORIENTED_EDGE('',*,*,#4079,.F.);
#6027=ORIENTED_EDGE('',*,*,#4082,.F.);
#6028=ORIENTED_EDGE('',*,*,#4085,.F.);
#6029=ORIENTED_EDGE('',*,*,#4088,.F.);
#6030=ORIENTED_EDGE('',*,*,#4091,.F.);
#6031=ORIENTED_EDGE('',*,*,#4094,.F.);
#6032=ORIENTED_EDGE('',*,*,#4097,.F.);
#6033=ORIENTED_EDGE('',*,*,#4100,.F.);
#6034=ORIENTED_EDGE('',*,*,#4103,.F.);
#6035=ORIENTED_EDGE('',*,*,#4106,.F.);
#6036=ORIENTED_EDGE('',*,*,#4109,.F.);
#6037=ORIENTED_EDGE('',*,*,#4112,.F.);
#6038=ORIENTED_EDGE('',*,*,#4115,.F.);
#6039=ORIENTED_EDGE('',*,*,#4118,.F.);
#6040=ORIENTED_EDGE('',*,*,#4121,.F.);
#6041=ORIENTED_EDGE('',*,*,#4124,.F.);
#6042=ORIENTED_EDGE('',*,*,#4127,.F.);
#6043=ORIENTED_EDGE('',*,*,#4130,.F.);
#6044=ORIENTED_EDGE('',*,*,#4133,.F.);
#6045=ORIENTED_EDGE('',*,*,#4136,.F.);
#6046=ORIENTED_EDGE('',*,*,#4139,.F.);
#6047=ORIENTED_EDGE('',*,*,#4142,.F.);
#6048=ORIENTED_EDGE('',*,*,#4243,.F.);
#6049=ORIENTED_EDGE('',*,*,#4232,.T.);
#6050=ORIENTED_EDGE('',*,*,#4244,.F.);
#6051=ORIENTED_EDGE('',*,*,#4245,.F.);
#6052=ORIENTED_EDGE('',*,*,#4241,.T.);
#6053=ORIENTED_EDGE('',*,*,#4235,.T.);
#6054=ORIENTED_EDGE('',*,*,#4238,.T.);
#6055=ORIENTED_EDGE('',*,*,#4246,.F.);
#6056=ORIENTED_EDGE('',*,*,#4143,.F.);
#6057=ORIENTED_EDGE('',*,*,#4140,.F.);
#6058=ORIENTED_EDGE('',*,*,#4137,.F.);
#6059=ORIENTED_EDGE('',*,*,#4134,.F.);
#6060=ORIENTED_EDGE('',*,*,#4131,.F.);
#6061=ORIENTED_EDGE('',*,*,#4128,.F.);
#6062=ORIENTED_EDGE('',*,*,#4125,.F.);
#6063=ORIENTED_EDGE('',*,*,#4122,.F.);
#6064=ORIENTED_EDGE('',*,*,#4119,.F.);
#6065=ORIENTED_EDGE('',*,*,#4116,.F.);
#6066=ORIENTED_EDGE('',*,*,#4113,.F.);
#6067=ORIENTED_EDGE('',*,*,#4110,.F.);
#6068=ORIENTED_EDGE('',*,*,#4107,.F.);
#6069=ORIENTED_EDGE('',*,*,#4104,.F.);
#6070=ORIENTED_EDGE('',*,*,#4101,.F.);
#6071=ORIENTED_EDGE('',*,*,#4098,.F.);
#6072=ORIENTED_EDGE('',*,*,#4095,.F.);
#6073=ORIENTED_EDGE('',*,*,#4092,.F.);
#6074=ORIENTED_EDGE('',*,*,#4089,.F.);
#6075=ORIENTED_EDGE('',*,*,#4086,.F.);
#6076=ORIENTED_EDGE('',*,*,#4083,.F.);
#6077=ORIENTED_EDGE('',*,*,#4080,.F.);
#6078=ORIENTED_EDGE('',*,*,#4077,.F.);
#6079=ORIENTED_EDGE('',*,*,#4074,.F.);
#6080=ORIENTED_EDGE('',*,*,#4071,.F.);
#6081=ORIENTED_EDGE('',*,*,#4068,.F.);
#6082=ORIENTED_EDGE('',*,*,#4065,.F.);
#6083=ORIENTED_EDGE('',*,*,#4062,.F.);
#6084=ORIENTED_EDGE('',*,*,#4059,.F.);
#6085=ORIENTED_EDGE('',*,*,#4056,.F.);
#6086=ORIENTED_EDGE('',*,*,#4247,.F.);
#6087=ORIENTED_EDGE('',*,*,#4244,.T.);
#6088=ORIENTED_EDGE('',*,*,#4234,.T.);
#6089=ORIENTED_EDGE('',*,*,#4231,.T.);
#6090=ORIENTED_EDGE('',*,*,#4228,.T.);
#6091=ORIENTED_EDGE('',*,*,#4225,.T.);
#6092=ORIENTED_EDGE('',*,*,#4222,.T.);
#6093=ORIENTED_EDGE('',*,*,#4219,.T.);
#6094=ORIENTED_EDGE('',*,*,#4216,.T.);
#6095=ORIENTED_EDGE('',*,*,#4213,.T.);
#6096=ORIENTED_EDGE('',*,*,#4210,.T.);
#6097=ORIENTED_EDGE('',*,*,#4207,.T.);
#6098=ORIENTED_EDGE('',*,*,#4204,.T.);
#6099=ORIENTED_EDGE('',*,*,#4201,.T.);
#6100=ORIENTED_EDGE('',*,*,#4198,.T.);
#6101=ORIENTED_EDGE('',*,*,#4195,.T.);
#6102=ORIENTED_EDGE('',*,*,#4192,.T.);
#6103=ORIENTED_EDGE('',*,*,#4189,.T.);
#6104=ORIENTED_EDGE('',*,*,#4186,.T.);
#6105=ORIENTED_EDGE('',*,*,#4183,.T.);
#6106=ORIENTED_EDGE('',*,*,#4180,.T.);
#6107=ORIENTED_EDGE('',*,*,#4177,.T.);
#6108=ORIENTED_EDGE('',*,*,#4174,.T.);
#6109=ORIENTED_EDGE('',*,*,#4171,.T.);
#6110=ORIENTED_EDGE('',*,*,#4168,.T.);
#6111=ORIENTED_EDGE('',*,*,#4165,.T.);
#6112=ORIENTED_EDGE('',*,*,#4162,.T.);
#6113=ORIENTED_EDGE('',*,*,#4159,.T.);
#6114=ORIENTED_EDGE('',*,*,#4156,.T.);
#6115=ORIENTED_EDGE('',*,*,#4153,.T.);
#6116=ORIENTED_EDGE('',*,*,#4150,.T.);
#6117=ORIENTED_EDGE('',*,*,#4147,.T.);
#6118=ORIENTED_EDGE('',*,*,#4141,.T.);
#6119=ORIENTED_EDGE('',*,*,#4246,.T.);
#6120=ORIENTED_EDGE('',*,*,#4237,.T.);
#6121=ORIENTED_EDGE('',*,*,#4243,.T.);
#6122=ORIENTED_EDGE('',*,*,#4248,.F.);
#6123=ORIENTED_EDGE('',*,*,#4249,.T.);
#6124=ORIENTED_EDGE('',*,*,#4250,.T.);
#6125=ORIENTED_EDGE('',*,*,#4251,.F.);
#6126=ORIENTED_EDGE('',*,*,#4252,.F.);
#6127=ORIENTED_EDGE('',*,*,#4253,.T.);
#6128=ORIENTED_EDGE('',*,*,#4254,.T.);
#6129=ORIENTED_EDGE('',*,*,#4249,.F.);
#6130=ORIENTED_EDGE('',*,*,#4255,.F.);
#6131=ORIENTED_EDGE('',*,*,#4256,.T.);
#6132=ORIENTED_EDGE('',*,*,#4257,.T.);
#6133=ORIENTED_EDGE('',*,*,#4253,.F.);
#6134=ORIENTED_EDGE('',*,*,#4258,.F.);
#6135=ORIENTED_EDGE('',*,*,#4259,.T.);
#6136=ORIENTED_EDGE('',*,*,#4260,.T.);
#6137=ORIENTED_EDGE('',*,*,#4256,.F.);
#6138=ORIENTED_EDGE('',*,*,#4261,.F.);
#6139=ORIENTED_EDGE('',*,*,#4262,.T.);
#6140=ORIENTED_EDGE('',*,*,#4263,.T.);
#6141=ORIENTED_EDGE('',*,*,#4259,.F.);
#6142=ORIENTED_EDGE('',*,*,#4264,.F.);
#6143=ORIENTED_EDGE('',*,*,#4251,.T.);
#6144=ORIENTED_EDGE('',*,*,#4265,.T.);
#6145=ORIENTED_EDGE('',*,*,#4262,.F.);
#6146=ORIENTED_EDGE('',*,*,#4265,.F.);
#6147=ORIENTED_EDGE('',*,*,#4250,.F.);
#6148=ORIENTED_EDGE('',*,*,#4254,.F.);
#6149=ORIENTED_EDGE('',*,*,#4257,.F.);
#6150=ORIENTED_EDGE('',*,*,#4260,.F.);
#6151=ORIENTED_EDGE('',*,*,#4263,.F.);
#6152=ORIENTED_EDGE('',*,*,#4266,.T.);
#6153=ORIENTED_EDGE('',*,*,#4242,.T.);
#6154=ORIENTED_EDGE('',*,*,#4245,.T.);
#6155=ORIENTED_EDGE('',*,*,#4247,.T.);
#6156=ORIENTED_EDGE('',*,*,#4055,.F.);
#6157=ORIENTED_EDGE('',*,*,#4266,.F.);
#6158=ORIENTED_EDGE('',*,*,#4267,.T.);
#6159=ORIENTED_EDGE('',*,*,#4268,.T.);
#6160=ORIENTED_EDGE('',*,*,#4267,.F.);
#6161=ORIENTED_EDGE('',*,*,#4268,.F.);
#6162=ORIENTED_EDGE('',*,*,#4248,.T.);
#6163=ORIENTED_EDGE('',*,*,#4264,.T.);
#6164=ORIENTED_EDGE('',*,*,#4261,.T.);
#6165=ORIENTED_EDGE('',*,*,#4258,.T.);
#6166=ORIENTED_EDGE('',*,*,#4255,.T.);
#6167=ORIENTED_EDGE('',*,*,#4252,.T.);
#6168=ORIENTED_EDGE('',*,*,#4240,.T.);
#6355=CYLINDRICAL_SURFACE('',#7305,0.14635);
#6356=CYLINDRICAL_SURFACE('',#7307,0.14635);
#6357=CYLINDRICAL_SURFACE('',#7308,0.14635);
#6358=CYLINDRICAL_SURFACE('',#7309,0.14635);
#6359=CYLINDRICAL_SURFACE('',#7310,0.14635);
#6360=CYLINDRICAL_SURFACE('',#7311,0.14635);
#6361=CYLINDRICAL_SURFACE('',#7312,0.14635);
#6362=CYLINDRICAL_SURFACE('',#7313,0.14635);
#6363=CYLINDRICAL_SURFACE('',#7314,0.14635);
#6364=CYLINDRICAL_SURFACE('',#7315,0.14635);
#6365=CYLINDRICAL_SURFACE('',#7316,0.14635);
#6366=CYLINDRICAL_SURFACE('',#7317,0.14635);
#6367=CYLINDRICAL_SURFACE('',#7318,0.14635);
#6368=CYLINDRICAL_SURFACE('',#7319,0.14635);
#6369=CYLINDRICAL_SURFACE('',#7320,0.14635);
#6370=CYLINDRICAL_SURFACE('',#7321,0.14635);
#6371=CYLINDRICAL_SURFACE('',#7322,0.14635);
#6372=CYLINDRICAL_SURFACE('',#7323,0.14635);
#6373=CYLINDRICAL_SURFACE('',#7324,0.14635);
#6374=CYLINDRICAL_SURFACE('',#7325,0.14635);
#6375=CYLINDRICAL_SURFACE('',#7326,0.14635);
#6376=CYLINDRICAL_SURFACE('',#7327,0.14635);
#6377=CYLINDRICAL_SURFACE('',#7328,0.14635);
#6378=CYLINDRICAL_SURFACE('',#7329,0.14635);
#6379=CYLINDRICAL_SURFACE('',#7330,0.14635);
#6380=CYLINDRICAL_SURFACE('',#7331,0.14635);
#6381=CYLINDRICAL_SURFACE('',#7332,0.14635);
#6382=CYLINDRICAL_SURFACE('',#7333,0.14635);
#6383=CYLINDRICAL_SURFACE('',#7334,0.14635);
#6384=CYLINDRICAL_SURFACE('',#7335,0.14635);
#6385=CYLINDRICAL_SURFACE('',#7336,0.117775);
#6386=CYLINDRICAL_SURFACE('',#7338,0.117775);
#6387=CYLINDRICAL_SURFACE('',#7339,0.117775);
#6388=CYLINDRICAL_SURFACE('',#7340,0.117775);
#6389=CYLINDRICAL_SURFACE('',#7341,0.117775);
#6390=CYLINDRICAL_SURFACE('',#7342,0.117775);
#6391=CYLINDRICAL_SURFACE('',#7343,0.117775);
#6392=CYLINDRICAL_SURFACE('',#7344,0.117775);
#6393=CYLINDRICAL_SURFACE('',#7345,0.117775);
#6394=CYLINDRICAL_SURFACE('',#7346,0.117775);
#6395=CYLINDRICAL_SURFACE('',#7347,0.117775);
#6396=CYLINDRICAL_SURFACE('',#7348,0.117775);
#6397=CYLINDRICAL_SURFACE('',#7349,0.117775);
#6398=CYLINDRICAL_SURFACE('',#7350,0.117775);
#6399=CYLINDRICAL_SURFACE('',#7351,0.117775);
#6400=CYLINDRICAL_SURFACE('',#7352,0.117775);
#6401=CYLINDRICAL_SURFACE('',#7353,0.117775);
#6402=CYLINDRICAL_SURFACE('',#7354,0.117775);
#6403=CYLINDRICAL_SURFACE('',#7355,0.117775);
#6404=CYLINDRICAL_SURFACE('',#7356,0.117775);
#6405=CYLINDRICAL_SURFACE('',#7357,0.117775);
#6406=CYLINDRICAL_SURFACE('',#7358,0.117775);
#6407=CYLINDRICAL_SURFACE('',#7359,0.117775);
#6408=CYLINDRICAL_SURFACE('',#7360,0.117775);
#6409=CYLINDRICAL_SURFACE('',#7361,0.117775);
#6410=CYLINDRICAL_SURFACE('',#7362,0.117775);
#6411=CYLINDRICAL_SURFACE('',#7363,0.117775);
#6412=CYLINDRICAL_SURFACE('',#7364,0.117775);
#6413=CYLINDRICAL_SURFACE('',#7365,0.117775);
#6414=CYLINDRICAL_SURFACE('',#7366,0.117775);
#6415=CYLINDRICAL_SURFACE('',#7370,0.117775);
#6416=CYLINDRICAL_SURFACE('',#7372,0.14635);
#6417=CYLINDRICAL_SURFACE('',#7382,0.275);
#6718=ADVANCED_FACE('',(#1099),#6355,.T.);
#6719=ADVANCED_FACE('',(#1100),#6356,.T.);
#6720=ADVANCED_FACE('',(#1101),#6357,.T.);
#6721=ADVANCED_FACE('',(#1102),#6358,.T.);
#6722=ADVANCED_FACE('',(#1103),#6359,.T.);
#6723=ADVANCED_FACE('',(#1104),#6360,.T.);
#6724=ADVANCED_FACE('',(#1105),#6361,.T.);
#6725=ADVANCED_FACE('',(#1106),#6362,.T.);
#6726=ADVANCED_FACE('',(#1107),#6363,.T.);
#6727=ADVANCED_FACE('',(#1108),#6364,.T.);
#6728=ADVANCED_FACE('',(#1109),#6365,.T.);
#6729=ADVANCED_FACE('',(#1110),#6366,.T.);
#6730=ADVANCED_FACE('',(#1111),#6367,.T.);
#6731=ADVANCED_FACE('',(#1112),#6368,.T.);
#6732=ADVANCED_FACE('',(#1113),#6369,.T.);
#6733=ADVANCED_FACE('',(#1114),#6370,.T.);
#6734=ADVANCED_FACE('',(#1115),#6371,.T.);
#6735=ADVANCED_FACE('',(#1116),#6372,.T.);
#6736=ADVANCED_FACE('',(#1117),#6373,.T.);
#6737=ADVANCED_FACE('',(#1118),#6374,.T.);
#6738=ADVANCED_FACE('',(#1119),#6375,.T.);
#6739=ADVANCED_FACE('',(#1120),#6376,.T.);
#6740=ADVANCED_FACE('',(#1121),#6377,.T.);
#6741=ADVANCED_FACE('',(#1122),#6378,.T.);
#6742=ADVANCED_FACE('',(#1123),#6379,.T.);
#6743=ADVANCED_FACE('',(#1124),#6380,.T.);
#6744=ADVANCED_FACE('',(#1125),#6381,.T.);
#6745=ADVANCED_FACE('',(#1126),#6382,.T.);
#6746=ADVANCED_FACE('',(#1127),#6383,.T.);
#6747=ADVANCED_FACE('',(#1128),#6384,.T.);
#6748=ADVANCED_FACE('',(#1129),#6385,.T.);
#6749=ADVANCED_FACE('',(#1130),#6386,.T.);
#6750=ADVANCED_FACE('',(#1131),#6387,.T.);
#6751=ADVANCED_FACE('',(#1132),#6388,.T.);
#6752=ADVANCED_FACE('',(#1133),#6389,.T.);
#6753=ADVANCED_FACE('',(#1134),#6390,.T.);
#6754=ADVANCED_FACE('',(#1135),#6391,.T.);
#6755=ADVANCED_FACE('',(#1136),#6392,.T.);
#6756=ADVANCED_FACE('',(#1137),#6393,.T.);
#6757=ADVANCED_FACE('',(#1138),#6394,.T.);
#6758=ADVANCED_FACE('',(#1139),#6395,.T.);
#6759=ADVANCED_FACE('',(#1140),#6396,.T.);
#6760=ADVANCED_FACE('',(#1141),#6397,.T.);
#6761=ADVANCED_FACE('',(#1142),#6398,.T.);
#6762=ADVANCED_FACE('',(#1143),#6399,.T.);
#6763=ADVANCED_FACE('',(#1144),#6400,.T.);
#6764=ADVANCED_FACE('',(#1145),#6401,.T.);
#6765=ADVANCED_FACE('',(#1146),#6402,.T.);
#6766=ADVANCED_FACE('',(#1147),#6403,.T.);
#6767=ADVANCED_FACE('',(#1148),#6404,.T.);
#6768=ADVANCED_FACE('',(#1149),#6405,.T.);
#6769=ADVANCED_FACE('',(#1150),#6406,.T.);
#6770=ADVANCED_FACE('',(#1151),#6407,.T.);
#6771=ADVANCED_FACE('',(#1152),#6408,.T.);
#6772=ADVANCED_FACE('',(#1153),#6409,.T.);
#6773=ADVANCED_FACE('',(#1154),#6410,.T.);
#6774=ADVANCED_FACE('',(#1155),#6411,.T.);
#6775=ADVANCED_FACE('',(#1156),#6412,.T.);
#6776=ADVANCED_FACE('',(#1157),#6413,.T.);
#6777=ADVANCED_FACE('',(#1158),#6414,.T.);
#6778=ADVANCED_FACE('',(#1159),#75,.T.);
#6779=ADVANCED_FACE('',(#1160),#168,.F.);
#6780=ADVANCED_FACE('',(#1161),#6415,.T.);
#6781=ADVANCED_FACE('',(#1162),#169,.F.);
#6782=ADVANCED_FACE('',(#1163),#6416,.T.);
#6783=ADVANCED_FACE('',(#1164),#793,.F.);
#6784=ADVANCED_FACE('',(#1165),#794,.F.);
#6785=ADVANCED_FACE('',(#1166),#795,.F.);
#6786=ADVANCED_FACE('',(#1167),#796,.F.);
#6787=ADVANCED_FACE('',(#1168),#797,.F.);
#6788=ADVANCED_FACE('',(#1169),#798,.F.);
#6789=ADVANCED_FACE('',(#1170),#799,.F.);
#6790=ADVANCED_FACE('',(#1171,#647),#800,.T.);
#6791=ADVANCED_FACE('',(#1172),#6417,.T.);
#6792=ADVANCED_FACE('',(#1173,#648),#801,.F.);
#6793=ADVANCED_FACE('',(#1174),#802,.T.);
#6827=CLOSED_SHELL('',(#6718,#6719,#6720,#6721,#6722,#6723,#6724,#6725,
#6726,#6727,#6728,#6729,#6730,#6731,#6732,#6733,#6734,#6735,#6736,#6737,
#6738,#6739,#6740,#6741,#6742,#6743,#6744,#6745,#6746,#6747,#6748,#6749,
#6750,#6751,#6752,#6753,#6754,#6755,#6756,#6757,#6758,#6759,#6760,#6761,
#6762,#6763,#6764,#6765,#6766,#6767,#6768,#6769,#6770,#6771,#6772,#6773,
#6774,#6775,#6776,#6777,#6778,#6779,#6780,#6781,#6782,#6783,#6784,#6785,
#6786,#6787,#6788,#6789,#6790,#6791,#6792,#6793));
#7304=AXIS2_PLACEMENT_3D('',#13956,#8502,#8503);
#7305=AXIS2_PLACEMENT_3D('',#13957,#8504,#8505);
#7306=AXIS2_PLACEMENT_3D('',#13973,#8507,#8508);
#7307=AXIS2_PLACEMENT_3D('',#13981,#8509,#8510);
#7308=AXIS2_PLACEMENT_3D('',#14029,#8512,#8513);
#7309=AXIS2_PLACEMENT_3D('',#14077,#8515,#8516);
#7310=AXIS2_PLACEMENT_3D('',#14128,#8518,#8519);
#7311=AXIS2_PLACEMENT_3D('',#14176,#8521,#8522);
#7312=AXIS2_PLACEMENT_3D('',#14224,#8524,#8525);
#7313=AXIS2_PLACEMENT_3D('',#14272,#8527,#8528);
#7314=AXIS2_PLACEMENT_3D('',#14326,#8530,#8531);
#7315=AXIS2_PLACEMENT_3D('',#14374,#8533,#8534);
#7316=AXIS2_PLACEMENT_3D('',#14422,#8536,#8537);
#7317=AXIS2_PLACEMENT_3D('',#14476,#8539,#8540);
#7318=AXIS2_PLACEMENT_3D('',#14524,#8542,#8543);
#7319=AXIS2_PLACEMENT_3D('',#14572,#8545,#8546);
#7320=AXIS2_PLACEMENT_3D('',#14620,#8548,#8549);
#7321=AXIS2_PLACEMENT_3D('',#14674,#8551,#8552);
#7322=AXIS2_PLACEMENT_3D('',#14722,#8554,#8555);
#7323=AXIS2_PLACEMENT_3D('',#14770,#8557,#8558);
#7324=AXIS2_PLACEMENT_3D('',#14824,#8560,#8561);
#7325=AXIS2_PLACEMENT_3D('',#14872,#8563,#8564);
#7326=AXIS2_PLACEMENT_3D('',#14920,#8566,#8567);
#7327=AXIS2_PLACEMENT_3D('',#14974,#8569,#8570);
#7328=AXIS2_PLACEMENT_3D('',#15022,#8572,#8573);
#7329=AXIS2_PLACEMENT_3D('',#15070,#8575,#8576);
#7330=AXIS2_PLACEMENT_3D('',#15118,#8578,#8579);
#7331=AXIS2_PLACEMENT_3D('',#15172,#8581,#8582);
#7332=AXIS2_PLACEMENT_3D('',#15220,#8584,#8585);
#7333=AXIS2_PLACEMENT_3D('',#15268,#8587,#8588);
#7334=AXIS2_PLACEMENT_3D('',#15322,#8590,#8591);
#7335=AXIS2_PLACEMENT_3D('',#15370,#8593,#8594);
#7336=AXIS2_PLACEMENT_3D('',#15418,#8596,#8597);
#7337=AXIS2_PLACEMENT_3D('',#15434,#8599,#8600);
#7338=AXIS2_PLACEMENT_3D('',#15444,#8601,#8602);
#7339=AXIS2_PLACEMENT_3D('',#15468,#8604,#8605);
#7340=AXIS2_PLACEMENT_3D('',#15492,#8607,#8608);
#7341=AXIS2_PLACEMENT_3D('',#15517,#8610,#8611);
#7342=AXIS2_PLACEMENT_3D('',#15542,#8613,#8614);
#7343=AXIS2_PLACEMENT_3D('',#15566,#8616,#8617);
#7344=AXIS2_PLACEMENT_3D('',#15591,#8619,#8620);
#7345=AXIS2_PLACEMENT_3D('',#15616,#8622,#8623);
#7346=AXIS2_PLACEMENT_3D('',#15640,#8625,#8626);
#7347=AXIS2_PLACEMENT_3D('',#15664,#8628,#8629);
#7348=AXIS2_PLACEMENT_3D('',#15689,#8631,#8632);
#7349=AXIS2_PLACEMENT_3D('',#15714,#8634,#8635);
#7350=AXIS2_PLACEMENT_3D('',#15738,#8637,#8638);
#7351=AXIS2_PLACEMENT_3D('',#15763,#8640,#8641);
#7352=AXIS2_PLACEMENT_3D('',#15788,#8643,#8644);
#7353=AXIS2_PLACEMENT_3D('',#15812,#8646,#8647);
#7354=AXIS2_PLACEMENT_3D('',#15837,#8649,#8650);
#7355=AXIS2_PLACEMENT_3D('',#15862,#8652,#8653);
#7356=AXIS2_PLACEMENT_3D('',#15886,#8655,#8656);
#7357=AXIS2_PLACEMENT_3D('',#15910,#8658,#8659);
#7358=AXIS2_PLACEMENT_3D('',#15935,#8661,#8662);
#7359=AXIS2_PLACEMENT_3D('',#15960,#8664,#8665);
#7360=AXIS2_PLACEMENT_3D('',#15984,#8667,#8668);
#7361=AXIS2_PLACEMENT_3D('',#16009,#8670,#8671);
#7362=AXIS2_PLACEMENT_3D('',#16034,#8673,#8674);
#7363=AXIS2_PLACEMENT_3D('',#16058,#8676,#8677);
#7364=AXIS2_PLACEMENT_3D('',#16083,#8679,#8680);
#7365=AXIS2_PLACEMENT_3D('',#16107,#8682,#8683);
#7366=AXIS2_PLACEMENT_3D('',#16132,#8685,#8686);
#7367=AXIS2_PLACEMENT_3D('',#16156,#8688,#8689);
#7368=AXIS2_PLACEMENT_3D('',#16318,#8690,#8691);
#7369=AXIS2_PLACEMENT_3D('',#16337,#8693,#8694);
#7370=AXIS2_PLACEMENT_3D('',#17199,#8695,#8696);
#7371=AXIS2_PLACEMENT_3D('',#17210,#8697,#8698);
#7372=AXIS2_PLACEMENT_3D('',#18077,#8699,#8700);
#7373=AXIS2_PLACEMENT_3D('',#18078,#8701,#8702);
#7374=AXIS2_PLACEMENT_3D('',#18087,#8707,#8708);
#7375=AXIS2_PLACEMENT_3D('',#18093,#8712,#8713);
#7376=AXIS2_PLACEMENT_3D('',#18099,#8717,#8718);
#7377=AXIS2_PLACEMENT_3D('',#18105,#8722,#8723);
#7378=AXIS2_PLACEMENT_3D('',#18111,#8727,#8728);
#7379=AXIS2_PLACEMENT_3D('',#18114,#8731,#8732);
#7380=AXIS2_PLACEMENT_3D('',#18115,#8733,#8734);
#7381=AXIS2_PLACEMENT_3D('',#18117,#8735,#8736);
#7382=AXIS2_PLACEMENT_3D('',#18118,#8737,#8738);
#7383=AXIS2_PLACEMENT_3D('',#18121,#8740,#8741);
#7384=AXIS2_PLACEMENT_3D('',#18122,#8742,#8743);
#7385=AXIS2_PLACEMENT_3D('',#18123,#8744,#8745);
#8502=DIRECTION('axis',(0.,0.,1.));
#8503=DIRECTION('refdir',(1.,0.,0.));
#8504=DIRECTION('center_axis',(0.,0.,1.));
#8505=DIRECTION('ref_axis',(1.,0.,0.));
#8506=DIRECTION('',(0.,0.,-1.));
#8507=DIRECTION('center_axis',(0.,0.,-1.));
#8508=DIRECTION('ref_axis',(1.,0.,0.));
#8509=DIRECTION('center_axis',(0.,0.,1.));
#8510=DIRECTION('ref_axis',(1.,0.,0.));
#8511=DIRECTION('',(0.,0.,-1.));
#8512=DIRECTION('center_axis',(0.,0.,1.));
#8513=DIRECTION('ref_axis',(1.,0.,0.));
#8514=DIRECTION('',(0.,0.,-1.));
#8515=DIRECTION('center_axis',(0.,0.,1.));
#8516=DIRECTION('ref_axis',(1.,0.,0.));
#8517=DIRECTION('',(0.,0.,-1.));
#8518=DIRECTION('center_axis',(0.,0.,1.));
#8519=DIRECTION('ref_axis',(1.,0.,0.));
#8520=DIRECTION('',(0.,0.,-1.));
#8521=DIRECTION('center_axis',(0.,0.,1.));
#8522=DIRECTION('ref_axis',(1.,0.,0.));
#8523=DIRECTION('',(0.,0.,-1.));
#8524=DIRECTION('center_axis',(0.,0.,1.));
#8525=DIRECTION('ref_axis',(1.,0.,0.));
#8526=DIRECTION('',(0.,0.,-1.));
#8527=DIRECTION('center_axis',(0.,0.,1.));
#8528=DIRECTION('ref_axis',(1.,0.,0.));
#8529=DIRECTION('',(0.,0.,-1.));
#8530=DIRECTION('center_axis',(0.,0.,1.));
#8531=DIRECTION('ref_axis',(1.,0.,0.));
#8532=DIRECTION('',(0.,0.,-1.));
#8533=DIRECTION('center_axis',(0.,0.,1.));
#8534=DIRECTION('ref_axis',(1.,0.,0.));
#8535=DIRECTION('',(0.,0.,-1.));
#8536=DIRECTION('center_axis',(0.,0.,1.));
#8537=DIRECTION('ref_axis',(1.,0.,0.));
#8538=DIRECTION('',(0.,0.,-1.));
#8539=DIRECTION('center_axis',(0.,0.,1.));
#8540=DIRECTION('ref_axis',(1.,0.,0.));
#8541=DIRECTION('',(0.,0.,-1.));
#8542=DIRECTION('center_axis',(0.,0.,1.));
#8543=DIRECTION('ref_axis',(1.,0.,0.));
#8544=DIRECTION('',(0.,0.,-1.));
#8545=DIRECTION('center_axis',(0.,0.,1.));
#8546=DIRECTION('ref_axis',(1.,0.,0.));
#8547=DIRECTION('',(0.,0.,-1.));
#8548=DIRECTION('center_axis',(0.,0.,1.));
#8549=DIRECTION('ref_axis',(1.,0.,0.));
#8550=DIRECTION('',(0.,0.,-1.));
#8551=DIRECTION('center_axis',(0.,0.,1.));
#8552=DIRECTION('ref_axis',(1.,0.,0.));
#8553=DIRECTION('',(0.,0.,-1.));
#8554=DIRECTION('center_axis',(0.,0.,1.));
#8555=DIRECTION('ref_axis',(1.,0.,0.));
#8556=DIRECTION('',(0.,0.,-1.));
#8557=DIRECTION('center_axis',(0.,0.,1.));
#8558=DIRECTION('ref_axis',(1.,0.,0.));
#8559=DIRECTION('',(0.,0.,-1.));
#8560=DIRECTION('center_axis',(0.,0.,1.));
#8561=DIRECTION('ref_axis',(1.,0.,0.));
#8562=DIRECTION('',(0.,0.,-1.));
#8563=DIRECTION('center_axis',(0.,0.,1.));
#8564=DIRECTION('ref_axis',(1.,0.,0.));
#8565=DIRECTION('',(0.,0.,-1.));
#8566=DIRECTION('center_axis',(0.,0.,1.));
#8567=DIRECTION('ref_axis',(1.,0.,0.));
#8568=DIRECTION('',(0.,0.,-1.));
#8569=DIRECTION('center_axis',(0.,0.,1.));
#8570=DIRECTION('ref_axis',(1.,0.,0.));
#8571=DIRECTION('',(0.,0.,-1.));
#8572=DIRECTION('center_axis',(0.,0.,1.));
#8573=DIRECTION('ref_axis',(1.,0.,0.));
#8574=DIRECTION('',(0.,0.,-1.));
#8575=DIRECTION('center_axis',(0.,0.,1.));
#8576=DIRECTION('ref_axis',(1.,0.,0.));
#8577=DIRECTION('',(0.,0.,-1.));
#8578=DIRECTION('center_axis',(0.,0.,1.));
#8579=DIRECTION('ref_axis',(1.,0.,0.));
#8580=DIRECTION('',(0.,0.,-1.));
#8581=DIRECTION('center_axis',(0.,0.,1.));
#8582=DIRECTION('ref_axis',(1.,0.,0.));
#8583=DIRECTION('',(0.,0.,-1.));
#8584=DIRECTION('center_axis',(0.,0.,1.));
#8585=DIRECTION('ref_axis',(1.,0.,0.));
#8586=DIRECTION('',(0.,0.,-1.));
#8587=DIRECTION('center_axis',(0.,0.,1.));
#8588=DIRECTION('ref_axis',(1.,0.,0.));
#8589=DIRECTION('',(0.,0.,-1.));
#8590=DIRECTION('center_axis',(0.,0.,1.));
#8591=DIRECTION('ref_axis',(1.,0.,0.));
#8592=DIRECTION('',(0.,0.,-1.));
#8593=DIRECTION('center_axis',(0.,0.,1.));
#8594=DIRECTION('ref_axis',(1.,0.,0.));
#8595=DIRECTION('',(0.,0.,-1.));
#8596=DIRECTION('center_axis',(0.,0.,1.));
#8597=DIRECTION('ref_axis',(1.,-2.42503376499884E-13,0.));
#8598=DIRECTION('',(0.,0.,1.));
#8599=DIRECTION('center_axis',(0.,0.,-1.));
#8600=DIRECTION('ref_axis',(1.,-2.42503376499884E-13,0.));
#8601=DIRECTION('center_axis',(0.,0.,1.));
#8602=DIRECTION('ref_axis',(1.,-2.42503376499884E-13,0.));
#8603=DIRECTION('',(0.,0.,1.));
#8604=DIRECTION('center_axis',(0.,0.,1.));
#8605=DIRECTION('ref_axis',(1.,-2.42503376499884E-13,0.));
#8606=DIRECTION('',(0.,0.,1.));
#8607=DIRECTION('center_axis',(0.,0.,1.));
#8608=DIRECTION('ref_axis',(1.,-2.42503376499884E-13,0.));
#8609=DIRECTION('',(0.,0.,1.));
#8610=DIRECTION('center_axis',(0.,0.,1.));
#8611=DIRECTION('ref_axis',(1.,-2.42503376499884E-13,0.));
#8612=DIRECTION('',(0.,0.,1.));
#8613=DIRECTION('center_axis',(0.,0.,1.));
#8614=DIRECTION('ref_axis',(1.,-2.42503376499884E-13,0.));
#8615=DIRECTION('',(0.,0.,1.));
#8616=DIRECTION('center_axis',(0.,0.,1.));
#8617=DIRECTION('ref_axis',(1.,-2.42503376499884E-13,0.));
#8618=DIRECTION('',(0.,0.,1.));
#8619=DIRECTION('center_axis',(0.,0.,1.));
#8620=DIRECTION('ref_axis',(1.,-2.42503376499884E-13,0.));
#8621=DIRECTION('',(0.,0.,1.));
#8622=DIRECTION('center_axis',(0.,0.,1.));
#8623=DIRECTION('ref_axis',(1.,-2.42503376499884E-13,0.));
#8624=DIRECTION('',(0.,0.,1.));
#8625=DIRECTION('center_axis',(0.,0.,1.));
#8626=DIRECTION('ref_axis',(1.,-2.42503376499884E-13,0.));
#8627=DIRECTION('',(0.,0.,1.));
#8628=DIRECTION('center_axis',(0.,0.,1.));
#8629=DIRECTION('ref_axis',(1.,-2.42503376499884E-13,0.));
#8630=DIRECTION('',(0.,0.,1.));
#8631=DIRECTION('center_axis',(0.,0.,1.));
#8632=DIRECTION('ref_axis',(1.,-2.42503376499884E-13,0.));
#8633=DIRECTION('',(0.,0.,1.));
#8634=DIRECTION('center_axis',(0.,0.,1.));
#8635=DIRECTION('ref_axis',(1.,-2.42503376499884E-13,0.));
#8636=DIRECTION('',(0.,0.,1.));
#8637=DIRECTION('center_axis',(0.,0.,1.));
#8638=DIRECTION('ref_axis',(1.,-2.42503376499884E-13,0.));
#8639=DIRECTION('',(0.,0.,1.));
#8640=DIRECTION('center_axis',(0.,0.,1.));
#8641=DIRECTION('ref_axis',(1.,-2.42503376499884E-13,0.));
#8642=DIRECTION('',(0.,0.,1.));
#8643=DIRECTION('center_axis',(0.,0.,1.));
#8644=DIRECTION('ref_axis',(1.,-2.42503376499884E-13,0.));
#8645=DIRECTION('',(0.,0.,1.));
#8646=DIRECTION('center_axis',(0.,0.,1.));
#8647=DIRECTION('ref_axis',(1.,-2.42503376499884E-13,0.));
#8648=DIRECTION('',(0.,0.,1.));
#8649=DIRECTION('center_axis',(0.,0.,1.));
#8650=DIRECTION('ref_axis',(1.,-2.42503376499884E-13,0.));
#8651=DIRECTION('',(0.,0.,1.));
#8652=DIRECTION('center_axis',(0.,0.,1.));
#8653=DIRECTION('ref_axis',(1.,-2.42503376499884E-13,0.));
#8654=DIRECTION('',(0.,0.,1.));
#8655=DIRECTION('center_axis',(0.,0.,1.));
#8656=DIRECTION('ref_axis',(1.,-2.42503376499884E-13,0.));
#8657=DIRECTION('',(0.,0.,1.));
#8658=DIRECTION('center_axis',(0.,0.,1.));
#8659=DIRECTION('ref_axis',(1.,-2.42503376499884E-13,0.));
#8660=DIRECTION('',(0.,0.,1.));
#8661=DIRECTION('center_axis',(0.,0.,1.));
#8662=DIRECTION('ref_axis',(1.,-2.42503376499884E-13,0.));
#8663=DIRECTION('',(0.,0.,1.));
#8664=DIRECTION('center_axis',(0.,0.,1.));
#8665=DIRECTION('ref_axis',(1.,-2.42503376499884E-13,0.));
#8666=DIRECTION('',(0.,0.,1.));
#8667=DIRECTION('center_axis',(0.,0.,1.));
#8668=DIRECTION('ref_axis',(1.,-2.42503376499884E-13,0.));
#8669=DIRECTION('',(0.,0.,1.));
#8670=DIRECTION('center_axis',(0.,0.,1.));
#8671=DIRECTION('ref_axis',(1.,-2.42503376499884E-13,0.));
#8672=DIRECTION('',(0.,0.,1.));
#8673=DIRECTION('center_axis',(0.,0.,1.));
#8674=DIRECTION('ref_axis',(1.,-2.42503376499884E-13,0.));
#8675=DIRECTION('',(0.,0.,1.));
#8676=DIRECTION('center_axis',(0.,0.,1.));
#8677=DIRECTION('ref_axis',(1.,-2.42503376499884E-13,0.));
#8678=DIRECTION('',(0.,0.,1.));
#8679=DIRECTION('center_axis',(0.,0.,1.));
#8680=DIRECTION('ref_axis',(1.,-2.42503376499884E-13,0.));
#8681=DIRECTION('',(0.,0.,1.));
#8682=DIRECTION('center_axis',(0.,0.,1.));
#8683=DIRECTION('ref_axis',(1.,-2.42503376499884E-13,0.));
#8684=DIRECTION('',(0.,0.,1.));
#8685=DIRECTION('center_axis',(0.,0.,1.));
#8686=DIRECTION('ref_axis',(1.,-2.42503376499884E-13,0.));
#8687=DIRECTION('',(0.,0.,1.));
#8688=DIRECTION('center_axis',(0.,0.,-1.));
#8689=DIRECTION('ref_axis',(1.,0.,0.));
#8690=DIRECTION('center_axis',(0.,0.,-1.));
#8691=DIRECTION('ref_axis',(1.,0.,0.));
#8692=DIRECTION('',(0.707106781186547,8.65956056235493E-17,0.707106781186548));
#8693=DIRECTION('center_axis',(0.,0.,1.));
#8694=DIRECTION('ref_axis',(1.,0.,0.));
#8695=DIRECTION('center_axis',(0.,0.,1.));
#8696=DIRECTION('ref_axis',(1.,-2.42503376499884E-13,0.));
#8697=DIRECTION('center_axis',(0.,0.,-1.));
#8698=DIRECTION('ref_axis',(1.,-2.42503376499884E-13,0.));
#8699=DIRECTION('center_axis',(0.,0.,1.));
#8700=DIRECTION('ref_axis',(1.,0.,0.));
#8701=DIRECTION('center_axis',(-1.92296268638356E-16,-1.,0.));
#8702=DIRECTION('ref_axis',(1.,-1.92296268638356E-16,0.));
#8703=DIRECTION('',(1.,-1.92296268638356E-16,0.));
#8704=DIRECTION('',(0.,0.,1.));
#8705=DIRECTION('',(1.,-1.92296268638356E-16,0.));
#8706=DIRECTION('',(0.,0.,1.));
#8707=DIRECTION('center_axis',(-0.866025403784439,-0.5,0.));
#8708=DIRECTION('ref_axis',(0.5,-0.866025403784439,0.));
#8709=DIRECTION('',(0.5,-0.866025403784439,0.));
#8710=DIRECTION('',(0.,0.,1.));
#8711=DIRECTION('',(0.5,-0.866025403784439,0.));
#8712=DIRECTION('center_axis',(-0.866025403784439,0.5,0.));
#8713=DIRECTION('ref_axis',(-0.5,-0.866025403784439,0.));
#8714=DIRECTION('',(-0.5,-0.866025403784439,0.));
#8715=DIRECTION('',(0.,0.,1.));
#8716=DIRECTION('',(-0.5,-0.866025403784438,0.));
#8717=DIRECTION('center_axis',(1.92296268638356E-16,1.,0.));
#8718=DIRECTION('ref_axis',(-1.,1.92296268638356E-16,0.));
#8719=DIRECTION('',(-1.,1.92296268638356E-16,0.));
#8720=DIRECTION('',(0.,0.,1.));
#8721=DIRECTION('',(-1.,1.92296268638356E-16,0.));
#8722=DIRECTION('center_axis',(0.866025403784439,0.5,0.));
#8723=DIRECTION('ref_axis',(-0.5,0.866025403784439,0.));
#8724=DIRECTION('',(-0.5,0.866025403784439,0.));
#8725=DIRECTION('',(0.,0.,1.));
#8726=DIRECTION('',(-0.5,0.866025403784439,0.));
#8727=DIRECTION('center_axis',(0.866025403784439,-0.5,0.));
#8728=DIRECTION('ref_axis',(0.5,0.866025403784439,0.));
#8729=DIRECTION('',(0.5,0.866025403784439,0.));
#8730=DIRECTION('',(0.5,0.866025403784439,0.));
#8731=DIRECTION('center_axis',(0.,0.,1.));
#8732=DIRECTION('ref_axis',(1.,0.,0.));
#8733=DIRECTION('center_axis',(0.,0.,1.));
#8734=DIRECTION('ref_axis',(1.,0.,0.));
#8735=DIRECTION('center_axis',(0.,0.,1.));
#8736=DIRECTION('ref_axis',(1.,0.,0.));
#8737=DIRECTION('center_axis',(0.,0.,1.));
#8738=DIRECTION('ref_axis',(1.,0.,0.));
#8739=DIRECTION('',(0.,0.,-1.));
#8740=DIRECTION('center_axis',(0.,0.,1.));
#8741=DIRECTION('ref_axis',(1.,0.,0.));
#8742=DIRECTION('center_axis',(0.,0.,1.));
#8743=DIRECTION('ref_axis',(1.,0.,0.));
#8744=DIRECTION('center_axis',(0.,0.,1.));
#8745=DIRECTION('ref_axis',(1.,0.,0.));
#13956=CARTESIAN_POINT('',(0.,0.,0.));
#13957=CARTESIAN_POINT('Origin',(0.,0.,0.));
#13958=CARTESIAN_POINT('',(-0.14652705620645,9.44412402177196E-5,0.0160655045842905));
#13959=CARTESIAN_POINT('',(-0.146479946776166,0.000162062070299865,0.00893449541571059));
#13960=CARTESIAN_POINT('',(-0.14635,-1.79227059055215E-17,0.));
#13961=CARTESIAN_POINT('',(0.0634007094575209,0.131904027763685,0.));
#13962=CARTESIAN_POINT('Ctrl Pts',(-0.14652705620645,9.44412402177196E-5,
0.0160655045842905));
#13963=CARTESIAN_POINT('Ctrl Pts',(-0.146560923555419,0.00502618404349199,
0.0157963945919035));
#13964=CARTESIAN_POINT('Ctrl Pts',(-0.146333578783787,0.00995455679532004,
0.0155272845995164));
#13965=CARTESIAN_POINT('Ctrl Pts',(-0.14583475180505,0.0148550342388422,
0.0152581746071293));
#13966=CARTESIAN_POINT('Ctrl Pts',(-0.140929468554047,0.0630445487404258,
0.0126118447280274));
#13967=CARTESIAN_POINT('Ctrl Pts',(-0.10977174472993,0.108536575508351,
0.0099655148489255));
#13968=CARTESIAN_POINT('Ctrl Pts',(-0.0666135938566871,0.13056551637767,
0.00731918496982359));
#13969=CARTESIAN_POINT('Ctrl Pts',(-0.0268248419338395,0.150874636338504,
0.00487945664654906));
#13970=CARTESIAN_POINT('Ctrl Pts',(0.0231637104697219,0.151241233100125,
0.00243972832327453));
#13971=CARTESIAN_POINT('Ctrl Pts',(0.0635546915223951,0.132092229195826,
-2.16840434497101E-19));
#13972=CARTESIAN_POINT('',(-0.0634007094575146,0.131904027763688,0.));
#13973=CARTESIAN_POINT('Origin',(0.,0.,0.));
#13974=CARTESIAN_POINT('Ctrl Pts',(-0.0634007094575145,0.131904027763688,
-3.88578058618805E-16));
#13975=CARTESIAN_POINT('Ctrl Pts',(-0.107282641710421,0.110811831533068,
0.00264738937425961));
#13976=CARTESIAN_POINT('Ctrl Pts',(-0.139432201149969,0.0662847592091173,
0.00529477874851962));
#13977=CARTESIAN_POINT('Ctrl Pts',(-0.145436119191498,0.0182745223106641,
0.00794216812277962));
#13978=CARTESIAN_POINT('Ctrl Pts',(-0.146186273512714,0.0122759249909008,
0.00827294388708994));
#13979=CARTESIAN_POINT('Ctrl Pts',(-0.146528267289359,0.00622295186417552,
0.00860371965140026));
#13980=CARTESIAN_POINT('Ctrl Pts',(-0.146479946776166,0.000162062070299865,
0.00893449541571059));
#13981=CARTESIAN_POINT('Origin',(0.,0.,0.));
#13982=CARTESIAN_POINT('',(-0.146148830924315,7.59978318484386E-5,0.0660655045842905));
#13983=CARTESIAN_POINT('',(-0.146133770585873,6.2751561688711E-5,0.0589344954157103));
#13984=CARTESIAN_POINT('',(-0.14635,-1.79227059055215E-17,0.));
#13985=CARTESIAN_POINT('Ctrl Pts',(-0.146148830924315,7.59978318484386E-5,
0.0660655045842905));
#13986=CARTESIAN_POINT('Ctrl Pts',(-0.146240443598182,0.0195917497831913,
0.0650077071998482));
#13987=CARTESIAN_POINT('Ctrl Pts',(-0.142607114239671,0.0390747476468127,
0.0639499098154059));
#13988=CARTESIAN_POINT('Ctrl Pts',(-0.135087779856993,0.056920264102034,
0.0628921124309636));
#13989=CARTESIAN_POINT('Ctrl Pts',(-0.116276389754784,0.10156503643559,
0.0602457825518617));
#13990=CARTESIAN_POINT('Ctrl Pts',(-0.073143724514267,0.135961331060063,
0.0575994526727599));
#13991=CARTESIAN_POINT('Ctrl Pts',(-0.025432083612881,0.144366623974243,
0.054953122793658));
#13992=CARTESIAN_POINT('Ctrl Pts',(0.0222795572885053,0.152771916888423,
0.0523067929145561));
#13993=CARTESIAN_POINT('Ctrl Pts',(0.0745701738507606,0.135186208092309,
0.0496604630354541));
#13994=CARTESIAN_POINT('Ctrl Pts',(0.107505148494886,0.0996564726649905,
0.0470141331563522));
#13995=CARTESIAN_POINT('Ctrl Pts',(0.140440123139012,0.0641267372376721,
0.0443678032772503));
#13996=CARTESIAN_POINT('Ctrl Pts',(0.154019455865009,0.010652975179149,
0.0417214733981484));
#13997=CARTESIAN_POINT('Ctrl Pts',(0.14202839331759,-0.0362847016460775,
0.0390751435190465));
#13998=CARTESIAN_POINT('Ctrl Pts',(0.130037330770172,-0.0832223784713041,
0.0364288136399446));
#13999=CARTESIAN_POINT('Ctrl Pts',(0.0924758729493388,-0.123623970063234,
0.0337824837608427));
#14000=CARTESIAN_POINT('Ctrl Pts',(0.0465351214488668,-0.139005253038876,
0.0311361538817407));
#14001=CARTESIAN_POINT('Ctrl Pts',(0.000594369948394902,-0.154386536014517,
0.0284898240026388));
#14002=CARTESIAN_POINT('Ctrl Pts',(-0.0537256752317158,-0.144747510373871,
0.025843494123537));
#14003=CARTESIAN_POINT('Ctrl Pts',(-0.0915592764828275,-0.114484496435928,
0.0231971642444351));
#14004=CARTESIAN_POINT('Ctrl Pts',(-0.125545511528741,-0.0872989822136326,
0.0208199443577202));
#14005=CARTESIAN_POINT('Ctrl Pts',(-0.146227884351973,-0.0434707826450544,
0.0184427244710054));
#14006=CARTESIAN_POINT('Ctrl Pts',(-0.14652705620645,9.44412402177196E-5,
0.0160655045842905));
#14007=CARTESIAN_POINT('Ctrl Pts',(-0.146479946776166,0.000162062070299865,
0.00893449541571059));
#14008=CARTESIAN_POINT('Ctrl Pts',(-0.146141530330399,-0.0422858476614564,
0.0112511090256603));
#14009=CARTESIAN_POINT('Ctrl Pts',(-0.126658161292025,-0.0851220706608281,
0.0135677226356099));
#14010=CARTESIAN_POINT('Ctrl Pts',(-0.0941604943243988,-0.112386678841155,
0.0158843362455596));
#14011=CARTESIAN_POINT('Ctrl Pts',(-0.0570226747722624,-0.143544241621566,
0.0185317256198196));
#14012=CARTESIAN_POINT('Ctrl Pts',(-0.00288875902448078,-0.154365965709432,
0.0211791149940796));
#14013=CARTESIAN_POINT('Ctrl Pts',(0.0434083729543798,-0.140002007265973,
0.0238265043683396));
#14014=CARTESIAN_POINT('Ctrl Pts',(0.0897055049332404,-0.125638048822514,
0.0264738937425996));
#14015=CARTESIAN_POINT('Ctrl Pts',(0.12816585314318,-0.0860884078477292,
0.0291212831168596));
#14016=CARTESIAN_POINT('Ctrl Pts',(0.141191617966992,-0.0394144013492358,
0.0317686724911196));
#14017=CARTESIAN_POINT('Ctrl Pts',(0.154217382790803,0.00725960514925768,
0.0344160618653796));
#14018=CARTESIAN_POINT('Ctrl Pts',(0.141808564228487,0.0610579771714599,
0.0370634512396396));
#14019=CARTESIAN_POINT('Ctrl Pts',(0.109639063769471,0.0973098477439542,
0.0397108406138996));
#14020=CARTESIAN_POINT('Ctrl Pts',(0.0774695633104545,0.133561718316448,
0.0423582299881596));
#14021=CARTESIAN_POINT('Ctrl Pts',(0.0255393809547383,0.152267087439235,
0.0450056193624196));
#14022=CARTESIAN_POINT('Ctrl Pts',(-0.0223595433272462,0.144872892294413,
0.0476530087366796));
#14023=CARTESIAN_POINT('Ctrl Pts',(-0.070258467609231,0.137478697149591,
0.0503003981109396));
#14024=CARTESIAN_POINT('Ctrl Pts',(-0.114126133817484,0.10398493773716,
0.0529477874851996));
#14025=CARTESIAN_POINT('Ctrl Pts',(-0.133871661545403,0.059725601630819,
0.0555951768594596));
#14026=CARTESIAN_POINT('Ctrl Pts',(-0.142173753131161,0.0411165744656389,
0.0567082830448765));
#14027=CARTESIAN_POINT('Ctrl Pts',(-0.146211489678532,0.0206043892842972,
0.0578213892302934));
#14028=CARTESIAN_POINT('Ctrl Pts',(-0.146133770585873,6.2751561688711E-5,
0.0589344954157103));
#14029=CARTESIAN_POINT('Origin',(0.,0.,0.));
#14030=CARTESIAN_POINT('',(-0.146252097264499,-0.000124487410312429,0.116065504584291));
#14031=CARTESIAN_POINT('',(-0.146276374479508,-0.000129480650117819,0.10893449541571));
#14032=CARTESIAN_POINT('',(-0.14635,-1.79227059055215E-17,0.));
#14033=CARTESIAN_POINT('Ctrl Pts',(-0.146252097264499,-0.000124487410312429,
0.116065504584291));
#14034=CARTESIAN_POINT('Ctrl Pts',(-0.145977101830714,0.0338815411246725,
0.114219019807793));
#14035=CARTESIAN_POINT('Ctrl Pts',(-0.134160879762789,0.0680598926014691,
0.112372535031295));
#14036=CARTESIAN_POINT('Ctrl Pts',(-0.112484833627769,0.0939988017516943,
0.110526050254798));
#14037=CARTESIAN_POINT('Ctrl Pts',(-0.0814193359437304,0.131173714423195,
0.107879720375696));
#14038=CARTESIAN_POINT('Ctrl Pts',(-0.0301019434218634,0.151424966146533,
0.105233390496594));
#14039=CARTESIAN_POINT('Ctrl Pts',(0.0179785702873004,0.145483266051774,
0.102587060617492));
#14040=CARTESIAN_POINT('Ctrl Pts',(0.0660590839964643,0.139541565957016,
0.0999407307383904));
#14041=CARTESIAN_POINT('Ctrl Pts',(0.110902718892925,0.107406914044162,
0.0972944008592884));
#14042=CARTESIAN_POINT('Ctrl Pts',(0.131983829661647,0.0637877973597534,
0.0946480709801865));
#14043=CARTESIAN_POINT('Ctrl Pts',(0.15306494043037,0.0201686806753445,
0.0920017411010846));
#14044=CARTESIAN_POINT('Ctrl Pts',(0.150383527071356,-0.0349349007806195,
0.0893554112219828));
#14045=CARTESIAN_POINT('Ctrl Pts',(0.125166930059577,-0.0763010783846813,
0.0867090813428809));
#14046=CARTESIAN_POINT('Ctrl Pts',(0.0999503330477985,-0.117667255988743,
0.084062751463779));
#14047=CARTESIAN_POINT('Ctrl Pts',(0.0521985523832557,-0.145296029740903,
0.081416421584677));
#14048=CARTESIAN_POINT('Ctrl Pts',(0.00376830011669856,-0.146541450754272,
0.0787700917055751));
#14049=CARTESIAN_POINT('Ctrl Pts',(-0.0446619521498586,-0.147786871767642,
0.0761237618264732));
#14050=CARTESIAN_POINT('Ctrl Pts',(-0.09377067601843,-0.122648940042221,
0.0734774319473713));
#14051=CARTESIAN_POINT('Ctrl Pts',(-0.121079980470766,-0.0826333491581908,
0.0708311020682694));
#14052=CARTESIAN_POINT('Ctrl Pts',(-0.137473143648068,-0.0586128871159229,
0.0692425695736098));
#14053=CARTESIAN_POINT('Ctrl Pts',(-0.146011252866834,-0.02923151094855,
0.0676540370789502));
#14054=CARTESIAN_POINT('Ctrl Pts',(-0.146148830924315,7.59978318484386E-5,
0.0660655045842905));
#14055=CARTESIAN_POINT('Ctrl Pts',(-0.146133770585873,6.2751561688711E-5,
0.0589344954157103));
#14056=CARTESIAN_POINT('Ctrl Pts',(-0.146026644150963,-0.0282514289199324,
0.0604687786045534));
#14057=CARTESIAN_POINT('Ctrl Pts',(-0.138100435392092,-0.0566215672018456,
0.0620030617933965));
#14058=CARTESIAN_POINT('Ctrl Pts',(-0.122745086057252,-0.0801407530065182,
0.0635373449822396));
#14059=CARTESIAN_POINT('Ctrl Pts',(-0.0962495935935968,-0.120722858737265,
0.0661847343564996));
#14060=CARTESIAN_POINT('Ctrl Pts',(-0.0476352194187008,-0.146862157398507,
0.0688321237307596));
#14061=CARTESIAN_POINT('Ctrl Pts',(0.00082938917649622,-0.146587691816784,
0.0714795131050196));
#14062=CARTESIAN_POINT('Ctrl Pts',(0.0492939977716932,-0.146313226235061,
0.0741269024792796));
#14063=CARTESIAN_POINT('Ctrl Pts',(0.0976088407871913,-0.119624996410372,
0.0767742918535397));
#14064=CARTESIAN_POINT('Ctrl Pts',(0.123643642180798,-0.0787464320231966,
0.0794216812277997));
#14065=CARTESIAN_POINT('Ctrl Pts',(0.149678443574405,-0.0378678676360213,
0.0820690706020596));
#14066=CARTESIAN_POINT('Ctrl Pts',(0.153433203346121,0.0172010313136401,
0.0847164599763195));
#14067=CARTESIAN_POINT('Ctrl Pts',(0.133187835944515,0.06123527443138,0.0873638493505795));
#14068=CARTESIAN_POINT('Ctrl Pts',(0.11294246854291,0.10526951754912,0.0900112387248395));
#14069=CARTESIAN_POINT('Ctrl Pts',(0.0686969739679828,0.138269104834938,
0.0926586280990997));
#14070=CARTESIAN_POINT('Ctrl Pts',(0.0207181735233275,0.145118849380084,
0.0953060174733597));
#14071=CARTESIAN_POINT('Ctrl Pts',(-0.027260626921328,0.151968593925229,
0.0979534068476197));
#14072=CARTESIAN_POINT('Ctrl Pts',(-0.0789727332357116,0.132668495729702,
0.10060079622188));
#14073=CARTESIAN_POINT('Ctrl Pts',(-0.110731403441959,0.0960588230543748,
0.10324818559614));
#14074=CARTESIAN_POINT('Ctrl Pts',(-0.133469481440122,0.0698475998711364,
0.105143622202663));
#14075=CARTESIAN_POINT('Ctrl Pts',(-0.145979327216774,0.0347634013028336,
0.107039058809187));
#14076=CARTESIAN_POINT('Ctrl Pts',(-0.146276374479508,-0.000129480650117819,
0.10893449541571));
#14077=CARTESIAN_POINT('Origin',(0.,0.,0.));
#14078=CARTESIAN_POINT('',(-0.146589818999335,-3.81787486967988E-6,0.166065504584291));
#14079=CARTESIAN_POINT('',(-0.146589453522336,1.04004190909306E-5,0.15893449541571));
#14080=CARTESIAN_POINT('',(-0.14635,-1.79227059055215E-17,0.));
#14081=CARTESIAN_POINT('Ctrl Pts',(-0.146589818999335,-3.81787486967988E-6,
0.166065504584291));
#14082=CARTESIAN_POINT('Ctrl Pts',(-0.146571339149733,0.0482382848470949,
0.163430332415738));
#14083=CARTESIAN_POINT('Ctrl Pts',(-0.120433071521034,0.0964975486977609,
0.160795160247185));
#14084=CARTESIAN_POINT('Ctrl Pts',(-0.0800107885095625,0.122828684230981,
0.158159988078632));
#14085=CARTESIAN_POINT('Ctrl Pts',(-0.0394173515450545,0.149271309704865,
0.15551365819953));
#14086=CARTESIAN_POINT('Ctrl Pts',(0.0155813181737399,0.153599719825856,
0.152867328320428));
#14087=CARTESIAN_POINT('Ctrl Pts',(0.0598114643267532,0.133832733731537,
0.150220998441327));
#14088=CARTESIAN_POINT('Ctrl Pts',(0.104041610479766,0.114065747637217,
0.147574668562225));
#14089=CARTESIAN_POINT('Ctrl Pts',(0.137503233066998,0.0702033653275883,
0.144928338683123));
#14090=CARTESIAN_POINT('Ctrl Pts',(0.144880420813362,0.0223220882221681,
0.142282008804021));
#14091=CARTESIAN_POINT('Ctrl Pts',(0.152257608559726,-0.0255591888832524,
0.139635678924919));
#14092=CARTESIAN_POINT('Ctrl Pts',(0.133550361465222,-0.077459360784464,
0.136989349045817));
#14093=CARTESIAN_POINT('Ctrl Pts',(0.0973212811704284,-0.109622900294719,
0.134343019166715));
#14094=CARTESIAN_POINT('Ctrl Pts',(0.0610922008756344,-0.141786439804975,
0.131696689287613));
#14095=CARTESIAN_POINT('Ctrl Pts',(0.00734128738055008,-0.154213346924274,
0.129050359408511));
#14096=CARTESIAN_POINT('Ctrl Pts',(-0.0393288211819405,-0.141215634503184,
0.126404029529409));
#14097=CARTESIAN_POINT('Ctrl Pts',(-0.0859989297444312,-0.128217922082094,
0.123757699650308));
#14098=CARTESIAN_POINT('Ctrl Pts',(-0.125588233374328,-0.0897955901206149,
0.121111369771206));
#14099=CARTESIAN_POINT('Ctrl Pts',(-0.139976083766172,-0.043535137330043,
0.118465039892104));
#14100=CARTESIAN_POINT('Ctrl Pts',(-0.144324767489921,-0.0295530571287048,
0.117665194789499));
#14101=CARTESIAN_POINT('Ctrl Pts',(-0.146371217526823,-0.0148549394177889,
0.116865349686895));
#14102=CARTESIAN_POINT('Ctrl Pts',(-0.146252097264499,-0.000124487410312429,
0.116065504584291));
#14103=CARTESIAN_POINT('Ctrl Pts',(-0.146276374479508,-0.000129480650117819,
0.10893449541571));
#14104=CARTESIAN_POINT('Ctrl Pts',(-0.14639421831063,-0.0139720956278579,
0.109686448183447));
#14105=CARTESIAN_POINT('Ctrl Pts',(-0.14458995413065,-0.0277846002915201,
0.110438400951183));
#14106=CARTESIAN_POINT('Ctrl Pts',(-0.140739671041232,-0.041001045008257,
0.11119035371892));
#14107=CARTESIAN_POINT('Ctrl Pts',(-0.127184034336146,-0.0875319932404337,
0.11383774309318));
#14108=CARTESIAN_POINT('Ctrl Pts',(-0.0882675268278623,-0.12667464254966,
0.11648513246744));
#14109=CARTESIAN_POINT('Ctrl Pts',(-0.0418159243469935,-0.140499695546946,
0.1191325218417));
#14110=CARTESIAN_POINT('Ctrl Pts',(0.00463567813387508,-0.154324748544231,
0.12177991121596));
#14111=CARTESIAN_POINT('Ctrl Pts',(0.0586223755873289,-0.142832205229577,
0.12442730059022));
#14112=CARTESIAN_POINT('Ctrl Pts',(0.0954154960694136,-0.111286216216264,
0.12707468996448));
#14113=CARTESIAN_POINT('Ctrl Pts',(0.132208616551499,-0.0797402272029501,
0.12972207933874));
#14114=CARTESIAN_POINT('Ctrl Pts',(0.151808160062214,-0.0281407924909768,
0.132369468712999));
#14115=CARTESIAN_POINT('Ctrl Pts',(0.145236524363737,0.0198768833792122,
0.135016858087259));
#14116=CARTESIAN_POINT('Ctrl Pts',(0.138664888665259,0.0678945592494009,
0.13766424746152));
#14117=CARTESIAN_POINT('Ctrl Pts',(0.105922073757589,0.112330476277805,
0.14031163683578));
#14118=CARTESIAN_POINT('Ctrl Pts',(0.062005973158836,0.132830708741579,
0.14295902621004));
#14119=CARTESIAN_POINT('Ctrl Pts',(0.0180898725600832,0.153330941205352,
0.1456064155843));
#14120=CARTESIAN_POINT('Ctrl Pts',(-0.0369995137297515,0.149895489104495,
0.14825380495856));
#14121=CARTESIAN_POINT('Ctrl Pts',(-0.0780284182758478,0.124097962381086,
0.15090119433282));
#14122=CARTESIAN_POINT('Ctrl Pts',(-0.119057322821944,0.0983004356576776,
0.153548583707079));
#14123=CARTESIAN_POINT('Ctrl Pts',(-0.146025745624302,0.0501408343117172,
0.15619597308134));
#14124=CARTESIAN_POINT('Ctrl Pts',(-0.14658076309025,0.00167873146180186,
0.1588433624556));
#14125=CARTESIAN_POINT('Ctrl Pts',(-0.146587131676737,0.00112264969450139,
0.15887374010897));
#14126=CARTESIAN_POINT('Ctrl Pts',(-0.146590022522527,0.000566528098114988,
0.15890411776234));
#14127=CARTESIAN_POINT('Ctrl Pts',(-0.146589453522336,1.04004190909306E-5,
0.15893449541571));
#14128=CARTESIAN_POINT('Origin',(0.,0.,0.));
#14129=CARTESIAN_POINT('',(-0.146263250741535,0.000126870157254357,0.21606550458429));
#14130=CARTESIAN_POINT('',(-0.146245769975643,0.000123264779366826,0.20893449541571));
#14131=CARTESIAN_POINT('',(-0.14635,-1.79227059055215E-17,0.));
#14132=CARTESIAN_POINT('Ctrl Pts',(-0.146263250741535,0.000126870157254357,
0.21606550458429));
#14133=CARTESIAN_POINT('Ctrl Pts',(-0.146381923100139,0.0144435832128767,
0.215287974902784));
#14134=CARTESIAN_POINT('Ctrl Pts',(-0.144450237714319,0.0287289633064517,
0.214510445221278));
#14135=CARTESIAN_POINT('Ctrl Pts',(-0.140337374518256,0.0423560295890773,
0.213732915539772));
#14136=CARTESIAN_POINT('Ctrl Pts',(-0.126339204386259,0.0887358830222778,
0.21108658566067));
#14137=CARTESIAN_POINT('Ctrl Pts',(-0.0870745347363382,0.127489909020004,
0.208440255781569));
#14138=CARTESIAN_POINT('Ctrl Pts',(-0.0405154226099946,0.140879780169064,
0.205793925902467));
#14139=CARTESIAN_POINT('Ctrl Pts',(0.00604368951634975,0.154269651318124,
0.203147596023365));
#14140=CARTESIAN_POINT('Ctrl Pts',(0.0598972441191175,0.142295367618517,
0.200501266144263));
#14141=CARTESIAN_POINT('Ctrl Pts',(0.0963956219934077,0.110437747119808,
0.197854936265161));
#14142=CARTESIAN_POINT('Ctrl Pts',(0.132893999867697,0.0785801266211,0.195208606386059));
#14143=CARTESIAN_POINT('Ctrl Pts',(0.15203720101351,0.0268391693232909,
0.192562276506957));
#14144=CARTESIAN_POINT('Ctrl Pts',(0.145063081087281,-0.0211024746124516,
0.189915946627855));
#14145=CARTESIAN_POINT('Ctrl Pts',(0.138088961161051,-0.0690441185481943,
0.187269616748753));
#14146=CARTESIAN_POINT('Ctrl Pts',(0.10499752016278,-0.11318644912187,0.184623286869651));
#14147=CARTESIAN_POINT('Ctrl Pts',(0.060935231264163,-0.133324827106958,
0.181976956990549));
#14148=CARTESIAN_POINT('Ctrl Pts',(0.0168729423655461,-0.153463205092045,
0.179330627111448));
#14149=CARTESIAN_POINT('Ctrl Pts',(-0.0381601944334158,-0.149597630488544,
0.176684297232346));
#14150=CARTESIAN_POINT('Ctrl Pts',(-0.0789746466099193,-0.123497437688695,
0.174037967353244));
#14151=CARTESIAN_POINT('Ctrl Pts',(-0.119961184605052,-0.0972871987457574,
0.171380479763593));
#14152=CARTESIAN_POINT('Ctrl Pts',(-0.146608455341797,-0.0486544490602708,
0.168722992173942));
#14153=CARTESIAN_POINT('Ctrl Pts',(-0.146589818999335,-3.81787486967988E-6,
0.166065504584291));
#14154=CARTESIAN_POINT('Ctrl Pts',(-0.146589453522336,1.04004190909306E-5,
0.15893449541571));
#14155=CARTESIAN_POINT('Ctrl Pts',(-0.146540434588914,-0.0478995759235739,
0.1615515071366));
#14156=CARTESIAN_POINT('Ctrl Pts',(-0.120813506558866,-0.0958546957256878,
0.16416851885749));
#14157=CARTESIAN_POINT('Ctrl Pts',(-0.0808500697395765,-0.122278388912248,
0.16678553057838));
#14158=CARTESIAN_POINT('Ctrl Pts',(-0.0404227467934142,-0.149008802082514,
0.16943291995264));
#14159=CARTESIAN_POINT('Ctrl Pts',(0.0145735112284506,-0.153705024069172,
0.1720803093269));
#14160=CARTESIAN_POINT('Ctrl Pts',(0.0589475933459444,-0.134215943447351,
0.17472769870116));
#14161=CARTESIAN_POINT('Ctrl Pts',(0.103321675463438,-0.11472686282553,
0.17737508807542));
#14162=CARTESIAN_POINT('Ctrl Pts',(0.137073581676561,-0.0710524795952304,
0.18002247744968));
#14163=CARTESIAN_POINT('Ctrl Pts',(0.144743205110219,-0.0231979049720499,
0.18266986682394));
#14164=CARTESIAN_POINT('Ctrl Pts',(0.152412828543877,0.024656669651131,
0.1853172561982));
#14165=CARTESIAN_POINT('Ctrl Pts',(0.13400016919807,0.0766914356671922,
0.18796464557246));
#14166=CARTESIAN_POINT('Ctrl Pts',(0.0979391709064228,0.109071797518936,
0.19061203494672));
#14167=CARTESIAN_POINT('Ctrl Pts',(0.0618781726147763,0.141452159370678,
0.19325942432098));
#14168=CARTESIAN_POINT('Ctrl Pts',(0.00816883537729064,0.154178117058104,
0.195906813695239));
#14169=CARTESIAN_POINT('Ctrl Pts',(-0.0385872054932313,0.1414205281901,
0.198554203069499));
#14170=CARTESIAN_POINT('Ctrl Pts',(-0.0853432463637543,0.128662939322095,
0.201201592443759));
#14171=CARTESIAN_POINT('Ctrl Pts',(-0.125145990867313,0.0904218038986596,
0.20384898181802));
#14172=CARTESIAN_POINT('Ctrl Pts',(-0.139763737461459,0.0442135263146365,
0.20649637119228));
#14173=CARTESIAN_POINT('Ctrl Pts',(-0.144251162244238,0.030028291356252,
0.207309079266757));
#14174=CARTESIAN_POINT('Ctrl Pts',(-0.146365162502875,0.0150922359825044,
0.208121787341234));
#14175=CARTESIAN_POINT('Ctrl Pts',(-0.146245769975643,0.000123264779366826,
0.20893449541571));
#14176=CARTESIAN_POINT('Origin',(0.,0.,0.));
#14177=CARTESIAN_POINT('',(-0.146142672279203,-7.01165389862951E-5,0.266065504584291));
#14178=CARTESIAN_POINT('',(-0.146150215784492,-7.74481165901552E-5,0.258934495415711));
#14179=CARTESIAN_POINT('',(-0.14635,-1.79227059055215E-17,0.));
#14180=CARTESIAN_POINT('Ctrl Pts',(-0.146142672279203,-7.01165389862951E-5,
0.266065504584291));
#14181=CARTESIAN_POINT('Ctrl Pts',(-0.146017527260215,0.028828671850369,
0.264499287510729));
#14182=CARTESIAN_POINT('Ctrl Pts',(-0.137733916992107,0.0577936173630845,
0.262933070437168));
#14183=CARTESIAN_POINT('Ctrl Pts',(-0.121770841384076,0.0816117278206753,
0.261366853363607));
#14184=CARTESIAN_POINT('Ctrl Pts',(-0.0947991242083451,0.121855560193383,
0.258720523484505));
#14185=CARTESIAN_POINT('Ctrl Pts',(-0.0459036471244643,0.147405924851771,
0.256074193605403));
#14186=CARTESIAN_POINT('Ctrl Pts',(0.0025353607453442,0.146568017913755,
0.253427863726301));
#14187=CARTESIAN_POINT('Ctrl Pts',(0.050974368615152,0.145730110975738,
0.250781533847199));
#14188=CARTESIAN_POINT('Ctrl Pts',(0.0989569072708876,0.118503932441319,
0.248135203968097));
#14189=CARTESIAN_POINT('Ctrl Pts',(0.124520613871998,0.0773513325689396,
0.245488874088995));
#14190=CARTESIAN_POINT('Ctrl Pts',(0.150084320473109,0.0361987326965595,
0.242842544209893));
#14191=CARTESIAN_POINT('Ctrl Pts',(0.153229195019594,-0.0188802885137813,
0.240196214330791));
#14192=CARTESIAN_POINT('Ctrl Pts',(0.132515778953886,-0.0626751965094481,
0.237549884451689));
#14193=CARTESIAN_POINT('Ctrl Pts',(0.111802362888177,-0.106470104505115,
0.234903554572587));
#14194=CARTESIAN_POINT('Ctrl Pts',(0.0672306562102751,-0.138980899286108,
0.232257224693486));
#14195=CARTESIAN_POINT('Ctrl Pts',(0.0192018303028616,-0.145326878595667,
0.229610894814384));
#14196=CARTESIAN_POINT('Ctrl Pts',(-0.0288269956045516,-0.151672857905225,
0.226964564935282));
#14197=CARTESIAN_POINT('Ctrl Pts',(-0.0803129407414762,-0.131854021743351,
0.22431823505618));
#14198=CARTESIAN_POINT('Ctrl Pts',(-0.111690078002902,-0.0949417632280756,
0.221671905177078));
#14199=CARTESIAN_POINT('Ctrl Pts',(-0.133848162215005,-0.0688748557907962,
0.219803104979482));
#14200=CARTESIAN_POINT('Ctrl Pts',(-0.145978020566425,-0.0342834897603843,
0.217934304781886));
#14201=CARTESIAN_POINT('Ctrl Pts',(-0.146263250741535,0.000126870157254357,
0.21606550458429));
#14202=CARTESIAN_POINT('Ctrl Pts',(-0.146245769975643,0.000123264779366826,
0.20893449541571));
#14203=CARTESIAN_POINT('Ctrl Pts',(-0.145976242399967,-0.03366905549635,
0.210769176715493));
#14204=CARTESIAN_POINT('Ctrl Pts',(-0.134324750276972,-0.067629123606452,
0.212603858015276));
#14205=CARTESIAN_POINT('Ctrl Pts',(-0.112902327433,-0.0934976078712483,
0.214438539315059));
#14206=CARTESIAN_POINT('Ctrl Pts',(-0.0819904221256615,-0.130825044728502,
0.217085928689319));
#14207=CARTESIAN_POINT('Ctrl Pts',(-0.0307338628262512,-0.151304498698398,
0.21973331806358));
#14208=CARTESIAN_POINT('Ctrl Pts',(0.0173892134168267,-0.145555327884408,
0.22238070743784));
#14209=CARTESIAN_POINT('Ctrl Pts',(0.0655122896599044,-0.139806157070418,
0.2250280968121));
#14210=CARTESIAN_POINT('Ctrl Pts',(0.11050188284665,-0.107828361472542,
0.22767548618636));
#14211=CARTESIAN_POINT('Ctrl Pts',(0.131750448317205,-0.0642694140823833,
0.23032287556062));
#14212=CARTESIAN_POINT('Ctrl Pts',(0.15299901378776,-0.020710466692225,
0.232970264934879));
#14213=CARTESIAN_POINT('Ctrl Pts',(0.150506551542124,0.0344296324902152,
0.23561765430914));
#14214=CARTESIAN_POINT('Ctrl Pts',(0.125414737320077,0.0758938856636754,
0.2382650436834));
#14215=CARTESIAN_POINT('Ctrl Pts',(0.10032292309803,0.117358138837136,0.24091243305766));
#14216=CARTESIAN_POINT('Ctrl Pts',(0.0526317568995709,0.145146546001616,
0.24355982243192));
#14217=CARTESIAN_POINT('Ctrl Pts',(0.00418624259284972,0.146530589268381,
0.24620721180618));
#14218=CARTESIAN_POINT('Ctrl Pts',(-0.0442592717138715,0.147914632535146,
0.24885460118044));
#14219=CARTESIAN_POINT('Ctrl Pts',(-0.0934591341288551,0.122894311904195,
0.2515019905547));
#14220=CARTESIAN_POINT('Ctrl Pts',(-0.120877280418781,0.082930219442967,
0.25414937992896));
#14221=CARTESIAN_POINT('Ctrl Pts',(-0.137396572682769,0.0588520590724165,
0.255744418424543));
#14222=CARTESIAN_POINT('Ctrl Pts',(-0.146009100715185,0.0293493086505574,
0.257339456920127));
#14223=CARTESIAN_POINT('Ctrl Pts',(-0.146150215784492,-7.74481165901552E-5,
0.258934495415711));
#14224=CARTESIAN_POINT('Origin',(0.,0.,0.));
#14225=CARTESIAN_POINT('',(-0.146519404976022,-8.97763884284003E-5,0.316065504584291));
#14226=CARTESIAN_POINT('',(-0.146528765763263,-8.45393868379275E-5,0.30893449541571));
#14227=CARTESIAN_POINT('',(-0.14635,-1.79227059055215E-17,0.));
#14228=CARTESIAN_POINT('Ctrl Pts',(-0.146519404976022,-8.97763884284003E-5,
0.316065504584291));
#14229=CARTESIAN_POINT('Ctrl Pts',(-0.146208092107557,0.043076445171776,
0.313710600118674));
#14230=CARTESIAN_POINT('Ctrl Pts',(-0.125958424314353,0.0864965766126209,
0.311355695653057));
#14231=CARTESIAN_POINT('Ctrl Pts',(-0.0925183485457987,0.1137056160074,
0.309000791187441));
#14232=CARTESIAN_POINT('Ctrl Pts',(-0.0549399784004991,0.144281843189175,
0.306354461308339));
#14233=CARTESIAN_POINT('Ctrl Pts',(-0.00070450021881692,0.154386382754941,
0.303708131429237));
#14234=CARTESIAN_POINT('Ctrl Pts',(0.0453636543616171,0.139394227973128,
0.301061801550135));
#14235=CARTESIAN_POINT('Ctrl Pts',(0.0914318089420511,0.124402073191315,
0.298415471671033));
#14236=CARTESIAN_POINT('Ctrl Pts',(0.129332639921237,0.0843132240619223,
0.295769141791931));
#14237=CARTESIAN_POINT('Ctrl Pts',(0.141718340675246,0.0374769775398043,
0.293122811912829));
#14238=CARTESIAN_POINT('Ctrl Pts',(0.154104041429255,-0.00935926898231351,
0.290476482033727));
#14239=CARTESIAN_POINT('Ctrl Pts',(0.140974611958088,-0.0629429128971569,
0.287830152154626));
#14240=CARTESIAN_POINT('Ctrl Pts',(0.108339598692885,-0.0987478773661917,
0.285183822275524));
#14241=CARTESIAN_POINT('Ctrl Pts',(0.0757045854276824,-0.134552841835227,
0.282537492396422));
#14242=CARTESIAN_POINT('Ctrl Pts',(0.0235639883684441,-0.152579126858453,
0.27989116251732));
#14243=CARTESIAN_POINT('Ctrl Pts',(-0.0242166208952047,-0.144575818177467,
0.277244832638218));
#14244=CARTESIAN_POINT('Ctrl Pts',(-0.0719972301588528,-0.136572509496481,
0.274598502759116));
#14245=CARTESIAN_POINT('Ctrl Pts',(-0.115417851626912,-0.102539607111283,
0.271952172880014));
#14246=CARTESIAN_POINT('Ctrl Pts',(-0.13460418372715,-0.0580545058751705,
0.269305843000912));
#14247=CARTESIAN_POINT('Ctrl Pts',(-0.142435181350113,-0.0398976888130428,
0.268225730195372));
#14248=CARTESIAN_POINT('Ctrl Pts',(-0.146228976240411,-0.0199996345674016,
0.267145617389831));
#14249=CARTESIAN_POINT('Ctrl Pts',(-0.146142672279203,-7.01165389862951E-5,
0.266065504584291));
#14250=CARTESIAN_POINT('Ctrl Pts',(-0.146150215784492,-7.74481165901552E-5,
0.258934495415711));
#14251=CARTESIAN_POINT('Ctrl Pts',(-0.146243318595233,-0.0194921979337541,
0.259986846294387));
#14252=CARTESIAN_POINT('Ctrl Pts',(-0.142648899141753,-0.0388738684647463,
0.261039197173063));
#14253=CARTESIAN_POINT('Ctrl Pts',(-0.135204796371803,-0.0566427511368837,
0.26209154805174));
#14254=CARTESIAN_POINT('Ctrl Pts',(-0.116477735870028,-0.101343764964001,
0.264738937426));
#14255=CARTESIAN_POINT('Ctrl Pts',(-0.0733871847016099,-0.135837928326728,
0.26738632680026));
#14256=CARTESIAN_POINT('Ctrl Pts',(-0.0256708287318585,-0.144325142544676,
0.27003371617452));
#14257=CARTESIAN_POINT('Ctrl Pts',(0.0220455272378925,-0.152812356762624,
0.27268110554878));
#14258=CARTESIAN_POINT('Ctrl Pts',(0.0743876880089763,-0.135292621835792,
0.27532849492304));
#14259=CARTESIAN_POINT('Ctrl Pts',(0.10738025529095,-0.0997908762961729,
0.2779758842973));
#14260=CARTESIAN_POINT('Ctrl Pts',(0.140372822572925,-0.0642891307565533,
0.280623273671559));
#14261=CARTESIAN_POINT('Ctrl Pts',(0.154015796365789,-0.010805374604146,
0.283270663045819));
#14262=CARTESIAN_POINT('Ctrl Pts',(0.142059993874458,0.0361620845457957,
0.285918052420079));
#14263=CARTESIAN_POINT('Ctrl Pts',(0.130104191383128,0.0831295436957373,
0.288565441794339));
#14264=CARTESIAN_POINT('Ctrl Pts',(0.0925496126076039,0.123580705843213,
0.291212831168599));
#14265=CARTESIAN_POINT('Ctrl Pts',(0.0465981836912963,0.138986860871753,
0.29386022054286));
#14266=CARTESIAN_POINT('Ctrl Pts',(0.000646754774988913,0.154393015900293,
0.296507609917119));
#14267=CARTESIAN_POINT('Ctrl Pts',(-0.0537015242821025,0.144754163809898,
0.29915499929138));
#14268=CARTESIAN_POINT('Ctrl Pts',(-0.0915523499663989,0.114485393976436,
0.30180238866564));
#14269=CARTESIAN_POINT('Ctrl Pts',(-0.125542580994678,0.0873038870745135,
0.30417975758233));
#14270=CARTESIAN_POINT('Ctrl Pts',(-0.146229051243382,0.0434861464246214,
0.30655712649902));
#14271=CARTESIAN_POINT('Ctrl Pts',(-0.146528765763263,-8.45393868379275E-5,
0.30893449541571));
#14272=CARTESIAN_POINT('Origin',(0.,0.,0.));
#14273=CARTESIAN_POINT('',(-0.146416087288192,0.000126442170093593,0.366065504584291));
#14274=CARTESIAN_POINT('',(-0.146408012399712,0.000128195943346294,0.358934495415711));
#14275=CARTESIAN_POINT('',(-0.14635,-1.79227059055215E-17,0.));
#14276=CARTESIAN_POINT('Ctrl Pts',(-0.146416087288192,0.000126442170093593,
0.366065504584291));
#14277=CARTESIAN_POINT('Ctrl Pts',(-0.146499294961499,0.00925816812376314,
0.365568242605721));
#14278=CARTESIAN_POINT('Ctrl Pts',(-0.145718277739785,0.0183757049974218,
0.365070980627151));
#14279=CARTESIAN_POINT('Ctrl Pts',(-0.144021710151773,0.0273195705351122,
0.364573718648581));
#14280=CARTESIAN_POINT('Ctrl Pts',(-0.134992913071845,0.0749170536065741,
0.361927388769479));
#14281=CARTESIAN_POINT('Ctrl Pts',(-0.100034284522917,0.117595890322328,
0.359281058890377));
#14282=CARTESIAN_POINT('Ctrl Pts',(-0.0551469387876206,0.135821305661589,
0.356634729011275));
#14283=CARTESIAN_POINT('Ctrl Pts',(-0.0102595930523245,0.15404672100085,
0.353988399132173));
#14284=CARTESIAN_POINT('Ctrl Pts',(0.0445564698693406,0.147818714963618,
0.351342069253072));
#14285=CARTESIAN_POINT('Ctrl Pts',(0.0842110755700531,0.119987943896873,
0.34869573937397));
#14286=CARTESIAN_POINT('Ctrl Pts',(0.123865681270766,0.0921571728301272,
0.346049409494868));
#14287=CARTESIAN_POINT('Ctrl Pts',(0.148358829750526,0.0427236367338667,
0.343403079615766));
#14288=CARTESIAN_POINT('Ctrl Pts',(0.146479621605269,-0.00568615719458776,
0.340756749736664));
#14289=CARTESIAN_POINT('Ctrl Pts',(0.144600413460012,-0.0540959511230416,
0.338110419857562));
#14290=CARTESIAN_POINT('Ctrl Pts',(0.116348848689739,-0.101482002883689,
0.33546408997846));
#14291=CARTESIAN_POINT('Ctrl Pts',(0.0746561129649502,-0.126154971072205,
0.332817760099358));
#14292=CARTESIAN_POINT('Ctrl Pts',(0.0329633772401616,-0.150827939260721,
0.330171430220256));
#14293=CARTESIAN_POINT('Ctrl Pts',(-0.0221705294391424,-0.152787823877104,
0.327525100341154));
#14294=CARTESIAN_POINT('Ctrl Pts',(-0.0655099505772086,-0.131137554898038,
0.324878770462052));
#14295=CARTESIAN_POINT('Ctrl Pts',(-0.108849371715275,-0.109487285918972,
0.322232440582951));
#14296=CARTESIAN_POINT('Ctrl Pts',(-0.140394307312104,-0.0642268633444555,
0.319586110703849));
#14297=CARTESIAN_POINT('Ctrl Pts',(-0.14570614405606,-0.0160726946583056,
0.316939780824747));
#14298=CARTESIAN_POINT('Ctrl Pts',(-0.146291106736525,-0.0107697471190636,
0.316648355411261));
#14299=CARTESIAN_POINT('Ctrl Pts',(-0.146557930734812,-0.0054317060295066,
0.316356929997776));
#14300=CARTESIAN_POINT('Ctrl Pts',(-0.146519404976022,-8.97763884284003E-5,
0.316065504584291));
#14301=CARTESIAN_POINT('Ctrl Pts',(-0.146528765763263,-8.45393868379275E-5,
0.30893449541571));
#14302=CARTESIAN_POINT('Ctrl Pts',(-0.146562807199252,-0.00503327764821679,
0.30920451587328));
#14303=CARTESIAN_POINT('Ctrl Pts',(-0.14633385314783,-0.00997882882536714,
0.30947453633085));
#14304=CARTESIAN_POINT('Ctrl Pts',(-0.145831525524598,-0.0148964553326841,
0.309744556788419));
#14305=CARTESIAN_POINT('Ctrl Pts',(-0.140906503086998,-0.0631108472318147,
0.312391946162679));
#14306=CARTESIAN_POINT('Ctrl Pts',(-0.109703085900295,-0.108640943453547,
0.31503933553694));
#14307=CARTESIAN_POINT('Ctrl Pts',(-0.0665140418604196,-0.13063162118607,
0.3176867249112));
#14308=CARTESIAN_POINT('Ctrl Pts',(-0.0233249978205455,-0.152622298918592,
0.32033411428546));
#14309=CARTESIAN_POINT('Ctrl Pts',(0.0318496730725009,-0.151073558161906,
0.322981503659719));
#14310=CARTESIAN_POINT('Ctrl Pts',(0.0737371373950496,-0.126694801736668,
0.325628893033979));
#14311=CARTESIAN_POINT('Ctrl Pts',(0.115624601717599,-0.10231604531143,
0.328276282408239));
#14312=CARTESIAN_POINT('Ctrl Pts',(0.144224859469651,-0.0551072732176397,
0.3309236717825));
#14313=CARTESIAN_POINT('Ctrl Pts',(0.146437523492708,-0.0066925280449658,
0.33357106115676));
#14314=CARTESIAN_POINT('Ctrl Pts',(0.148650187515766,0.0417222171277085,
0.33621845053102));
#14315=CARTESIAN_POINT('Ctrl Pts',(0.124475257809829,0.0913429353792657,
0.33886583990528));
#14316=CARTESIAN_POINT('Ctrl Pts',(0.0849860939726622,0.119440788885456,
0.34151322927954));
#14317=CARTESIAN_POINT('Ctrl Pts',(0.0454969301354961,0.147538642391646,
0.344160618653799));
#14318=CARTESIAN_POINT('Ctrl Pts',(-0.00930646783289898,0.154113631152469,
0.346808008028059));
#14319=CARTESIAN_POINT('Ctrl Pts',(-0.0543213285795041,0.136154072578339,
0.349455397402319));
#14320=CARTESIAN_POINT('Ctrl Pts',(-0.0993361893261098,0.11819451400421,
0.352102786776579));
#14321=CARTESIAN_POINT('Ctrl Pts',(-0.134562512850926,0.0757004080951257,
0.35475017615084));
#14322=CARTESIAN_POINT('Ctrl Pts',(-0.143864833510727,0.0281362381501331,
0.3573975655251));
#14323=CARTESIAN_POINT('Ctrl Pts',(-0.145664973529558,0.0189318504589563,
0.357909875488637));
#14324=CARTESIAN_POINT('Ctrl Pts',(-0.146494308508217,0.00953759842677947,
0.358422185452174));
#14325=CARTESIAN_POINT('Ctrl Pts',(-0.146408012399712,0.000128195943346294,
0.358934495415711));
#14326=CARTESIAN_POINT('Origin',(0.,0.,0.));
#14327=CARTESIAN_POINT('',(-0.146110491840834,1.12683595067248E-5,0.416065504584291));
#14328=CARTESIAN_POINT('',(-0.146109756335714,8.81622270207575E-6,0.40893449541571));
#14329=CARTESIAN_POINT('',(-0.14635,-1.79227059055215E-17,0.));
#14330=CARTESIAN_POINT('Ctrl Pts',(-0.146110491840834,1.12683595067248E-5,
0.416065504584291));
#14331=CARTESIAN_POINT('Ctrl Pts',(-0.146126798292857,0.0237518011834032,
0.414779555213666));
#14332=CARTESIAN_POINT('Ctrl Pts',(-0.140669750958991,0.0474852665485293,
0.413493605843041));
#14333=CARTESIAN_POINT('Ctrl Pts',(-0.129698698951591,0.0683144158983218,
0.412207656472415));
#14334=CARTESIAN_POINT('Ctrl Pts',(-0.107121587134001,0.111178312051432,
0.409561326593314));
#14335=CARTESIAN_POINT('Ctrl Pts',(-0.0611933749717542,0.141742803557285,
0.406914996714211));
#14336=CARTESIAN_POINT('Ctrl Pts',(-0.0129361277491455,0.146018041789781,
0.40426866683511));
#14337=CARTESIAN_POINT('Ctrl Pts',(0.0353211194734639,0.150293280022276,
0.401622336956008));
#14338=CARTESIAN_POINT('Ctrl Pts',(0.0859074017564354,0.128279264981412,
0.398976007076906));
#14339=CARTESIAN_POINT('Ctrl Pts',(0.115668581836909,0.0900521576926538,
0.396329677197804));
#14340=CARTESIAN_POINT('Ctrl Pts',(0.145429761917382,0.0518250504038959,
0.393683347318702));
#14341=CARTESIAN_POINT('Ctrl Pts',(0.154365839795359,-0.0026151491327561,
0.3910370174396));
#14342=CARTESIAN_POINT('Ctrl Pts',(0.138386632036901,-0.0483503050946702,
0.388390687560498));
#14343=CARTESIAN_POINT('Ctrl Pts',(0.122407424278443,-0.094085461056585,
0.385744357681396));
#14344=CARTESIAN_POINT('Ctrl Pts',(0.0815129308835505,-0.131115573443762,
0.383098027802294));
#14345=CARTESIAN_POINT('Ctrl Pts',(0.0344212048624006,-0.142491377230642,
0.380451697923192));
#14346=CARTESIAN_POINT('Ctrl Pts',(-0.0126705211587486,-0.153867181017521,
0.37780536804409));
#14347=CARTESIAN_POINT('Ctrl Pts',(-0.0659594798061549,-0.139588676204105,
0.375159038164988));
#14348=CARTESIAN_POINT('Ctrl Pts',(-0.101054476324393,-0.106191359083811,
0.372512708285887));
#14349=CARTESIAN_POINT('Ctrl Pts',(-0.129554902927378,-0.0790696072742943,
0.370363640385355));
#14350=CARTESIAN_POINT('Ctrl Pts',(-0.146056480184715,-0.0393390709180539,
0.368214572484823));
#14351=CARTESIAN_POINT('Ctrl Pts',(-0.146416087288192,0.000126442170093593,
0.366065504584291));
#14352=CARTESIAN_POINT('Ctrl Pts',(-0.146408012399712,0.000128195943346294,
0.358934495415711));
#14353=CARTESIAN_POINT('Ctrl Pts',(-0.146048368712081,-0.0390859965171687,
0.361069574826434));
#14354=CARTESIAN_POINT('Ctrl Pts',(-0.1297855810823,-0.0785633296797545,
0.363204654237157));
#14355=CARTESIAN_POINT('Ctrl Pts',(-0.101613371150224,-0.105657280969165,
0.36533973364788));
#14356=CARTESIAN_POINT('Ctrl Pts',(-0.066681270335132,-0.139252396162569,
0.36798712302214));
#14357=CARTESIAN_POINT('Ctrl Pts',(-0.0134387509101597,-0.153808392568477,
0.370634512396399));
#14358=CARTESIAN_POINT('Ctrl Pts',(0.0337263783221333,-0.142657876135818,
0.373281901770659));
#14359=CARTESIAN_POINT('Ctrl Pts',(0.0808915075544263,-0.13150735970316,
0.375929291144919));
#14360=CARTESIAN_POINT('Ctrl Pts',(0.12197924659404,-0.0946503304319347,
0.378576680519179));
#14361=CARTESIAN_POINT('Ctrl Pts',(0.138169300408926,-0.0489692009616054,
0.38122406989344));
#14362=CARTESIAN_POINT('Ctrl Pts',(0.154359354223812,-0.00328807149127619,
0.3838714592677));
#14363=CARTESIAN_POINT('Ctrl Pts',(0.14565172281397,0.0512171581781573,
0.38651884864196));
#14364=CARTESIAN_POINT('Ctrl Pts',(0.11603494864959,0.0895802930905963,
0.38916623801622));
#14365=CARTESIAN_POINT('Ctrl Pts',(0.0864181744852101,0.127943428003035,
0.39181362739048));
#14366=CARTESIAN_POINT('Ctrl Pts',(0.0358922575662923,0.15016446815848,
0.394461016764739));
#14367=CARTESIAN_POINT('Ctrl Pts',(-0.0123993367959677,0.146065035738641,
0.397108406138999));
#14368=CARTESIAN_POINT('Ctrl Pts',(-0.0606909311582276,0.141965603318802,
0.399755795513259));
#14369=CARTESIAN_POINT('Ctrl Pts',(-0.106748202963829,0.111545698323679,
0.40240318488752));
#14370=CARTESIAN_POINT('Ctrl Pts',(-0.129474555904152,0.0687391998188283,
0.40505057426178));
#14371=CARTESIAN_POINT('Ctrl Pts',(-0.140588317483115,0.0478057390183907,
0.406345214646423));
#14372=CARTESIAN_POINT('Ctrl Pts',(-0.146122589096428,0.0239100770892618,
0.407639855031067));
#14373=CARTESIAN_POINT('Ctrl Pts',(-0.146109756335714,8.81622270207575E-6,
0.40893449541571));
#14374=CARTESIAN_POINT('Origin',(0.,0.,0.));
#14375=CARTESIAN_POINT('',(-0.146374718215768,-0.000132229735885947,0.466065504584291));
#14376=CARTESIAN_POINT('',(-0.146375609273197,-0.000132432188538665,0.458934495415711));
#14377=CARTESIAN_POINT('',(-0.14635,-1.79227059055215E-17,0.));
#14378=CARTESIAN_POINT('Ctrl Pts',(-0.146374718215768,-0.000132229735885947,
0.466065504584291));
#14379=CARTESIAN_POINT('Ctrl Pts',(-0.146022504084922,0.0379941335185874,
0.46399086782161));
#14380=CARTESIAN_POINT('Ctrl Pts',(-0.130761950520226,0.0763703265456945,
0.46191623105893));
#14381=CARTESIAN_POINT('Ctrl Pts',(-0.103994021541854,0.103314352404769,
0.45984159429625));
#14382=CARTESIAN_POINT('Ctrl Pts',(-0.0698498419286355,0.137683154682254,
0.457195264417148));
#14383=CARTESIAN_POINT('Ctrl Pts',(-0.0169824611430249,0.153451124186949,
0.454548934538046));
#14384=CARTESIAN_POINT('Ctrl Pts',(0.030409888879481,0.143401013202843,
0.451902604658944));
#14385=CARTESIAN_POINT('Ctrl Pts',(0.0778022389019875,0.133350902218736,
0.449256274779842));
#14386=CARTESIAN_POINT('Ctrl Pts',(0.119719558161389,0.0974827107458278,
0.44660994490074));
#14387=CARTESIAN_POINT('Ctrl Pts',(0.136975630157447,0.0522138743269898,
0.443963615021638));
#14388=CARTESIAN_POINT('Ctrl Pts',(0.154231702153504,0.00694503790815254,
0.441317285142536));
#14389=CARTESIAN_POINT('Ctrl Pts',(0.146826526886218,-0.0477244434566137,
0.438670955263434));
#14390=CARTESIAN_POINT('Ctrl Pts',(0.118149569579287,-0.0867714880447125,
0.436024625384332));
#14391=CARTESIAN_POINT('Ctrl Pts',(0.0894726122723542,-0.125818532632812,
0.43337829550523));
#14392=CARTESIAN_POINT('Ctrl Pts',(0.0395238729257754,-0.149243140444243,
0.430731965626129));
#14393=CARTESIAN_POINT('Ctrl Pts',(-0.00883432462988853,-0.146323499949933,
0.428085635747027));
#14394=CARTESIAN_POINT('Ctrl Pts',(-0.0571925221855517,-0.143403859455623,
0.425439305867925));
#14395=CARTESIAN_POINT('Ctrl Pts',(-0.1039601779503,-0.114139970655572,
0.422792975988823));
#14396=CARTESIAN_POINT('Ctrl Pts',(-0.127731000096207,-0.0719263758553634,
0.420146646109721));
#14397=CARTESIAN_POINT('Ctrl Pts',(-0.139950702323481,-0.0502259249733931,
0.418786265601244));
#14398=CARTESIAN_POINT('Ctrl Pts',(-0.146093241566443,-0.0251033736724598,
0.417425885092767));
#14399=CARTESIAN_POINT('Ctrl Pts',(-0.146110491840834,1.12683595067248E-5,
0.416065504584291));
#14400=CARTESIAN_POINT('Ctrl Pts',(-0.146109756335714,8.81622270207575E-6,
0.40893449541571));
#14401=CARTESIAN_POINT('Ctrl Pts',(-0.146096347589706,-0.0249652282079418,
0.410287244405327));
#14402=CARTESIAN_POINT('Ctrl Pts',(-0.140026707259891,-0.049945385460595,
0.411639993394943));
#14403=CARTESIAN_POINT('Ctrl Pts',(-0.127937780377622,-0.0715588049813403,
0.412992742384559));
#14404=CARTESIAN_POINT('Ctrl Pts',(-0.104279217835726,-0.113857219262079,
0.415640131758819));
#14405=CARTESIAN_POINT('Ctrl Pts',(-0.0575666586768896,-0.14326095580898,
0.41828752113308));
#14406=CARTESIAN_POINT('Ctrl Pts',(-0.00919685447762893,-0.146301592903247,
0.42093491050734));
#14407=CARTESIAN_POINT('Ctrl Pts',(0.039172949721632,-0.149342229997515,
0.4235822998816));
#14408=CARTESIAN_POINT('Ctrl Pts',(0.089199998961318,-0.126019767639148,
0.426229689255859));
#14409=CARTESIAN_POINT('Ctrl Pts',(0.117969334952632,-0.0870170915920772,
0.428877078630119));
#14410=CARTESIAN_POINT('Ctrl Pts',(0.146738670943946,-0.0480144155450057,
0.431524468004379));
#14411=CARTESIAN_POINT('Ctrl Pts',(0.154250293686888,0.00666847419077017,
0.43417185737864));
#14412=CARTESIAN_POINT('Ctrl Pts',(0.137063494116028,0.051984005222912,
0.4368192467529));
#14413=CARTESIAN_POINT('Ctrl Pts',(0.119876694545168,0.0972995362550541,
0.43946663612716));
#14414=CARTESIAN_POINT('Ctrl Pts',(0.0779914726605056,0.133247708583562,
0.442114025501419));
#14415=CARTESIAN_POINT('Ctrl Pts',(0.0305934116013849,0.143362412733947,
0.444761414875679));
#14416=CARTESIAN_POINT('Ctrl Pts',(-0.0168046494577345,0.153477116884331,
0.447408804249939));
#14417=CARTESIAN_POINT('Ctrl Pts',(-0.0697155496913122,0.137758352856595,
0.4500561936242));
#14418=CARTESIAN_POINT('Ctrl Pts',(-0.103903378920715,0.103406122000434,
0.45270358299846));
#14419=CARTESIAN_POINT('Ctrl Pts',(-0.130724942802416,0.0764555792150183,
0.45478055380421));
#14420=CARTESIAN_POINT('Ctrl Pts',(-0.146022533856355,0.0380362146017157,
0.45685752460996));
#14421=CARTESIAN_POINT('Ctrl Pts',(-0.146375609273197,-0.000132432188538665,
0.458934495415711));
#14422=CARTESIAN_POINT('Origin',(0.,0.,0.));
#14423=CARTESIAN_POINT('',(-0.146548608312775,6.99729089778146E-5,0.516065504584291));
#14424=CARTESIAN_POINT('',(-0.146550766805835,6.86360251013434E-5,0.508934495415711));
#14425=CARTESIAN_POINT('',(-0.14635,-1.79227059055215E-17,0.));
#14426=CARTESIAN_POINT('Ctrl Pts',(-0.146548608312775,6.99729089778146E-5,
0.516065504584291));
#14427=CARTESIAN_POINT('Ctrl Pts',(-0.146572081366671,0.00404546554386884,
0.515848510308657));
#14428=CARTESIAN_POINT('Ctrl Pts',(-0.146424333269732,0.00801918670503405,
0.515631516033023));
#14429=CARTESIAN_POINT('Ctrl Pts',(-0.146099725131082,0.0119784074854107,
0.51541452175739));
#14430=CARTESIAN_POINT('Ctrl Pts',(-0.142141002193345,0.06026265009261,
0.512768191878288));
#14431=CARTESIAN_POINT('Ctrl Pts',(-0.111878319621163,0.106390286678145,
0.510121861999186));
#14432=CARTESIAN_POINT('Ctrl Pts',(-0.069163383343408,0.129247972261684,
0.507475532120084));
#14433=CARTESIAN_POINT('Ctrl Pts',(-0.0264484470656534,0.152105657845224,
0.504829202240982));
#14434=CARTESIAN_POINT('Ctrl Pts',(0.0287187429176733,0.151693392426768,
0.50218287236188));
#14435=CARTESIAN_POINT('Ctrl Pts',(0.07108729581893,0.128199876374419,0.499536542482778));
#14436=CARTESIAN_POINT('Ctrl Pts',(0.113455848720186,0.10470636032207,0.496890212603677));
#14437=CARTESIAN_POINT('Ctrl Pts',(0.143025764539373,0.0581315936358261,
0.494243882724575));
#14438=CARTESIAN_POINT('Ctrl Pts',(0.146262427589597,0.00979357977770552,
0.491597552845473));
#14439=CARTESIAN_POINT('Ctrl Pts',(0.149499090639821,-0.0385444340804161,
0.488951222966371));
#14440=CARTESIAN_POINT('Ctrl Pts',(0.126402500921083,-0.0886456951104151,
0.486304893087269));
#14441=CARTESIAN_POINT('Ctrl Pts',(0.087544330920799,-0.117578067907642,
0.483658563208167));
#14442=CARTESIAN_POINT('Ctrl Pts',(0.0486861609205161,-0.146510440704867,
0.481012233329065));
#14443=CARTESIAN_POINT('Ctrl Pts',(-0.00593358936131212,-0.154273925269321,
0.478365903449963));
#14444=CARTESIAN_POINT('Ctrl Pts',(-0.0513146009011563,-0.137315052574797,
0.475719573570861));
#14445=CARTESIAN_POINT('Ctrl Pts',(-0.0966956124410008,-0.120356179880273,
0.473073243691759));
#14446=CARTESIAN_POINT('Ctrl Pts',(-0.132837885238862,-0.078674949926771,
0.470426913812657));
#14447=CARTESIAN_POINT('Ctrl Pts',(-0.14319853241738,-0.0313495174248821,
0.467780583933555));
#14448=CARTESIAN_POINT('Ctrl Pts',(-0.145436768368387,-0.0211256884885646,
0.467208890817134));
#14449=CARTESIAN_POINT('Ctrl Pts',(-0.146471775395962,-0.0106384445195334,
0.466637197700712));
#14450=CARTESIAN_POINT('Ctrl Pts',(-0.146374718215768,-0.000132229735885947,
0.466065504584291));
#14451=CARTESIAN_POINT('Ctrl Pts',(-0.146375609273197,-0.000132432188538665,
0.458934495415711));
#14452=CARTESIAN_POINT('Ctrl Pts',(-0.146472577787773,-0.0106150565970108,
0.45950491398422));
#14453=CARTESIAN_POINT('Ctrl Pts',(-0.145442327125792,-0.021078770125739,
0.46007533255273));
#14454=CARTESIAN_POINT('Ctrl Pts',(-0.143213999951756,-0.0312807998000163,
0.460645751121239));
#14455=CARTESIAN_POINT('Ctrl Pts',(-0.132872033528166,-0.0786297930597184,
0.463293140495499));
#14456=CARTESIAN_POINT('Ctrl Pts',(-0.0967233424557573,-0.120342081894533,
0.465940529869759));
#14457=CARTESIAN_POINT('Ctrl Pts',(-0.0513258840937604,-0.13731129538499,
0.46858791924402));
#14458=CARTESIAN_POINT('Ctrl Pts',(-0.00592842573176499,-0.154280508875447,
0.47123530861828));
#14459=CARTESIAN_POINT('Ctrl Pts',(0.0487177999198187,-0.146506647021548,
0.47388269799254));
#14460=CARTESIAN_POINT('Ctrl Pts',(0.0875820145025328,-0.117550537871965,
0.476530087366799));
#14461=CARTESIAN_POINT('Ctrl Pts',(0.126446229085248,-0.0885944287223814,
0.47917747674106));
#14462=CARTESIAN_POINT('Ctrl Pts',(0.149528432599094,-0.0384560722771122,
0.481824866115319));
#14463=CARTESIAN_POINT('Ctrl Pts',(0.146255790172295,0.0098985887573764,
0.484472255489579));
#14464=CARTESIAN_POINT('Ctrl Pts',(0.142983147745498,0.0582532497918637,
0.487119644863839));
#14465=CARTESIAN_POINT('Ctrl Pts',(0.113355659378058,0.10482421541557,0.4897670342381));
#14466=CARTESIAN_POINT('Ctrl Pts',(0.0709442366160257,0.128279591164298,
0.49241442361236));
#14467=CARTESIAN_POINT('Ctrl Pts',(0.0285328138539934,0.151734966913027,
0.49506181298662));
#14468=CARTESIAN_POINT('Ctrl Pts',(-0.0266625433026316,0.152074752786777,
0.497709202360879));
#14469=CARTESIAN_POINT('Ctrl Pts',(-0.0693595260588707,0.129143309401606,
0.500356591735139));
#14470=CARTESIAN_POINT('Ctrl Pts',(-0.11205650881511,0.106211866016435,
0.503003981109399));
#14471=CARTESIAN_POINT('Ctrl Pts',(-0.142255117170964,0.060009193372344,
0.505651370483659));
#14472=CARTESIAN_POINT('Ctrl Pts',(-0.146122837288996,0.0116984888307781,
0.50829875985792));
#14473=CARTESIAN_POINT('Ctrl Pts',(-0.146432431239741,0.00783142983325791,
0.508510671710517));
#14474=CARTESIAN_POINT('Ctrl Pts',(-0.14657331536999,0.00395086404934249,
0.508722583563114));
#14475=CARTESIAN_POINT('Ctrl Pts',(-0.146550766805835,6.86360251013434E-5,
0.508934495415711));
#14476=CARTESIAN_POINT('Origin',(0.,0.,0.));
#14477=CARTESIAN_POINT('',(-0.146165204287215,8.83645032875094E-5,0.566065504584291));
#14478=CARTESIAN_POINT('',(-0.146168951232552,9.12430751481418E-5,0.558934495415711));
#14479=CARTESIAN_POINT('',(-0.14635,-1.79227059055215E-17,0.));
#14480=CARTESIAN_POINT('Ctrl Pts',(-0.146165204287215,8.83645032875094E-5,
0.566065504584291));
#14481=CARTESIAN_POINT('Ctrl Pts',(-0.146267412293664,0.0186373661349918,
0.565059822916602));
#14482=CARTESIAN_POINT('Ctrl Pts',(-0.142994166834961,0.0371516370495788,
0.564054141248913));
#14483=CARTESIAN_POINT('Ctrl Pts',(-0.136179985035193,0.0542551712289143,
0.563048459581224));
#14484=CARTESIAN_POINT('Ctrl Pts',(-0.118249288396568,0.0992610562830057,
0.560402129702122));
#14485=CARTESIAN_POINT('Ctrl Pts',(-0.0758005933416487,0.134498778989873,
0.55775579982302));
#14486=CARTESIAN_POINT('Ctrl Pts',(-0.0282633354322908,0.143839479279877,
0.555109469943918));
#14487=CARTESIAN_POINT('Ctrl Pts',(0.0192739224770691,0.153180179569881,
0.552463140064816));
#14488=CARTESIAN_POINT('Ctrl Pts',(0.0718997432408687,0.136623857443018,
0.549816810185715));
#14489=CARTESIAN_POINT('Ctrl Pts',(0.105526460745998,0.101748602013432,
0.547170480306613));
#14490=CARTESIAN_POINT('Ctrl Pts',(0.139153178251127,0.0668733465838454,
0.544524150427511));
#14491=CARTESIAN_POINT('Ctrl Pts',(0.153780792497586,0.0136791578515372,
0.541877820548409));
#14492=CARTESIAN_POINT('Ctrl Pts',(0.142714014311998,-0.0334861471092027,
0.539231490669307));
#14493=CARTESIAN_POINT('Ctrl Pts',(0.13164723612641,-0.0806514520699426,
0.536585160790205));
#14494=CARTESIAN_POINT('Ctrl Pts',(0.0948860655087725,-0.121787873259113,
0.533938830911103));
#14495=CARTESIAN_POINT('Ctrl Pts',(0.0492566686055307,-0.138066623508903,
0.531292501032001));
#14496=CARTESIAN_POINT('Ctrl Pts',(0.00362727170228945,-0.154345373758693,
0.528646171152899));
#14497=CARTESIAN_POINT('Ctrl Pts',(-0.050870351486557,-0.145766453069103,
0.525999841273797));
#14498=CARTESIAN_POINT('Ctrl Pts',(-0.089291781429334,-0.116256568409877,
0.523353511394695));
#14499=CARTESIAN_POINT('Ctrl Pts',(-0.124562723435938,-0.0891664410515947,
0.520924175791227));
#14500=CARTESIAN_POINT('Ctrl Pts',(-0.146285818313441,-0.0444372186796531,
0.518494840187759));
#14501=CARTESIAN_POINT('Ctrl Pts',(-0.146548608312775,6.99729089778146E-5,
0.516065504584291));
#14502=CARTESIAN_POINT('Ctrl Pts',(-0.146550766805835,6.86360251013434E-5,
0.508934495415711));
#14503=CARTESIAN_POINT('Ctrl Pts',(-0.146291618860727,-0.0445493453248537,
0.511369972937373));
#14504=CARTESIAN_POINT('Ctrl Pts',(-0.124445252016267,-0.0893868858389474,
0.513805450459036));
#14505=CARTESIAN_POINT('Ctrl Pts',(-0.0890226177929609,-0.116463349340462,
0.516240927980699));
#14506=CARTESIAN_POINT('Ctrl Pts',(-0.0505178462986829,-0.145895746531099,
0.518888317354959));
#14507=CARTESIAN_POINT('Ctrl Pts',(0.00402852857008221,-0.154341804473332,
0.52153570672922));
#14508=CARTESIAN_POINT('Ctrl Pts',(0.0496314652424392,-0.137932794781367,
0.52418309610348));
#14509=CARTESIAN_POINT('Ctrl Pts',(0.0952344019147948,-0.121523785089403,
0.52683048547774));
#14510=CARTESIAN_POINT('Ctrl Pts',(0.131893900390741,-0.0802597077632436,
0.529477874851999));
#14511=CARTESIAN_POINT('Ctrl Pts',(0.14281802728161,-0.0330416298281342,
0.532125264226259));
#14512=CARTESIAN_POINT('Ctrl Pts',(0.153742154172479,0.0141764481069759,
0.53477265360052));
#14513=CARTESIAN_POINT('Ctrl Pts',(0.138930909478268,0.0673485266510362,
0.53742004297478));
#14514=CARTESIAN_POINT('Ctrl Pts',(0.105168604077417,0.102119062543277,
0.54006743234904));
#14515=CARTESIAN_POINT('Ctrl Pts',(0.0714062986765666,0.136889598435517,
0.5427148217233));
#14516=CARTESIAN_POINT('Ctrl Pts',(0.018692932569077,0.153258591675938,
0.545362211097559));
#14517=CARTESIAN_POINT('Ctrl Pts',(-0.0288260648428939,0.143728202535144,
0.548009600471819));
#14518=CARTESIAN_POINT('Ctrl Pts',(-0.0763450622548654,0.13419781339435,
0.550656989846079));
#14519=CARTESIAN_POINT('Ctrl Pts',(-0.118669690971318,0.0987680418723385,
0.55330437922034));
#14520=CARTESIAN_POINT('Ctrl Pts',(-0.136413096952957,0.0536675432455532,
0.5559517685946));
#14521=CARTESIAN_POINT('Ctrl Pts',(-0.143076734904351,0.036729792140314,
0.556946010868304));
#14522=CARTESIAN_POINT('Ctrl Pts',(-0.146273385252938,0.0184280612467595,
0.557940253142007));
#14523=CARTESIAN_POINT('Ctrl Pts',(-0.146168951232552,9.12430751481418E-5,
0.558934495415711));
#14524=CARTESIAN_POINT('Origin',(0.,0.,0.));
#14525=CARTESIAN_POINT('',(-0.146227179098081,-0.000117664897458569,0.616065504584291));
#14526=CARTESIAN_POINT('',(-0.146218520919543,-0.000115076211918358,0.608934495415711));
#14527=CARTESIAN_POINT('',(-0.14635,-1.79227059055215E-17,0.));
#14528=CARTESIAN_POINT('Ctrl Pts',(-0.146227179098081,-0.000117664897458569,
0.616065504584291));
#14529=CARTESIAN_POINT('Ctrl Pts',(-0.145977603365176,0.0329427899635141,
0.614271135524546));
#14530=CARTESIAN_POINT('Ctrl Pts',(-0.134874795495675,0.0661550248562671,
0.612476766464802));
#14531=CARTESIAN_POINT('Ctrl Pts',(-0.114309815624116,0.091770790457776,
0.610682397405058));
#14532=CARTESIAN_POINT('Ctrl Pts',(-0.0839806476072558,0.129548841477563,
0.608036067525956));
#14533=CARTESIAN_POINT('Ctrl Pts',(-0.0330710111925292,0.150804375664025,
0.605389737646855));
#14534=CARTESIAN_POINT('Ctrl Pts',(0.0151169520838501,0.145808400611758,
0.602743407767753));
#14535=CARTESIAN_POINT('Ctrl Pts',(0.0633049153602295,0.140812425559491,
0.600097077888651));
#14536=CARTESIAN_POINT('Ctrl Pts',(0.108771205498262,0.109564941268491,
0.597450748009549));
#14537=CARTESIAN_POINT('Ctrl Pts',(0.130705186191441,0.0663684129079872,
0.594804418130447));
#14538=CARTESIAN_POINT('Ctrl Pts',(0.152639166884621,0.023171884547483,
0.592158088251345));
#14539=CARTESIAN_POINT('Ctrl Pts',(0.151040838132949,-0.0319736878825246,
0.589511758372243));
#14540=CARTESIAN_POINT('Ctrl Pts',(0.126641780152193,-0.0738273082886534,
0.586865428493141));
#14541=CARTESIAN_POINT('Ctrl Pts',(0.102242722171437,-0.115680928694782,
0.584219098614039));
#14542=CARTESIAN_POINT('Ctrl Pts',(0.0550429349615966,-0.14424259707703,
0.581572768734937));
#14543=CARTESIAN_POINT('Ctrl Pts',(0.00664650371163741,-0.14643918846291,
0.578926438855836));
#14544=CARTESIAN_POINT('Ctrl Pts',(-0.0417499275383225,-0.148635779848789,
0.576280108976733));
#14545=CARTESIAN_POINT('Ctrl Pts',(-0.0913430028284016,-0.1244672942383,
0.573633779097631));
#14546=CARTESIAN_POINT('Ctrl Pts',(-0.119433191362276,-0.0849960277323969,
0.570987449218529));
#14547=CARTESIAN_POINT('Ctrl Pts',(-0.136848298201485,-0.0605249807527623,
0.569346801007117));
#14548=CARTESIAN_POINT('Ctrl Pts',(-0.145998464265635,-0.0301720919893573,
0.567706152795704));
#14549=CARTESIAN_POINT('Ctrl Pts',(-0.146165204287215,8.83645032875094E-5,
0.566065504584291));
#14550=CARTESIAN_POINT('Ctrl Pts',(-0.146168951232552,9.12430751481418E-5,
0.558934495415711));
#14551=CARTESIAN_POINT('Ctrl Pts',(-0.145995306636495,-0.0303977620653178,
0.560587642516267));
#14552=CARTESIAN_POINT('Ctrl Pts',(-0.136695352934655,-0.0609837708898569,
0.562240789616823));
#14553=CARTESIAN_POINT('Ctrl Pts',(-0.119031718004195,-0.0855580991331628,
0.563893936717379));
#14554=CARTESIAN_POINT('Ctrl Pts',(-0.090744749826965,-0.124912017153538,
0.566541326091639));
#14555=CARTESIAN_POINT('Ctrl Pts',(-0.0410086302256792,-0.148848627462727,
0.5691887154659));
#14556=CARTESIAN_POINT('Ctrl Pts',(0.00739494322942312,-0.146403732988417,
0.57183610484016));
#14557=CARTESIAN_POINT('Ctrl Pts',(0.0557985166845234,-0.143958838514108,
0.57448349421442));
#14558=CARTESIAN_POINT('Ctrl Pts',(0.10286954399344,-0.1151324392563,0.57713088358868));
#14559=CARTESIAN_POINT('Ctrl Pts',(0.127047076753504,-0.0731285067993286,
0.579778272962939));
#14560=CARTESIAN_POINT('Ctrl Pts',(0.151224609513568,-0.031124574342357,
0.5824256623372));
#14561=CARTESIAN_POINT('Ctrl Pts',(0.15250864772478,0.0240568913137802,
0.58507305171146));
#14562=CARTESIAN_POINT('Ctrl Pts',(0.130311035929276,0.0671399443948921,
0.58772044108572));
#14563=CARTESIAN_POINT('Ctrl Pts',(0.108113424133771,0.110222997476006,
0.59036783045998));
#14564=CARTESIAN_POINT('Ctrl Pts',(0.0624341623315493,0.141207637982093,
0.593015219834239));
#14565=CARTESIAN_POINT('Ctrl Pts',(0.0141966988324609,0.145901308974836,
0.595662609208499));
#14566=CARTESIAN_POINT('Ctrl Pts',(-0.0340407646666261,0.150594979967579,
0.598309998582759));
#14567=CARTESIAN_POINT('Ctrl Pts',(-0.0848364298625779,0.128997681446978,
0.60095738795702));
#14568=CARTESIAN_POINT('Ctrl Pts',(-0.114923272877171,0.091002085522857,
0.60360477733128));
#14569=CARTESIAN_POINT('Ctrl Pts',(-0.135113526827902,0.0655045372973676,
0.60538135002609));
#14570=CARTESIAN_POINT('Ctrl Pts',(-0.14597798884013,0.0326223532682757,
0.6071579227209));
#14571=CARTESIAN_POINT('Ctrl Pts',(-0.146218520919543,-0.000115076211918358,
0.608934495415711));
#14572=CARTESIAN_POINT('Origin',(0.,0.,0.));
#14573=CARTESIAN_POINT('',(-0.146586033401767,-2.15382961294558E-5,0.66606550458429));
#14574=CARTESIAN_POINT('',(-0.146582846697157,-3.00215943766004E-5,0.65893449541571));
#14575=CARTESIAN_POINT('',(-0.14635,-1.79227059055215E-17,0.));
#14576=CARTESIAN_POINT('Ctrl Pts',(-0.146586033401767,-2.15382961294558E-5,
0.66606550458429));
#14577=CARTESIAN_POINT('Ctrl Pts',(-0.146488810225965,0.0472697707580183,
0.663482448132491));
#14578=CARTESIAN_POINT('Ctrl Pts',(-0.121516563758978,0.0946492637554097,
0.660899391680692));
#14579=CARTESIAN_POINT('Ctrl Pts',(-0.0824084263440199,0.121233094478226,
0.658316335228893));
#14580=CARTESIAN_POINT('Ctrl Pts',(-0.0423423130056393,0.148468111155377,
0.655670005349791));
#14581=CARTESIAN_POINT('Ctrl Pts',(0.0125607065496858,0.153876184485078,
0.653023675470689));
#14582=CARTESIAN_POINT('Ctrl Pts',(0.0571706564953393,0.134981954220393,
0.650377345591587));
#14583=CARTESIAN_POINT('Ctrl Pts',(0.101780606440992,0.116087723955709,
0.647731015712485));
#14584=CARTESIAN_POINT('Ctrl Pts',(0.136097486776972,0.0728911900966409,
0.645084685833384));
#14585=CARTESIAN_POINT('Ctrl Pts',(0.144413921474191,0.0251640857912735,
0.642438355954282));
#14586=CARTESIAN_POINT('Ctrl Pts',(0.152730356171409,-0.0225630185140953,
0.63979202607518));
#14587=CARTESIAN_POINT('Ctrl Pts',(0.135046345229863,-0.0748206932657649,
0.637145696196077));
#14588=CARTESIAN_POINT('Ctrl Pts',(0.0994561386758346,-0.10768977857233,
0.634499366316975));
#14589=CARTESIAN_POINT('Ctrl Pts',(0.0638659321218069,-0.140558863878895,
0.631853036437873));
#14590=CARTESIAN_POINT('Ctrl Pts',(0.0103695299552984,-0.154039359740357,
0.629206706558772));
#14591=CARTESIAN_POINT('Ctrl Pts',(-0.0365469229059137,-0.141961031115491,
0.62656037667967));
#14592=CARTESIAN_POINT('Ctrl Pts',(-0.0834633757671259,-0.129882702490626,
0.623914046800568));
#14593=CARTESIAN_POINT('Ctrl Pts',(-0.123799879323041,-0.0922455493794331,
0.621267716921466));
#14594=CARTESIAN_POINT('Ctrl Pts',(-0.139093781291504,-0.0462766888972804,
0.618621387042364));
#14595=CARTESIAN_POINT('Ctrl Pts',(-0.14401750805555,-0.0314774500153124,
0.617769426223006));
#14596=CARTESIAN_POINT('Ctrl Pts',(-0.14634567687575,-0.0158146654998378,
0.616917465403648));
#14597=CARTESIAN_POINT('Ctrl Pts',(-0.146227179098081,-0.000117664897458569,
0.616065504584291));
#14598=CARTESIAN_POINT('Ctrl Pts',(-0.146218520919543,-0.000115076211918358,
0.608934495415711));
#14599=CARTESIAN_POINT('Ctrl Pts',(-0.1463364217222,-0.0161618722236638,
0.60980531209516));
#14600=CARTESIAN_POINT('Ctrl Pts',(-0.143901781624712,-0.032173889023867,
0.61067612877461));
#14601=CARTESIAN_POINT('Ctrl Pts',(-0.138761720114909,-0.0472643972675185,
0.611546945454059));
#14602=CARTESIAN_POINT('Ctrl Pts',(-0.123135303504819,-0.0931413908061287,
0.614194334828319));
#14603=CARTESIAN_POINT('Ctrl Pts',(-0.0825044494514074,-0.130501484555709,
0.616841724202579));
#14604=CARTESIAN_POINT('Ctrl Pts',(-0.0354801761942514,-0.142231836504824,
0.619489113576839));
#14605=CARTESIAN_POINT('Ctrl Pts',(0.0115440970629072,-0.15396218845394,
0.6221365029511));
#14606=CARTESIAN_POINT('Ctrl Pts',(0.0649617895238099,-0.140062798602586,
0.624783892325359));
#14607=CARTESIAN_POINT('Ctrl Pts',(0.100304854137336,-0.106900301471969,
0.627431281699619));
#14608=CARTESIAN_POINT('Ctrl Pts',(0.135647918750861,-0.0737378043413545,
0.630078671073879));
#14609=CARTESIAN_POINT('Ctrl Pts',(0.15291635551701,-0.0213121999314781,
0.63272606044814));
#14610=CARTESIAN_POINT('Ctrl Pts',(0.144200333369931,0.026362891994447,
0.6353734498224));
#14611=CARTESIAN_POINT('Ctrl Pts',(0.135484311222852,0.0740379839203748,
0.63802083919666));
#14612=CARTESIAN_POINT('Ctrl Pts',(0.100783830162543,0.11696256336235,0.640668228570919));
#14613=CARTESIAN_POINT('Ctrl Pts',(0.055993492972559,0.135474968031154,
0.643315617945179));
#14614=CARTESIAN_POINT('Ctrl Pts',(0.0112031557825773,0.153987372699956,
0.64596300731944));
#14615=CARTESIAN_POINT('Ctrl Pts',(-0.04367703753708,0.148087602595587,
0.6486103966937));
#14616=CARTESIAN_POINT('Ctrl Pts',(-0.0835091394177698,0.120478055479053,
0.65125778606796));
#14617=CARTESIAN_POINT('Ctrl Pts',(-0.122009894390588,0.0937913289882395,
0.653816689183877));
#14618=CARTESIAN_POINT('Ctrl Pts',(-0.146451680634158,0.0468218259492564,
0.656375592299793));
#14619=CARTESIAN_POINT('Ctrl Pts',(-0.146582846697157,-3.00215943766004E-5,
0.65893449541571));
#14620=CARTESIAN_POINT('Origin',(0.,0.,0.));
#14621=CARTESIAN_POINT('',(-0.146290249280603,0.000131112932912382,0.716065504584291));
#14622=CARTESIAN_POINT('',(-0.146307221518699,0.000133045872591754,0.708934495415711));
#14623=CARTESIAN_POINT('',(-0.14635,-1.79227059055215E-17,0.));
#14624=CARTESIAN_POINT('Ctrl Pts',(-0.146290249280603,0.000131112932912382,
0.716065504584291));
#14625=CARTESIAN_POINT('Ctrl Pts',(-0.146406294125046,0.0134819654399978,
0.715340090619538));
#14626=CARTESIAN_POINT('Ctrl Pts',(-0.144729088574721,0.0268041890186768,
0.714614676654786));
#14627=CARTESIAN_POINT('Ctrl Pts',(-0.141142411757643,0.0395908011096033,
0.713889262690033));
#14628=CARTESIAN_POINT('Ctrl Pts',(-0.128058117149462,0.0862367098911347,
0.711242932810931));
#14629=CARTESIAN_POINT('Ctrl Pts',(-0.0895623832093418,0.125754646095387,
0.708596602931829));
#14630=CARTESIAN_POINT('Ctrl Pts',(-0.0432753130058998,0.140056628595385,
0.705950273052727));
#14631=CARTESIAN_POINT('Ctrl Pts',(0.00301175719754219,0.154358611095384,
0.703303943173625));
#14632=CARTESIAN_POINT('Ctrl Pts',(0.0570901636643063,0.143444639891129,
0.700657613294523));
#14633=CARTESIAN_POINT('Ctrl Pts',(0.0942073689518517,0.11231021130972,
0.698011283415421));
#14634=CARTESIAN_POINT('Ctrl Pts',(0.131324574239397,0.0811757827283121,
0.695364953536319));
#14635=CARTESIAN_POINT('Ctrl Pts',(0.151480578347723,0.0298208967697505,
0.692718623657217));
#14636=CARTESIAN_POINT('Ctrl Pts',(0.145449661086834,-0.0182485073085286,
0.690072293778115));
#14637=CARTESIAN_POINT('Ctrl Pts',(0.139418743825945,-0.0663179113868083,
0.687425963899014));
#14638=CARTESIAN_POINT('Ctrl Pts',(0.107200905195838,-0.111101833584806,
0.684779634019911));
#14639=CARTESIAN_POINT('Ctrl Pts',(0.0635427568131047,-0.132101968137704,
0.68213330414081));
#14640=CARTESIAN_POINT('Ctrl Pts',(0.0198846084303716,-0.153102102690602,
0.679486974261708));
#14641=CARTESIAN_POINT('Ctrl Pts',(-0.0352138497049885,-0.150318449598402,
0.676840644382606));
#14642=CARTESIAN_POINT('Ctrl Pts',(-0.0765331864534889,-0.125025130675956,
0.674194314503504));
#14643=CARTESIAN_POINT('Ctrl Pts',(-0.117852523201989,-0.0997318117535095,
0.671547984624402));
#14644=CARTESIAN_POINT('Ctrl Pts',(-0.14539273856363,-0.0519288270008166,
0.6689016547453));
#14645=CARTESIAN_POINT('Ctrl Pts',(-0.146548242683733,-0.00349635461217019,
0.666255324866198));
#14646=CARTESIAN_POINT('Ctrl Pts',(-0.146575870647472,-0.00233834005587287,
0.666192051438896));
#14647=CARTESIAN_POINT('Ctrl Pts',(-0.146588414938392,-0.00117996563262623,
0.666128778011593));
#14648=CARTESIAN_POINT('Ctrl Pts',(-0.146586033401767,-2.15382961294558E-5,
0.66606550458429));
#14649=CARTESIAN_POINT('Ctrl Pts',(-0.146582846697157,-3.00215943766004E-5,
0.65893449541571));
#14650=CARTESIAN_POINT('Ctrl Pts',(-0.146587382388275,-0.00165014728799839,
0.659022981674053));
#14651=CARTESIAN_POINT('Ctrl Pts',(-0.146562848415234,-0.00327013229389975,
0.659111467932396));
#14652=CARTESIAN_POINT('Ctrl Pts',(-0.146508820881567,-0.00488913307276392,
0.659199954190739));
#14653=CARTESIAN_POINT('Ctrl Pts',(-0.144892390022949,-0.0533274503793473,
0.661847343564999));
#14654=CARTESIAN_POINT('Ctrl Pts',(-0.116875517863988,-0.100884760863813,
0.66449473293926));
#14655=CARTESIAN_POINT('Ctrl Pts',(-0.0752913709948059,-0.125777373450206,
0.66714212231352));
#14656=CARTESIAN_POINT('Ctrl Pts',(-0.0337072241256252,-0.150669986036599,
0.66978951168778));
#14657=CARTESIAN_POINT('Ctrl Pts',(0.021444197453776,-0.15289790072492,
0.672436901062039));
#14658=CARTESIAN_POINT('Ctrl Pts',(0.0649007096996251,-0.131440618146733,
0.675084290436299));
#14659=CARTESIAN_POINT('Ctrl Pts',(0.108357221945475,-0.109983335568545,
0.677731679810559));
#14660=CARTESIAN_POINT('Ctrl Pts',(0.140118824857774,-0.0648408557238465,
0.68037906918482));
#14661=CARTESIAN_POINT('Ctrl Pts',(0.145637072805965,-0.0166907532130915,
0.68302645855908));
#14662=CARTESIAN_POINT('Ctrl Pts',(0.151155320754156,0.031459349297663,
0.68567384793334));
#14663=CARTESIAN_POINT('Ctrl Pts',(0.130430213738242,0.0826170744744734,
0.688321237307599));
#14664=CARTESIAN_POINT('Ctrl Pts',(0.0929549153570804,0.113349556369966,
0.690968626681859));
#14665=CARTESIAN_POINT('Ctrl Pts',(0.0554796169759186,0.14408203826546,
0.693616016056119));
#14666=CARTESIAN_POINT('Ctrl Pts',(0.00125412722950909,0.154389276879634,
0.69626340543038));
#14667=CARTESIAN_POINT('Ctrl Pts',(-0.0448834941801804,0.139550027475769,
0.69891079480464));
#14668=CARTESIAN_POINT('Ctrl Pts',(-0.0910211155898686,0.124710778071904,
0.7015581841789));
#14669=CARTESIAN_POINT('Ctrl Pts',(-0.129070868662838,0.0847250406500019,
0.704205573553159));
#14670=CARTESIAN_POINT('Ctrl Pts',(-0.141604011991841,0.0379083368947344,
0.706852962927419));
#14671=CARTESIAN_POINT('Ctrl Pts',(-0.144888775625201,0.0256383259412015,
0.707546807090183));
#14672=CARTESIAN_POINT('Ctrl Pts',(-0.146420824649375,0.0128991016161637,
0.708240651252947));
#14673=CARTESIAN_POINT('Ctrl Pts',(-0.146307221518699,0.000133045872591754,
0.708934495415711));
#14674=CARTESIAN_POINT('Origin',(0.,0.,0.));
#14675=CARTESIAN_POINT('',(-0.1461301977291,-5.61458017395017E-5,0.766065504584291));
#14676=CARTESIAN_POINT('',(-0.14612241379348,-4.54149644099216E-5,0.758934495415711));
#14677=CARTESIAN_POINT('',(-0.14635,-1.79227059055215E-17,0.));
#14678=CARTESIAN_POINT('Ctrl Pts',(-0.1461301977291,-5.61458017395017E-5,
0.766065504584291));
#14679=CARTESIAN_POINT('Ctrl Pts',(-0.14603380141711,0.0278870014676159,
0.764551403227483));
#14680=CARTESIAN_POINT('Ctrl Pts',(-0.138327245009168,0.0558793842949389,
0.763037301870675));
#14681=CARTESIAN_POINT('Ctrl Pts',(-0.123350675409043,0.079203679241543,
0.761523200513867));
#14682=CARTESIAN_POINT('Ctrl Pts',(-0.0971747899961838,0.119969628197767,
0.758876870634766));
#14683=CARTESIAN_POINT('Ctrl Pts',(-0.048790709571801,0.146475657227381,
0.756230540755664));
#14684=CARTESIAN_POINT('Ctrl Pts',(-0.000344588961360588,0.146589539830481,
0.753584210876561));
#14685=CARTESIAN_POINT('Ctrl Pts',(0.0481015316490792,0.14670342243358,
0.750937880997459));
#14686=CARTESIAN_POINT('Ctrl Pts',(0.0966096924455767,0.120425158610167,
0.748291551118357));
#14687=CARTESIAN_POINT('Ctrl Pts',(0.122976945064223,0.0797827231418903,
0.745645221239255));
#14688=CARTESIAN_POINT('Ctrl Pts',(0.149344197682869,0.0391402876736125,
0.742998891360154));
#14689=CARTESIAN_POINT('Ctrl Pts',(0.153570542123663,-0.01586631943953,
0.740352561481052));
#14690=CARTESIAN_POINT('Ctrl Pts',(0.133721514043982,-0.0600597087159893,
0.73770623160195));
#14691=CARTESIAN_POINT('Ctrl Pts',(0.113872485964301,-0.104253097992448,
0.735059901722848));
#14692=CARTESIAN_POINT('Ctrl Pts',(0.0699480853641458,-0.137633269432224,
0.732413571843746));
#14693=CARTESIAN_POINT('Ctrl Pts',(0.0220532014503509,-0.144921593405036,
0.729767241964644));
#14694=CARTESIAN_POINT('Ctrl Pts',(-0.0258416824634434,-0.152209917377848,
0.727120912085542));
#14695=CARTESIAN_POINT('Ctrl Pts',(-0.0777070496908773,-0.133406393883698,
0.724474582206441));
#14696=CARTESIAN_POINT('Ctrl Pts',(-0.109803305666473,-0.0971176914572187,
0.721828252327339));
#14697=CARTESIAN_POINT('Ctrl Pts',(-0.133101311474982,-0.0707764758164216,
0.71990733641299));
#14698=CARTESIAN_POINT('Ctrl Pts',(-0.14598295937539,-0.0352223077304616,
0.71798642049864));
#14699=CARTESIAN_POINT('Ctrl Pts',(-0.146290249280603,0.000131112932912382,
0.716065504584291));
#14700=CARTESIAN_POINT('Ctrl Pts',(-0.146307221518699,0.000133045872591754,
0.708934495415711));
#14701=CARTESIAN_POINT('Ctrl Pts',(-0.145987367488279,-0.0358102803178394,
0.710888040627207));
#14702=CARTESIAN_POINT('Ctrl Pts',(-0.132622002370819,-0.0719663061161047,
0.712841585838703));
#14703=CARTESIAN_POINT('Ctrl Pts',(-0.1086007072861,-0.0984612847532928,
0.7147951310502));
#14704=CARTESIAN_POINT('Ctrl Pts',(-0.0760477256663158,-0.134366532557423,
0.71744252042446));
#14705=CARTESIAN_POINT('Ctrl Pts',(-0.0239252288417074,-0.152529358077047,
0.720089909798719));
#14706=CARTESIAN_POINT('Ctrl Pts',(0.0238920022682765,-0.144630254255197,
0.722737299172979));
#14707=CARTESIAN_POINT('Ctrl Pts',(0.071709233378259,-0.136731150433346,
0.725384688547239));
#14708=CARTESIAN_POINT('Ctrl Pts',(0.115221198773618,-0.102770117270024,
0.7280320779215));
#14709=CARTESIAN_POINT('Ctrl Pts',(0.134497183226257,-0.058303052428779,
0.730679467295759));
#14710=CARTESIAN_POINT('Ctrl Pts',(0.153773167678896,-0.0138359875875333,
0.733326856670019));
#14711=CARTESIAN_POINT('Ctrl Pts',(0.148813171188813,0.0411371089316358,
0.735974246044279));
#14712=CARTESIAN_POINT('Ctrl Pts',(0.121889126928366,0.0814357351225549,
0.738621635418539));
#14713=CARTESIAN_POINT('Ctrl Pts',(0.0949650826679194,0.121734361313473,
0.741269024792799));
#14714=CARTESIAN_POINT('Ctrl Pts',(0.0460769906371109,0.147358517176143,
0.74391641416706));
#14715=CARTESIAN_POINT('Ctrl Pts',(-0.00238189178169058,0.146571023090686,
0.74656380354132));
#14716=CARTESIAN_POINT('Ctrl Pts',(-0.0508407742004934,0.14578352900523,
0.74921119291558));
#14717=CARTESIAN_POINT('Ctrl Pts',(-0.0988704470072894,0.118584384971644,
0.751858582289839));
#14718=CARTESIAN_POINT('Ctrl Pts',(-0.124470852918682,0.0774321960944291,
0.754505971664099));
#14719=CARTESIAN_POINT('Ctrl Pts',(-0.138745545153454,0.0544858868428234,
0.75598214624797));
#14720=CARTESIAN_POINT('Ctrl Pts',(-0.146046671909043,0.027201385339783,
0.757458320831841));
#14721=CARTESIAN_POINT('Ctrl Pts',(-0.14612241379348,-4.54149644099216E-5,
0.758934495415711));
#14722=CARTESIAN_POINT('Origin',(0.,0.,0.));
#14723=CARTESIAN_POINT('',(-0.146495788566881,-0.000101744904923998,0.816065504584291));
#14724=CARTESIAN_POINT('',(-0.146473871348434,-0.000110945968026819,0.808934495415711));
#14725=CARTESIAN_POINT('',(-0.14635,-1.79227059055215E-17,0.));
#14726=CARTESIAN_POINT('Ctrl Pts',(-0.146495788566881,-0.000101744904923998,
0.816065504584291));
#14727=CARTESIAN_POINT('Ctrl Pts',(-0.14616118452328,0.0421270051992108,
0.813762715835428));
#14728=CARTESIAN_POINT('Ctrl Pts',(-0.126905337350145,0.0846218946815527,
0.811459927086565));
#14729=CARTESIAN_POINT('Ctrl Pts',(-0.0947343415465314,0.111866064832055,
0.809157138337701));
#14730=CARTESIAN_POINT('Ctrl Pts',(-0.0577639214515077,0.143174651664521,
0.806510808458599));
#14731=CARTESIAN_POINT('Ctrl Pts',(-0.00373742343573488,0.154342745753647,
0.803864478579497));
#14732=CARTESIAN_POINT('Ctrl Pts',(0.0426163743729279,0.140258534729872,
0.801218148700395));
#14733=CARTESIAN_POINT('Ctrl Pts',(0.0889701721815907,0.126174323706097,
0.798571818821294));
#14734=CARTESIAN_POINT('Ctrl Pts',(0.127651269783143,0.0868378075694234,
0.795925488942192));
#14735=CARTESIAN_POINT('Ctrl Pts',(0.140954720244851,0.040253928627653,
0.79327915906309));
#14736=CARTESIAN_POINT('Ctrl Pts',(0.154258170706558,-0.00632995031411615,
0.790632829183988));
#14737=CARTESIAN_POINT('Ctrl Pts',(0.14218397402842,-0.060161192060982,
0.787986499304886));
#14738=CARTESIAN_POINT('Ctrl Pts',(0.110258679990485,-0.0966003903512828,
0.785340169425784));
#14739=CARTESIAN_POINT('Ctrl Pts',(0.0783333859525485,-0.133039588641585,
0.782693839546682));
#14740=CARTESIAN_POINT('Ctrl Pts',(0.0265569945548152,-0.152086743475322,
0.780047509667581));
#14741=CARTESIAN_POINT('Ctrl Pts',(-0.021371625274328,-0.14502367242074,
0.777401179788479));
#14742=CARTESIAN_POINT('Ctrl Pts',(-0.0693002451034712,-0.137960601366157,
0.774754849909377));
#14743=CARTESIAN_POINT('Ctrl Pts',(-0.113381093364023,-0.104787304423254,
0.772108520030274));
#14744=CARTESIAN_POINT('Ctrl Pts',(-0.133437672293631,-0.0606877215103841,
0.769462190151172));
#14745=CARTESIAN_POINT('Ctrl Pts',(-0.1420188514214,-0.0418197768941368,
0.768329961628878));
#14746=CARTESIAN_POINT('Ctrl Pts',(-0.146202281842484,-0.0209517273285418,
0.767197733106584));
#14747=CARTESIAN_POINT('Ctrl Pts',(-0.1461301977291,-5.61458017395017E-5,
0.766065504584291));
#14748=CARTESIAN_POINT('Ctrl Pts',(-0.14612241379348,-4.54149644099216E-5,
0.758934495415711));
#14749=CARTESIAN_POINT('Ctrl Pts',(-0.146182508321779,-0.0216633562673834,
0.760105710206101));
#14750=CARTESIAN_POINT('Ctrl Pts',(-0.141694203021096,-0.0432575645610501,
0.76127692499649));
#14751=CARTESIAN_POINT('Ctrl Pts',(-0.132531725405586,-0.0626424774360703,
0.76244813978688));
#14752=CARTESIAN_POINT('Ctrl Pts',(-0.111821052965107,-0.106459728368519,
0.76509552916114));
#14753=CARTESIAN_POINT('Ctrl Pts',(-0.067228569068158,-0.138988996512573,
0.767742918535399));
#14754=CARTESIAN_POINT('Ctrl Pts',(-0.0191799219195066,-0.145330206128911,
0.770390307909659));
#14755=CARTESIAN_POINT('Ctrl Pts',(0.0288687252291434,-0.151671415745249,
0.773037697283919));
#14756=CARTESIAN_POINT('Ctrl Pts',(0.080373535629496,-0.131824566833873,
0.77568508665818));
#14757=CARTESIAN_POINT('Ctrl Pts',(0.111742660473083,-0.0948805356683208,
0.77833247603244));
#14758=CARTESIAN_POINT('Ctrl Pts',(0.14311178531667,-0.0579365045027684,
0.7809798654067));
#14759=CARTESIAN_POINT('Ctrl Pts',(0.154345224603492,-0.00389529108304171,
0.783627254780959));
#14760=CARTESIAN_POINT('Ctrl Pts',(0.140297486112651,0.0424894529122293,
0.786274644155219));
#14761=CARTESIAN_POINT('Ctrl Pts',(0.126249747621811,0.0888741969075009,
0.788922033529479));
#14762=CARTESIAN_POINT('Ctrl Pts',(0.0869208313533056,0.127602471478316,
0.79156942290374));
#14763=CARTESIAN_POINT('Ctrl Pts',(0.0403254011646538,0.140934737517831,
0.794216812278));
#14764=CARTESIAN_POINT('Ctrl Pts',(-0.00627002902399674,0.154267003557346,
0.79686420165226));
#14765=CARTESIAN_POINT('Ctrl Pts',(-0.0601319731327944,0.142203261065564,
0.799511591026519));
#14766=CARTESIAN_POINT('Ctrl Pts',(-0.0965888940360299,0.110269323781398,
0.802158980400779));
#14767=CARTESIAN_POINT('Ctrl Pts',(-0.127690529151203,0.0830262752573849,
0.804417485405756));
#14768=CARTESIAN_POINT('Ctrl Pts',(-0.146124951115714,0.0413218847513699,
0.806675990410734));
#14769=CARTESIAN_POINT('Ctrl Pts',(-0.146473871348434,-0.000110945968026819,
0.808934495415711));
#14770=CARTESIAN_POINT('Origin',(0.,0.,0.));
#14771=CARTESIAN_POINT('',(-0.146444331750498,0.000119944961782359,0.866065504584291));
#14772=CARTESIAN_POINT('',(-0.146471560192382,0.00011177640072981,0.858934495415711));
#14773=CARTESIAN_POINT('',(-0.14635,-1.79227059055215E-17,0.));
#14774=CARTESIAN_POINT('Ctrl Pts',(-0.146444331750498,0.000119944961782359,
0.866065504584291));
#14775=CARTESIAN_POINT('Ctrl Pts',(-0.146516681599632,0.00829054204730037,
0.865620358322474));
#14776=CARTESIAN_POINT('Ctrl Pts',(-0.145891801779796,0.0164500693154795,
0.865175212060658));
#14777=CARTESIAN_POINT('Ctrl Pts',(-0.14453063157077,0.0244848619971339,
0.864730065798841));
#14778=CARTESIAN_POINT('Ctrl Pts',(-0.136438672357208,0.0722505376181754,
0.862083735919739));
#14779=CARTESIAN_POINT('Ctrl Pts',(-0.102325254887189,0.115607931012472,
0.859437406040638));
#14780=CARTESIAN_POINT('Ctrl Pts',(-0.0578046270350215,0.134711681091902,
0.856791076161536));
#14781=CARTESIAN_POINT('Ctrl Pts',(-0.0132839991828526,0.153815431171333,
0.854144746282434));
#14782=CARTESIAN_POINT('Ctrl Pts',(0.0416438390514653,0.148665537935894,
0.851498416403331));
#14783=CARTESIAN_POINT('Ctrl Pts',(0.081837551941475,0.121619188541491,
0.848852086524229));
#14784=CARTESIAN_POINT('Ctrl Pts',(0.122031264831484,0.0945728391470885,
0.846205756645128));
#14785=CARTESIAN_POINT('Ctrl Pts',(0.147490852377186,0.0456300335937214,
0.843559426766026));
#14786=CARTESIAN_POINT('Ctrl Pts',(0.146563060809277,-0.0028073360113171,
0.840913096886925));
#14787=CARTESIAN_POINT('Ctrl Pts',(0.145635269241369,-0.0512447056163556,
0.838266767007823));
#14788=CARTESIAN_POINT('Ctrl Pts',(0.118320098559852,-0.0991766392730661,
0.835620437128721));
#14789=CARTESIAN_POINT('Ctrl Pts',(0.0771201321287374,-0.124663936845065,
0.832974107249619));
#14790=CARTESIAN_POINT('Ctrl Pts',(0.035920165697623,-0.150151234417064,
0.830327777370517));
#14791=CARTESIAN_POINT('Ctrl Pts',(-0.0191645964830881,-0.153193895904352,
0.827681447491415));
#14792=CARTESIAN_POINT('Ctrl Pts',(-0.0629209921278279,-0.132399247274726,
0.825035117612313));
#14793=CARTESIAN_POINT('Ctrl Pts',(-0.106677387772568,-0.111604598645101,
0.822388787733211));
#14794=CARTESIAN_POINT('Ctrl Pts',(-0.139105416881337,-0.0669726398985626,
0.819742457854109));
#14795=CARTESIAN_POINT('Ctrl Pts',(-0.145362260348583,-0.0189321207373897,
0.817096127975007));
#14796=CARTESIAN_POINT('Ctrl Pts',(-0.146174510965348,-0.0126955988357878,
0.816752586844768));
#14797=CARTESIAN_POINT('Ctrl Pts',(-0.146545706411658,-0.00640163348415362,
0.81640904571453));
#14798=CARTESIAN_POINT('Ctrl Pts',(-0.146495788566881,-0.000101744904923998,
0.816065504584291));
#14799=CARTESIAN_POINT('Ctrl Pts',(-0.146473871348434,-0.000110945968026819,
0.808934495415711));
#14800=CARTESIAN_POINT('Ctrl Pts',(-0.146533950748007,-0.00724512552769256,
0.809323379784994));
#14801=CARTESIAN_POINT('Ctrl Pts',(-0.146057826922151,-0.0143712538186879,
0.809712264154277));
#14802=CARTESIAN_POINT('Ctrl Pts',(-0.145017839345608,-0.0214141189368497,
0.81010114852356));
#14803=CARTESIAN_POINT('Ctrl Pts',(-0.137937966054276,-0.0693594922943736,
0.81274853789782));
#14804=CARTESIAN_POINT('Ctrl Pts',(-0.104726321773939,-0.113446106932874,
0.81539592727208));
#14805=CARTESIAN_POINT('Ctrl Pts',(-0.0605955455659204,-0.133480028752914,
0.818043316646339));
#14806=CARTESIAN_POINT('Ctrl Pts',(-0.0164647693578984,-0.153513950572954,
0.820690706020599));
#14807=CARTESIAN_POINT('Ctrl Pts',(0.0385851387778066,-0.149495179574532,
0.823338095394859));
#14808=CARTESIAN_POINT('Ctrl Pts',(0.0793384931690736,-0.12326451930694,
0.825985484769119));
#14809=CARTESIAN_POINT('Ctrl Pts',(0.120091847560339,-0.0970338590393495,
0.828632874143379));
#14810=CARTESIAN_POINT('Ctrl Pts',(0.146548648207165,-0.0485913095025905,
0.83128026351764));
#14811=CARTESIAN_POINT('Ctrl Pts',(0.146590321408106,-0.000126046730599388,
0.833927652891899));
#14812=CARTESIAN_POINT('Ctrl Pts',(0.146631994609047,0.0483392160413931,
0.836575042266159));
#14813=CARTESIAN_POINT('Ctrl Pts',(0.120258540364101,0.0968271920486179,
0.839222431640419));
#14814=CARTESIAN_POINT('Ctrl Pts',(0.0795503554414038,0.123127897600245,
0.841869821014679));
#14815=CARTESIAN_POINT('Ctrl Pts',(0.0388421705187073,0.149428603151872,
0.844517210388939));
#14816=CARTESIAN_POINT('Ctrl Pts',(-0.0162007450817403,0.153542038247903,
0.8471645997632));
#14817=CARTESIAN_POINT('Ctrl Pts',(-0.0603659086281491,0.133584038319734,
0.84981198913746));
#14818=CARTESIAN_POINT('Ctrl Pts',(-0.104531072174558,0.113626038391565,
0.85245937851172));
#14819=CARTESIAN_POINT('Ctrl Pts',(-0.137818483666928,0.0695966034391962,
0.855106767885979));
#14820=CARTESIAN_POINT('Ctrl Pts',(-0.144980798768897,0.0216634763286692,
0.857754157260239));
#14821=CARTESIAN_POINT('Ctrl Pts',(-0.146045237806912,0.0145398171508471,
0.858147603312063));
#14822=CARTESIAN_POINT('Ctrl Pts',(-0.146532654486068,0.00732993751956911,
0.858541049363887));
#14823=CARTESIAN_POINT('Ctrl Pts',(-0.146471560192382,0.00011177640072981,
0.858934495415711));
#14824=CARTESIAN_POINT('Origin',(0.,0.,0.));
#14825=CARTESIAN_POINT('',(-0.146114231148477,2.69008449349656E-5,0.916065504584291));
#14826=CARTESIAN_POINT('',(-0.146121644853617,4.41067432152685E-5,0.908934495415711));
#14827=CARTESIAN_POINT('',(-0.14635,-1.79227059055215E-17,0.));
#14828=CARTESIAN_POINT('Ctrl Pts',(-0.146114231148477,2.69008449349656E-5,
0.916065504584291));
#14829=CARTESIAN_POINT('Ctrl Pts',(-0.146151635159142,0.0228038459942234,
0.914831670930419));
#14830=CARTESIAN_POINT('Ctrl Pts',(-0.141147538069067,0.0455652341090756,
0.913597837276548));
#14831=CARTESIAN_POINT('Ctrl Pts',(-0.131015765267123,0.0657531838068269,
0.912364003622676));
#14832=CARTESIAN_POINT('Ctrl Pts',(-0.109285110563454,0.109052354902802,
0.909717673743574));
#14833=CARTESIAN_POINT('Ctrl Pts',(-0.0639662294071284,0.140513248471977,
0.907071343864472));
#14834=CARTESIAN_POINT('Ctrl Pts',(-0.015802286694576,0.145735718560985,
0.90442501398537));
#14835=CARTESIAN_POINT('Ctrl Pts',(0.0323616560179757,0.150958188649994,
0.901778684106268));
#14836=CARTESIAN_POINT('Ctrl Pts',(0.0833706602867547,0.129942235258839,
0.899132354227166));
#14837=CARTESIAN_POINT('Ctrl Pts',(0.113877102345416,0.0923071908936453,
0.896486024348064));
#14838=CARTESIAN_POINT('Ctrl Pts',(0.144383544404078,0.0546721465284523,
0.893839694468962));
#14839=CARTESIAN_POINT('Ctrl Pts',(0.15438742425262,0.000418011189221586,
0.891193364589861));
#14840=CARTESIAN_POINT('Ctrl Pts',(0.139309808695705,-0.0456222438118789,
0.888547034710759));
#14841=CARTESIAN_POINT('Ctrl Pts',(0.124232193138789,-0.0916624988129813,
0.885900704831657));
#14842=CARTESIAN_POINT('Ctrl Pts',(0.0840730821764119,-0.129488873475953,
0.883254374952555));
#14843=CARTESIAN_POINT('Ctrl Pts',(0.0372139327097935,-0.141787641004198,
0.880608045073453));
#14844=CARTESIAN_POINT('Ctrl Pts',(-0.00964521675682358,-0.154086408532443,
0.877961715194351));
#14845=CARTESIAN_POINT('Ctrl Pts',(-0.0632044047276821,-0.140857568925962,
0.875315385315249));
#14846=CARTESIAN_POINT('Ctrl Pts',(-0.0989487482345592,-0.108156170198829,
0.872669055436147));
#14847=CARTESIAN_POINT('Ctrl Pts',(-0.128680439645858,-0.0809555616469925,
0.870467871818862));
#14848=CARTESIAN_POINT('Ctrl Pts',(-0.146086572253705,-0.0402824710322022,
0.868266688201576));
#14849=CARTESIAN_POINT('Ctrl Pts',(-0.146444331750498,0.000119944961782359,
0.866065504584291));
#14850=CARTESIAN_POINT('Ctrl Pts',(-0.146471560192382,0.00011177640072981,
0.858934495415711));
#14851=CARTESIAN_POINT('Ctrl Pts',(-0.146121567926216,-0.0412390669452651,
0.861188438738147));
#14852=CARTESIAN_POINT('Ctrl Pts',(-0.127770397964496,-0.0828616943330661,
0.863442382060584));
#14853=CARTESIAN_POINT('Ctrl Pts',(-0.096778382793969,-0.110103055552942,
0.86569632538302));
#14854=CARTESIAN_POINT('Ctrl Pts',(-0.0603764330055066,-0.142099641055337,
0.86834371475728));
#14855=CARTESIAN_POINT('Ctrl Pts',(-0.00653531471701479,-0.154255992791443,
0.870991104131539));
#14856=CARTESIAN_POINT('Ctrl Pts',(0.040082974241256,-0.14100387723139,
0.873638493505799));
#14857=CARTESIAN_POINT('Ctrl Pts',(0.0867012631995282,-0.127751761671338,
0.876285882880059));
#14858=CARTESIAN_POINT('Ctrl Pts',(0.12609672282758,-0.0890911788151255,
0.878933272254319));
#14859=CARTESIAN_POINT('Ctrl Pts',(0.140224208991091,-0.042730661487191,
0.88158066162858));
#14860=CARTESIAN_POINT('Ctrl Pts',(0.154351695154603,0.00362985584074295,
0.88422805100284));
#14861=CARTESIAN_POINT('Ctrl Pts',(0.143211207853577,0.057690307640398,
0.886875440377099));
#14862=CARTESIAN_POINT('Ctrl Pts',(0.111905662524754,0.09468823006692,0.889522829751359));
#14863=CARTESIAN_POINT('Ctrl Pts',(0.0806001171959318,0.131686152493442,
0.892170219125619));
#14864=CARTESIAN_POINT('Ctrl Pts',(0.0291295138393125,0.15162154554683,
0.894817608499879));
#14865=CARTESIAN_POINT('Ctrl Pts',(-0.0189299673197759,0.145362975188259,
0.897464997874139));
#14866=CARTESIAN_POINT('Ctrl Pts',(-0.0669894484788628,0.139104404829688,
0.9001123872484));
#14867=CARTESIAN_POINT('Ctrl Pts',(-0.11163780744042,0.10665187105916,0.902759776622659));
#14868=CARTESIAN_POINT('Ctrl Pts',(-0.132423802349956,0.0628703013313112,
0.905407165996919));
#14869=CARTESIAN_POINT('Ctrl Pts',(-0.141655418982822,0.043425734493323,
0.90658294246985));
#14870=CARTESIAN_POINT('Ctrl Pts',(-0.146180218154578,0.0217465313827003,
0.907758718942781));
#14871=CARTESIAN_POINT('Ctrl Pts',(-0.146121644853617,4.41067432152685E-5,
0.908934495415711));
#14872=CARTESIAN_POINT('Origin',(0.,0.,0.));
#14873=CARTESIAN_POINT('',(-0.146345621585321,-0.000133809880645736,0.966065504584291));
#14874=CARTESIAN_POINT('',(-0.146309694201085,-0.000133223314395004,0.958934495415711));
#14875=CARTESIAN_POINT('',(-0.14635,-1.79227059055215E-17,0.));
#14876=CARTESIAN_POINT('Ctrl Pts',(-0.146345621585321,-0.000133809880645736,
0.966065504584291));
#14877=CARTESIAN_POINT('Ctrl Pts',(-0.146004672532387,0.0370537288701324,
0.964042983538364));
#14878=CARTESIAN_POINT('Ctrl Pts',(-0.131578083002406,0.0744765756810296,
0.962020462492437));
#14879=CARTESIAN_POINT('Ctrl Pts',(-0.106003654037246,0.101251356830495,
0.959997941446511));
#14880=CARTESIAN_POINT('Ctrl Pts',(-0.0725412702228666,0.136284319036219,
0.957351611567409));
#14881=CARTESIAN_POINT('Ctrl Pts',(-0.0199938687303381,0.153087872523943,
0.954705281688306));
#14882=CARTESIAN_POINT('Ctrl Pts',(0.0275867780614433,0.143970766496025,
0.952058951809204));
#14883=CARTESIAN_POINT('Ctrl Pts',(0.0751674248532248,0.134853660468108,
0.949412621930102));
#14884=CARTESIAN_POINT('Ctrl Pts',(0.11778131694426,0.0998158949245492,
0.946766292051));
#14885=CARTESIAN_POINT('Ctrl Pts',(0.135923405490256,0.0548948063954655,
0.944119962171899));
#14886=CARTESIAN_POINT('Ctrl Pts',(0.154065494036253,0.0099737178663825,
0.941473632292797));
#14887=CARTESIAN_POINT('Ctrl Pts',(0.147735779037212,-0.0448306936482241,
0.938827302413695));
#14888=CARTESIAN_POINT('Ctrl Pts',(0.119831470632095,-0.0844335867733556,
0.936180972534593));
#14889=CARTESIAN_POINT('Ctrl Pts',(0.0919271622269763,-0.124036479898489,
0.933534642655491));
#14890=CARTESIAN_POINT('Ctrl Pts',(0.0424482604157787,-0.148437854634144,
0.93088831277639));
#14891=CARTESIAN_POINT('Ctrl Pts',(-0.00595796300272124,-0.146468817862788,
0.928241982897288));
#14892=CARTESIAN_POINT('Ctrl Pts',(-0.0543641864212212,-0.144499781091432,
0.925595653018186));
#14893=CARTESIAN_POINT('Ctrl Pts',(-0.101697731447024,-0.116160332813065,
0.922949323139084));
#14894=CARTESIAN_POINT('Ctrl Pts',(-0.126293289834417,-0.0744218843624929,
0.920302993259982));
#14895=CARTESIAN_POINT('Ctrl Pts',(-0.139421333187579,-0.052143709087005,
0.918890497034752));
#14896=CARTESIAN_POINT('Ctrl Pts',(-0.146071410932229,-0.0260482098028304,
0.917478000809521));
#14897=CARTESIAN_POINT('Ctrl Pts',(-0.146114231148477,2.69008449349656E-5,
0.916065504584291));
#14898=CARTESIAN_POINT('Ctrl Pts',(-0.146121644853617,4.41067432152685E-5,
0.908934495415711));
#14899=CARTESIAN_POINT('Ctrl Pts',(-0.146048333958771,-0.027118852224649,
0.910406108317041));
#14900=CARTESIAN_POINT('Ctrl Pts',(-0.138795050353101,-0.0543181883240968,
0.91187772121837));
#14901=CARTESIAN_POINT('Ctrl Pts',(-0.124603830013468,-0.0772180274565794,
0.9133493341197));
#14902=CARTESIAN_POINT('Ctrl Pts',(-0.0990742319099257,-0.118414180831446,
0.91599672349396));
#14903=CARTESIAN_POINT('Ctrl Pts',(-0.0510914048453256,-0.145695881896007,
0.91864411286822));
#14904=CARTESIAN_POINT('Ctrl Pts',(-0.00263394834681351,-0.146566710184873,
0.92129150224248));
#14905=CARTESIAN_POINT('Ctrl Pts',(0.0458235081516972,-0.147437538473739,
0.92393889161674));
#14906=CARTESIAN_POINT('Ctrl Pts',(0.0947555940841207,-0.121897493986912,
0.926586280990999));
#14907=CARTESIAN_POINT('Ctrl Pts',(0.121748900601314,-0.0816452290135895,
0.929233670365259));
#14908=CARTESIAN_POINT('Ctrl Pts',(0.148742207118509,-0.0413929640402651,
0.931881059739519));
#14909=CARTESIAN_POINT('Ctrl Pts',(0.153796734220472,0.0135715214195569,
0.93452844911378));
#14910=CARTESIAN_POINT('Ctrl Pts',(0.134597248858856,0.0580716696672091,
0.93717583848804));
#14911=CARTESIAN_POINT('Ctrl Pts',(0.115397763497239,0.102571817914861,
0.9398232278623));
#14912=CARTESIAN_POINT('Ctrl Pts',(0.0719442656720451,0.136607628950342,
0.942470617236559));
#14913=CARTESIAN_POINT('Ctrl Pts',(0.0241406894609324,0.144588953003544,
0.945118006610819));
#14914=CARTESIAN_POINT('Ctrl Pts',(-0.023662886750181,0.152570277056746,
0.947765395985079));
#14915=CARTESIAN_POINT('Ctrl Pts',(-0.0758165413472122,0.134497114127667,
0.950412785359339));
#14916=CARTESIAN_POINT('Ctrl Pts',(-0.108431221550465,0.0986479012011113,
0.953060174733599));
#14917=CARTESIAN_POINT('Ctrl Pts',(-0.132554242808212,0.0721325001574252,
0.955018281627637));
#14918=CARTESIAN_POINT('Ctrl Pts',(-0.145988218858404,0.0358924841874147,
0.956976388521674));
#14919=CARTESIAN_POINT('Ctrl Pts',(-0.146309694201085,-0.000133223314395004,
0.958934495415711));
#14920=CARTESIAN_POINT('Origin',(0.,0.,0.));
#14921=CARTESIAN_POINT('',(-0.146565171121453,5.44893591410845E-5,1.01606550458429));
#14922=CARTESIAN_POINT('',(-0.146582076026177,3.15354312248815E-5,1.00893449541571));
#14923=CARTESIAN_POINT('',(-0.14635,-1.79227059055215E-17,0.));
#14924=CARTESIAN_POINT('Ctrl Pts',(-0.146565171121453,5.44893591410845E-5,
1.01606550458429));
#14925=CARTESIAN_POINT('Ctrl Pts',(-0.146579596851449,0.00307427920823236,
1.01590062602541));
#14926=CARTESIAN_POINT('Ctrl Pts',(-0.146494352296349,0.00609323927190738,
1.01573574746653));
#14927=CARTESIAN_POINT('Ctrl Pts',(-0.146306854564556,0.00910583530985269,
1.01557086890765));
#14928=CARTESIAN_POINT('Ctrl Pts',(-0.143297482980539,0.0574585317612167,
1.01292453902855));
#14929=CARTESIAN_POINT('Ctrl Pts',(-0.11394685994478,0.104171803331984,
1.01027820914945));
#14930=CARTESIAN_POINT('Ctrl Pts',(-0.0716892273871119,0.127864250695428,
1.00763187927034));
#14931=CARTESIAN_POINT('Ctrl Pts',(-0.0294315948294418,0.151556698058874,
1.00498554939124));
#14932=CARTESIAN_POINT('Ctrl Pts',(0.0257330472501378,0.152228321214993,
1.00233921951214));
#14933=CARTESIAN_POINT('Ctrl Pts',(0.0685549742796134,0.129571707678744,
0.999692889633039));
#14934=CARTESIAN_POINT('Ctrl Pts',(0.111376901309088,0.106915094142495,
0.997046559753937));
#14935=CARTESIAN_POINT('Ctrl Pts',(0.141856113288459,0.0609302439138786,
0.994400229874835));
#14936=CARTESIAN_POINT('Ctrl Pts',(0.146041795372579,0.0126651464112397,
0.991753899995733));
#14937=CARTESIAN_POINT('Ctrl Pts',(0.150227477456699,-0.0355999510913994,
0.989107570116631));
#14938=CARTESIAN_POINT('Ctrl Pts',(0.128119629645567,-0.0861452958680607,
0.986461240237529));
#14939=CARTESIAN_POINT('Ctrl Pts',(0.0898373616998479,-0.115835488396583,
0.983814910358427));
#14940=CARTESIAN_POINT('Ctrl Pts',(0.051555093754129,-0.145525680925106,
0.981168580479325));
#14941=CARTESIAN_POINT('Ctrl Pts',(-0.00290159432617693,-0.154360721205491,
0.978522250600224));
#14942=CARTESIAN_POINT('Ctrl Pts',(-0.0486070196525971,-0.138296672301818,
0.975875920721122));
#14943=CARTESIAN_POINT('Ctrl Pts',(-0.0943124449790173,-0.122232623398145,
0.97322959084202));
#14944=CARTESIAN_POINT('Ctrl Pts',(-0.131266607551552,-0.081269485310415,
0.970583260962917));
#14945=CARTESIAN_POINT('Ctrl Pts',(-0.142555005769704,-0.0341567308046872,
0.967936931083816));
#14946=CARTESIAN_POINT('Ctrl Pts',(-0.145215975052668,-0.0230510282813687,
0.967313122250641));
#14947=CARTESIAN_POINT('Ctrl Pts',(-0.146450780951306,-0.0116036114945705,
0.966689313417466));
#14948=CARTESIAN_POINT('Ctrl Pts',(-0.146345621585321,-0.000133809880645736,
0.966065504584291));
#14949=CARTESIAN_POINT('Ctrl Pts',(-0.146309694201085,-0.000133223314395004,
0.958934495415711));
#14950=CARTESIAN_POINT('Ctrl Pts',(-0.146422858258782,-0.0128148032088542,
0.959623777895933));
#14951=CARTESIAN_POINT('Ctrl Pts',(-0.14491119500038,-0.0254698272036438,
0.960313060376156));
#14952=CARTESIAN_POINT('Ctrl Pts',(-0.141668994059001,-0.037664762585484,
0.961002342856379));
#14953=CARTESIAN_POINT('Ctrl Pts',(-0.129216380554811,-0.0845029505214961,
0.963649732230639));
#14954=CARTESIAN_POINT('Ctrl Pts',(-0.0912354477369537,-0.12455406346949,
0.966297121604899));
#14955=CARTESIAN_POINT('Ctrl Pts',(-0.0451234138007503,-0.1394726343957,
0.968944510979159));
#14956=CARTESIAN_POINT('Ctrl Pts',(0.00098862013545236,-0.154391205321909,
0.97159190035342));
#14957=CARTESIAN_POINT('Ctrl Pts',(0.055231755190001,-0.144177234226336,
0.974239289727679));
#14958=CARTESIAN_POINT('Ctrl Pts',(0.0927598492034174,-0.113509244531313,
0.976886679101939));
#14959=CARTESIAN_POINT('Ctrl Pts',(0.130287943216833,-0.0828412548362905,
0.979534068476199));
#14960=CARTESIAN_POINT('Ctrl Pts',(0.151100996189117,-0.0317192465418168,
0.982181457850459));
#14961=CARTESIAN_POINT('Ctrl Pts',(0.145665560755875,0.0164402745715088,
0.984828847224719));
#14962=CARTESIAN_POINT('Ctrl Pts',(0.140230125322634,0.0645997956848379,
0.987476236598979));
#14963=CARTESIAN_POINT('Ctrl Pts',(0.108546201483865,0.109796829617019,
0.990123625973239));
#14964=CARTESIAN_POINT('Ctrl Pts',(0.0651266538643092,0.131328813193254,
0.992771015347499));
#14965=CARTESIAN_POINT('Ctrl Pts',(0.0217071062447581,0.152860796769488,
0.995418404721759));
#14966=CARTESIAN_POINT('Ctrl Pts',(-0.0334480651555777,0.15072772998978,
0.998065794096019));
#14967=CARTESIAN_POINT('Ctrl Pts',(-0.0750749586823209,0.125906667008376,
1.00071318347028));
#14968=CARTESIAN_POINT('Ctrl Pts',(-0.116701852209067,0.101085604026969,
1.00336057284454));
#14969=CARTESIAN_POINT('Ctrl Pts',(-0.144800467862219,0.053576544843864,
1.0060079622188));
#14970=CARTESIAN_POINT('Ctrl Pts',(-0.146500196332402,0.00514107896046776,
1.00865535159306));
#14971=CARTESIAN_POINT('Ctrl Pts',(-0.146559936783033,0.00343871495990628,
1.00874839953394));
#14972=CARTESIAN_POINT('Ctrl Pts',(-0.146587066279139,0.00173520655478852,
1.00884144747483));
#14973=CARTESIAN_POINT('Ctrl Pts',(-0.146582076026177,3.15354312248815E-5,
1.00893449541571));
#14974=CARTESIAN_POINT('Origin',(0.,0.,0.));
#14975=CARTESIAN_POINT('',(-0.146184049129756,9.96948043307314E-5,1.06606550458429));
#14976=CARTESIAN_POINT('',(-0.146216477546812,0.000114345603752017,1.05893449541571));
#14977=CARTESIAN_POINT('',(-0.14635,-1.79227059055215E-17,0.));
#14978=CARTESIAN_POINT('Ctrl Pts',(-0.146184049129756,9.96948043307314E-5,
1.06606550458429));
#14979=CARTESIAN_POINT('Ctrl Pts',(-0.146294264763128,0.0176817746259609,
1.06511193863336));
#14980=CARTESIAN_POINT('Ctrl Pts',(-0.143360807533043,0.0352283113603788,
1.06415837268242));
#14981=CARTESIAN_POINT('Ctrl Pts',(-0.13721959397524,0.0515693218739058,
1.06320480673148));
#14982=CARTESIAN_POINT('Ctrl Pts',(-0.120176538991979,0.0969187854681546,
1.06055847685238));
#14983=CARTESIAN_POINT('Ctrl Pts',(-0.0784283132238915,0.132983650068601,
1.05791214697328));
#14984=CARTESIAN_POINT('Ctrl Pts',(-0.0310837364199337,0.143256459747686,
1.05526581709418));
#14985=CARTESIAN_POINT('Ctrl Pts',(0.0162608403840241,0.153529269426771,
1.05261948721508));
#14986=CARTESIAN_POINT('Ctrl Pts',(0.0692017682238519,0.138010024184496,
1.04997315733597));
#14987=CARTESIAN_POINT('Ctrl Pts',(0.103507151520239,0.103802126728842,
1.04732682745687));
#14988=CARTESIAN_POINT('Ctrl Pts',(0.137812534816628,0.0695942292731864,
1.04468049757777));
#14989=CARTESIAN_POINT('Ctrl Pts',(0.153482373569574,0.01669767960415,1.04203416769867));
#14990=CARTESIAN_POINT('Ctrl Pts',(0.143344336052008,-0.0306759392859165,
1.03938783781957));
#14991=CARTESIAN_POINT('Ctrl Pts',(0.133206298534443,-0.0780495581759789,
1.03674150794047));
#14992=CARTESIAN_POINT('Ctrl Pts',(0.0972603847463712,-0.119900246287072,
1.03409517806136));
#14993=CARTESIAN_POINT('Ctrl Pts',(0.0519596049571008,-0.137072285243832,
1.03144884818226));
#14994=CARTESIAN_POINT('Ctrl Pts',(0.00665882516783032,-0.154244324200591,
1.02880251830316));
#14995=CARTESIAN_POINT('Ctrl Pts',(-0.0479968206226384,-0.146737714003016,
1.02615618842406));
#14996=CARTESIAN_POINT('Ctrl Pts',(-0.0869905834517384,-0.11798834823825,
1.02350985854496));
#14997=CARTESIAN_POINT('Ctrl Pts',(-0.123554854979944,-0.0910302005802824,
1.02102840722473));
#14998=CARTESIAN_POINT('Ctrl Pts',(-0.146348061346918,-0.0453938791777224,
1.01854695590451));
#14999=CARTESIAN_POINT('Ctrl Pts',(-0.146565171121453,5.44893591410845E-5,
1.01606550458429));
#15000=CARTESIAN_POINT('Ctrl Pts',(-0.146582076026177,3.15354312248815E-5,
1.00893449541571));
#15001=CARTESIAN_POINT('Ctrl Pts',(-0.146445084172466,-0.0467374494427972,
1.01148883684909));
#15002=CARTESIAN_POINT('Ctrl Pts',(-0.122102455869861,-0.0936290599181376,
1.01404317828246));
#15003=CARTESIAN_POINT('Ctrl Pts',(-0.0837162036049941,-0.120334265578335,
1.01659751971584));
#15004=CARTESIAN_POINT('Ctrl Pts',(-0.0439316411201867,-0.14801227165006,
1.0192449090901));
#15005=CARTESIAN_POINT('Ctrl Pts',(0.0109383251366414,-0.154006411209824,
1.02189229846436));
#15006=CARTESIAN_POINT('Ctrl Pts',(0.0557604321169594,-0.135571060438576,
1.02453968783862));
#15007=CARTESIAN_POINT('Ctrl Pts',(0.100582539097277,-0.11713570966733,
1.02718707721288));
#15008=CARTESIAN_POINT('Ctrl Pts',(0.135356786801084,-0.0742708685650716,
1.02983446658714));
#15009=CARTESIAN_POINT('Ctrl Pts',(0.144154783532934,-0.0266108361928598,
1.0324818559614));
#15010=CARTESIAN_POINT('Ctrl Pts',(0.152952780264784,0.0210491961793507,
1.03512924533566));
#15011=CARTESIAN_POINT('Ctrl Pts',(0.135774526024679,0.0735044198215165,
1.03777663470992));
#15012=CARTESIAN_POINT('Ctrl Pts',(0.100488543649143,0.106727647840587,
1.04042402408418));
#15013=CARTESIAN_POINT('Ctrl Pts',(0.0652025612736062,0.139950875859659,
1.04307141345844));
#15014=CARTESIAN_POINT('Ctrl Pts',(0.0118088507626404,0.153942108255635,
1.0457188028327));
#15015=CARTESIAN_POINT('Ctrl Pts',(-0.0352355257975899,0.142292641904202,
1.04836619220696));
#15016=CARTESIAN_POINT('Ctrl Pts',(-0.0822799023578202,0.130643175552769,
1.05101358158122));
#15017=CARTESIAN_POINT('Ctrl Pts',(-0.122974944967313,0.0933530104539243,
1.05366097095548));
#15018=CARTESIAN_POINT('Ctrl Pts',(-0.138680233730631,0.0475029577050484,
1.05630836032974));
#15019=CARTESIAN_POINT('Ctrl Pts',(-0.143873300563147,0.0323423075707214,
1.05718373869173));
#15020=CARTESIAN_POINT('Ctrl Pts',(-0.146334133026589,0.0162457690968458,
1.05805911705372));
#15021=CARTESIAN_POINT('Ctrl Pts',(-0.146216477546812,0.000114345603752017,
1.05893449541571));
#15022=CARTESIAN_POINT('Origin',(0.,0.,0.));
#15023=CARTESIAN_POINT('',(-0.146204073634541,-0.000109175101205505,1.11606550458429));
#15024=CARTESIAN_POINT('',(-0.146170555016798,-9.22629125885076E-5,1.10893449541571));
#15025=CARTESIAN_POINT('',(-0.14635,-1.79227059055215E-17,0.));
#15026=CARTESIAN_POINT('Ctrl Pts',(-0.146204073634541,-0.000109175101205505,
1.11606550458429));
#15027=CARTESIAN_POINT('Ctrl Pts',(-0.145981599624502,0.032003853555373,
1.1143232512413));
#15028=CARTESIAN_POINT('Ctrl Pts',(-0.135565881201595,0.0642480963468658,
1.11258099789831));
#15029=CARTESIAN_POINT('Ctrl Pts',(-0.11609067353381,0.0895073597405865,
1.11083874455532));
#15030=CARTESIAN_POINT('Ctrl Pts',(-0.0865095427755784,0.127873963375947,
1.10819241467622));
#15031=CARTESIAN_POINT('Ctrl Pts',(-0.0360273159486943,0.150125560802435,
1.10554608479712));
#15032=CARTESIAN_POINT('Ctrl Pts',(0.0122494975033169,0.14607724579886,
1.10289975491801));
#15033=CARTESIAN_POINT('Ctrl Pts',(0.0605263109553308,0.142028930795284,
1.10025342503891));
#15034=CARTESIAN_POINT('Ctrl Pts',(0.10659771103247,0.111680703361642,1.09760709515981));
#15035=CARTESIAN_POINT('Ctrl Pts',(0.129376093089052,0.0689234246557527,
1.09496076528071));
#15036=CARTESIAN_POINT('Ctrl Pts',(0.152154475145634,0.0261661459498645,
1.09231443540161));
#15037=CARTESIAN_POINT('Ctrl Pts',(0.151639839181659,-0.0290001840282729,
1.0896681055225));
#15038=CARTESIAN_POINT('Ctrl Pts',(0.128067742174483,-0.0713250681289163,
1.0870217756434));
#15039=CARTESIAN_POINT('Ctrl Pts',(0.104495645167307,-0.11364995222956,
1.0843754457643));
#15040=CARTESIAN_POINT('Ctrl Pts',(0.0578660871169326,-0.143133390452712,
1.0817291158852));
#15041=CARTESIAN_POINT('Ctrl Pts',(0.00952215035475689,-0.146280349267719,
1.0790827860061));
#15042=CARTESIAN_POINT('Ctrl Pts',(-0.0388217864074202,-0.149427308082725,
1.07643645612699));
#15043=CARTESIAN_POINT('Ctrl Pts',(-0.0888801018813974,-0.126237787489585,
1.07379012624789));
#15044=CARTESIAN_POINT('Ctrl Pts',(-0.117740317519168,-0.0873259958989869,
1.07114379636879));
#15045=CARTESIAN_POINT('Ctrl Pts',(-0.136201180005177,-0.0624354946409797,
1.06945103244062));
#15046=CARTESIAN_POINT('Ctrl Pts',(-0.145988395071105,-0.0311118962502767,
1.06775826851246));
#15047=CARTESIAN_POINT('Ctrl Pts',(-0.146184049129756,9.96948043307314E-5,
1.06606550458429));
#15048=CARTESIAN_POINT('Ctrl Pts',(-0.146216477546812,0.000114345603752017,
1.05893449541571));
#15049=CARTESIAN_POINT('Ctrl Pts',(-0.145978309898544,-0.0325401742182177,
1.06070650642798));
#15050=CARTESIAN_POINT('Ctrl Pts',(-0.135174246449945,-0.06533764273189,
1.06247851744025));
#15051=CARTESIAN_POINT('Ctrl Pts',(-0.115079600404687,-0.0908043159161929,
1.06425052845252));
#15052=CARTESIAN_POINT('Ctrl Pts',(-0.0850581433982766,-0.128851596389654,
1.06689791782678));
#15053=CARTESIAN_POINT('Ctrl Pts',(-0.0342996944683099,-0.150536216937668,
1.06954530720104));
#15054=CARTESIAN_POINT('Ctrl Pts',(0.0139457694684962,-0.145925507476389,
1.0721926965753));
#15055=CARTESIAN_POINT('Ctrl Pts',(0.0621912334052997,-0.14131479801511,
1.07484008594956));
#15056=CARTESIAN_POINT('Ctrl Pts',(0.107923712348941,-0.110408758544542,
1.07748747532382));
#15057=CARTESIAN_POINT('Ctrl Pts',(0.1301953818052,-0.0673639426912374,
1.08013486469808));
#15058=CARTESIAN_POINT('Ctrl Pts',(0.15246705126146,-0.024319126837932,
1.08278225407234));
#15059=CARTESIAN_POINT('Ctrl Pts',(0.151277911230334,0.0308644653981125,
1.0854296434466));
#15060=CARTESIAN_POINT('Ctrl Pts',(0.127172648928576,0.0729099141598672,
1.08807703282086));
#15061=CARTESIAN_POINT('Ctrl Pts',(0.103067386626818,0.114955362921624,
1.09072442219512));
#15062=CARTESIAN_POINT('Ctrl Pts',(0.0560460020544268,0.143862668209093,
1.09337181156938));
#15063=CARTESIAN_POINT('Ctrl Pts',(0.00764670469074742,0.146390799320458,
1.09601920094364));
#15064=CARTESIAN_POINT('Ctrl Pts',(-0.0407525926729279,0.148918930431823,
1.0986665903179));
#15065=CARTESIAN_POINT('Ctrl Pts',(-0.0905298028278899,0.125067887367091,
1.10131397969216));
#15066=CARTESIAN_POINT('Ctrl Pts',(-0.11888440661962,0.0857626730052823,
1.10396136906642));
#15067=CARTESIAN_POINT('Ctrl Pts',(-0.136639133674055,0.0611510311732957,
1.10561907784952));
#15068=CARTESIAN_POINT('Ctrl Pts',(-0.145994366384503,0.0304800321277272,
1.10727678663261));
#15069=CARTESIAN_POINT('Ctrl Pts',(-0.146170555016798,-9.22629125885076E-5,
1.10893449541571));
#15070=CARTESIAN_POINT('Origin',(0.,0.,0.));
#15071=CARTESIAN_POINT('',(-0.146577386142569,-3.88073511912723E-5,1.16606550458429));
#15072=CARTESIAN_POINT('',(-0.146552328192774,-6.73160170860698E-5,1.15893449541571));
#15073=CARTESIAN_POINT('',(-0.14635,-1.79227059055215E-17,0.));
#15074=CARTESIAN_POINT('Ctrl Pts',(-0.146577386142569,-3.88073511912723E-5,
1.16606550458429));
#15075=CARTESIAN_POINT('Ctrl Pts',(-0.146413350709018,0.0463056768050285,
1.16353456384924));
#15076=CARTESIAN_POINT('Ctrl Pts',(-0.122574225104448,0.0927954474992645,
1.1610036231142));
#15077=CARTESIAN_POINT('Ctrl Pts',(-0.0847742546295189,0.119590709008994,
1.15847268237915));
#15078=CARTESIAN_POINT('Ctrl Pts',(-0.0452509303920754,0.147607604138013,
1.15582635250005));
#15079=CARTESIAN_POINT('Ctrl Pts',(0.00953524646069181,0.154093252855687,
1.15318002262095));
#15080=CARTESIAN_POINT('Ctrl Pts',(0.0545077808453859,0.136079071706768,
1.15053369274185));
#15081=CARTESIAN_POINT('Ctrl Pts',(0.0994803152300801,0.118064890557849,
1.14788736286275));
#15082=CARTESIAN_POINT('Ctrl Pts',(0.134639207146701,0.0755508795423365,
1.14524103298364));
#15083=CARTESIAN_POINT('Ctrl Pts',(0.14389167861853,0.027996370364851,1.14259470310454));
#15084=CARTESIAN_POINT('Ctrl Pts',(0.15314415009036,-0.0195581388126345,
1.13994837322544));
#15085=CARTESIAN_POINT('Ctrl Pts',(0.136490201117397,-0.0721531461520931,
1.13730204334634));
#15086=CARTESIAN_POINT('Ctrl Pts',(0.101552606157185,-0.105715089329518,
1.13465571346724));
#15087=CARTESIAN_POINT('Ctrl Pts',(0.0666150111969725,-0.139277032506943,
1.13200938358813));
#15088=CARTESIAN_POINT('Ctrl Pts',(0.0133937702495101,-0.153805911522335,
1.12936305370903));
#15089=CARTESIAN_POINT('Ctrl Pts',(-0.033750917386428,-0.142651629870951,
1.12671672382993));
#15090=CARTESIAN_POINT('Ctrl Pts',(-0.0808956050223675,-0.131497348219567,
1.12407039395083));
#15091=CARTESIAN_POINT('Ctrl Pts',(-0.121963739346782,-0.094659905901407,
1.12142406407173));
#15092=CARTESIAN_POINT('Ctrl Pts',(-0.1381577891642,-0.0490003798202082,
1.11877773419262));
#15093=CARTESIAN_POINT('Ctrl Pts',(-0.143690228857438,-0.0334015285560649,
1.11787365765651));
#15094=CARTESIAN_POINT('Ctrl Pts',(-0.146319518115206,-0.0167730178360648,
1.1169695811204));
#15095=CARTESIAN_POINT('Ctrl Pts',(-0.146204073634541,-0.000109175101205505,
1.11606550458429));
#15096=CARTESIAN_POINT('Ctrl Pts',(-0.146170555016798,-9.22629125885076E-5,
1.10893449541571));
#15097=CARTESIAN_POINT('Ctrl Pts',(-0.146275742653821,-0.0183444476975235,
1.10992417600687));
#15098=CARTESIAN_POINT('Ctrl Pts',(-0.143109248288425,-0.0365614514641733,
1.11091385659804));
#15099=CARTESIAN_POINT('Ctrl Pts',(-0.136505188007283,-0.0534328725168923,
1.1119035371892));
#15100=CARTESIAN_POINT('Ctrl Pts',(-0.118839368174718,-0.0985638180183679,
1.11455092656346));
#15101=CARTESIAN_POINT('Ctrl Pts',(-0.0765757310810901,-0.134066323362434,
1.11719831593772));
#15102=CARTESIAN_POINT('Ctrl Pts',(-0.0290731934694857,-0.143678417446031,
1.11984570531198));
#15103=CARTESIAN_POINT('Ctrl Pts',(0.01842934414212,-0.153290511529629,
1.12249309468624));
#15104=CARTESIAN_POINT('Ctrl Pts',(0.071170782271703,-0.137012194352758,
1.1251404840605));
#15105=CARTESIAN_POINT('Ctrl Pts',(0.10499283308901,-0.102299771349957,
1.12778787343476));
#15106=CARTESIAN_POINT('Ctrl Pts',(0.138814883906317,-0.0675873483471558,
1.13043526280902));
#15107=CARTESIAN_POINT('Ctrl Pts',(0.153717547411349,-0.0144408195184256,
1.13308265218328));
#15108=CARTESIAN_POINT('Ctrl Pts',(0.142874638214406,0.0327959749574983,
1.13573004155754));
#15109=CARTESIAN_POINT('Ctrl Pts',(0.132031729017462,0.0800327694334235,
1.1383774309318));
#15110=CARTESIAN_POINT('Ctrl Pts',(0.0954432471185425,0.121359829556542,
1.14102482030606));
#15111=CARTESIAN_POINT('Ctrl Pts',(0.0498685966661331,0.137847238945365,
1.14367220968032));
#15112=CARTESIAN_POINT('Ctrl Pts',(0.00429394621372511,0.154334648334189,
1.14631959905458));
#15113=CARTESIAN_POINT('Ctrl Pts',(-0.0502668727921719,0.145982406988718,
1.14896698842884));
#15114=CARTESIAN_POINT('Ctrl Pts',(-0.0888222026239048,0.116616270474356,
1.1516143778031));
#15115=CARTESIAN_POINT('Ctrl Pts',(-0.124357782404925,0.0895501633622979,
1.1540544170073));
#15116=CARTESIAN_POINT('Ctrl Pts',(-0.146296868742479,0.0446329749882746,
1.15649445621151));
#15117=CARTESIAN_POINT('Ctrl Pts',(-0.146552328192774,-6.73160170860698E-5,
1.15893449541571));
#15118=CARTESIAN_POINT('Origin',(0.,0.,0.));
#15119=CARTESIAN_POINT('',(-0.146318311025392,0.000133437649768732,1.21606550458429));
#15120=CARTESIAN_POINT('',(-0.146373054956946,0.000132657382717961,1.20893449541571));
#15121=CARTESIAN_POINT('',(-0.14635,-1.79227059055215E-17,0.));
#15122=CARTESIAN_POINT('Ctrl Pts',(-0.146318311025392,0.000133437649768732,
1.21606550458429));
#15123=CARTESIAN_POINT('Ctrl Pts',(-0.146429658069886,0.0125190846592594,
1.21539220633629));
#15124=CARTESIAN_POINT('Ctrl Pts',(-0.144988168643405,0.0248791929292086,
1.21471890808829));
#15125=CARTESIAN_POINT('Ctrl Pts',(-0.141892968227885,0.0368102906365087,
1.21404560984029));
#15126=CARTESIAN_POINT('Ctrl Pts',(-0.129727599662405,0.083704249513052,
1.21139927996119));
#15127=CARTESIAN_POINT('Ctrl Pts',(-0.0920156607298113,0.123970842060419,
1.20875295008209));
#15128=CARTESIAN_POINT('Ctrl Pts',(-0.0460184991925076,0.139179415364965,
1.20610662020299));
#15129=CARTESIAN_POINT('Ctrl Pts',(-2.13376552038805E-5,0.15438798866951,
1.20346029032389));
#15130=CARTESIAN_POINT('Ctrl Pts',(0.0542610464868107,0.144538542731236,
1.20081396044478));
#15131=CARTESIAN_POINT('Ctrl Pts',(0.091982751999895,0.114139323915075,
1.19816763056568));
#15132=CARTESIAN_POINT('Ctrl Pts',(0.129704457512977,0.0837401050989159,
1.19552130068658));
#15133=CARTESIAN_POINT('Ctrl Pts',(0.150865484397133,0.0327911134048729,
1.19287497080748));
#15134=CARTESIAN_POINT('Ctrl Pts',(0.145780097726084,-0.0153874961003253,
1.19022864092838));
#15135=CARTESIAN_POINT('Ctrl Pts',(0.140694711055036,-0.063566105605525,
1.18758231104927));
#15136=CARTESIAN_POINT('Ctrl Pts',(0.109362910828785,-0.108974332921877,
1.18493598117017));
#15137=CARTESIAN_POINT('Ctrl Pts',(0.0661257549466402,-0.130828118009858,
1.18228965129107));
#15138=CARTESIAN_POINT('Ctrl Pts',(0.0228885990644955,-0.152681903097838,
1.17964332141197));
#15139=CARTESIAN_POINT('Ctrl Pts',(-0.0322539124735426,-0.150981245957443,
1.17699699153287));
#15140=CARTESIAN_POINT('Ctrl Pts',(-0.0740621845924981,-0.126504564117865,
1.17435066165376));
#15141=CARTESIAN_POINT('Ctrl Pts',(-0.115870456711455,-0.102027882278287,
1.17170433177466));
#15142=CARTESIAN_POINT('Ctrl Pts',(-0.144344489411329,-0.0547751757395235,
1.16905800189556));
#15143=CARTESIAN_POINT('Ctrl Pts',(-0.146451269950206,-0.00637475169995868,
1.16641167201646));
#15144=CARTESIAN_POINT('Ctrl Pts',(-0.146543132875163,-0.00426432565444621,
1.1662962828724));
#15145=CARTESIAN_POINT('Ctrl Pts',(-0.146584864748453,-0.00215171749738942,
1.16618089372835));
#15146=CARTESIAN_POINT('Ctrl Pts',(-0.146577386142569,-3.88073511912723E-5,
1.16606550458429));
#15147=CARTESIAN_POINT('Ctrl Pts',(-0.146552328192774,-6.73160170860698E-5,
1.15893449541571));
#15148=CARTESIAN_POINT('Ctrl Pts',(-0.146574036680232,-0.00386586684592084,
1.15914184558577));
#15149=CARTESIAN_POINT('Ctrl Pts',(-0.1464391612665,-0.00766285139452399,
1.15934919575582));
#15150=CARTESIAN_POINT('Ctrl Pts',(-0.146142739258869,-0.0114471821958193,
1.15955654592588));
#15151=CARTESIAN_POINT('Ctrl Pts',(-0.142358105404532,-0.0597644666683822,
1.16220393530014));
#15152=CARTESIAN_POINT('Ctrl Pts',(-0.112238997038288,-0.106019003930254,
1.1648513246744));
#15153=CARTESIAN_POINT('Ctrl Pts',(-0.0695815129186611,-0.129023839960917,
1.16749871404866));
#15154=CARTESIAN_POINT('Ctrl Pts',(-0.026924028799035,-0.15202867599158,
1.17014610342292));
#15155=CARTESIAN_POINT('Ctrl Pts',(0.0282718310739737,-0.151783810791035,
1.17279349279718));
#15156=CARTESIAN_POINT('Ctrl Pts',(0.0707235276354612,-0.128401405199111,
1.17544088217144));
#15157=CARTESIAN_POINT('Ctrl Pts',(0.11317522419695,-0.105018999607187,
1.1780882715457));
#15158=CARTESIAN_POINT('Ctrl Pts',(0.142882757446916,-0.0584990536238821,
1.18073566091996));
#15159=CARTESIAN_POINT('Ctrl Pts',(0.146238551171451,-0.0101500920973681,
1.18338305029422));
#15160=CARTESIAN_POINT('Ctrl Pts',(0.149594344895986,0.0381988694291446,
1.18603043966848));
#15161=CARTESIAN_POINT('Ctrl Pts',(0.12659839909509,0.0883768464988665,
1.18867782904274));
#15162=CARTESIAN_POINT('Ctrl Pts',(0.0877840381772113,0.117399748124142,
1.191325218417));
#15163=CARTESIAN_POINT('Ctrl Pts',(0.0489696772593311,0.146422649749419,
1.19397260779126));
#15164=CARTESIAN_POINT('Ctrl Pts',(-0.00566309877553352,0.154290475930249,
1.19661999716552));
#15165=CARTESIAN_POINT('Ctrl Pts',(-0.0510896721842483,0.137399358129564,
1.19926738653978));
#15166=CARTESIAN_POINT('Ctrl Pts',(-0.0965162455929618,0.12050824032888,
1.20191477591404));
#15167=CARTESIAN_POINT('Ctrl Pts',(-0.132736616375526,0.0788581785466829,
1.2045621652883));
#15168=CARTESIAN_POINT('Ctrl Pts',(-0.143159994183491,0.0315270405159292,
1.20720955466256));
#15169=CARTESIAN_POINT('Ctrl Pts',(-0.145423823013163,0.021247302336111,
1.20778453491361));
#15170=CARTESIAN_POINT('Ctrl Pts',(-0.146470795531708,0.0106995851133921,
1.20835951516466));
#15171=CARTESIAN_POINT('Ctrl Pts',(-0.146373054956946,0.000132657382717961,
1.20893449541571));
#15172=CARTESIAN_POINT('Origin',(0.,0.,0.));
#15173=CARTESIAN_POINT('',(-0.146120596765396,-4.14129048147555E-5,1.26606550458429));
#15174=CARTESIAN_POINT('',(-0.146109918970638,-1.0198006988139E-5,1.25893449541571));
#15175=CARTESIAN_POINT('',(-0.14635,-1.79227059055215E-17,0.));
#15176=CARTESIAN_POINT('Ctrl Pts',(-0.146120596765396,-4.14129048147555E-5,
1.26606550458429));
#15177=CARTESIAN_POINT('Ctrl Pts',(-0.14605219935785,0.0269443530192317,
1.26460351894424));
#15178=CARTESIAN_POINT('Ctrl Pts',(-0.138898723445843,0.053963836666407,
1.26314153330418));
#15179=CARTESIAN_POINT('Ctrl Pts',(-0.124882896249422,0.0767650581554474,
1.26167954766413));
#15180=CARTESIAN_POINT('Ctrl Pts',(-0.0995129464537159,0.118037388097231,
1.25903321778503));
#15181=CARTESIAN_POINT('Ctrl Pts',(-0.051658938874944,0.145488850208621,
1.25638688790592));
#15182=CARTESIAN_POINT('Ctrl Pts',(-0.00322440565727106,0.146554478394238,
1.25374055802682));
#15183=CARTESIAN_POINT('Ctrl Pts',(0.0452101275604033,0.147620106579856,
1.25109422814772));
#15184=CARTESIAN_POINT('Ctrl Pts',(0.0942251864169787,0.122299900839699,
1.24844789826862));
#15185=CARTESIAN_POINT('Ctrl Pts',(0.121385807331354,0.0821833176976391,
1.24580156838952));
#15186=CARTESIAN_POINT('Ctrl Pts',(0.148546428245729,0.0420667345555804,
1.24315523851041));
#15187=CARTESIAN_POINT('Ctrl Pts',(0.153852611217905,-0.0128462259883804,
1.24050890863131));
#15188=CARTESIAN_POINT('Ctrl Pts',(0.134875632820701,-0.0574210379606392,
1.23786257875221));
#15189=CARTESIAN_POINT('Ctrl Pts',(0.115898654423498,-0.101995849932898,
1.23521624887311));
#15190=CARTESIAN_POINT('Ctrl Pts',(0.0726385146569148,-0.136232513333455,
1.23256991899401));
#15191=CARTESIAN_POINT('Ctrl Pts',(0.0248960600935515,-0.144460368686643,
1.2299235891149));
#15192=CARTESIAN_POINT('Ctrl Pts',(-0.0228463944698117,-0.152688224039831,
1.2272772592358));
#15193=CARTESIAN_POINT('Ctrl Pts',(-0.0750711638299551,-0.134907271345651,
1.2246309293567));
#15194=CARTESIAN_POINT('Ctrl Pts',(-0.107874149410843,-0.0992561323957017,
1.2219845994776));
#15195=CARTESIAN_POINT('Ctrl Pts',(-0.132331163880887,-0.072675612185966,
1.2200115678465));
#15196=CARTESIAN_POINT('Ctrl Pts',(-0.145992019903337,-0.0361614337449312,
1.21803853621539));
#15197=CARTESIAN_POINT('Ctrl Pts',(-0.146318311025392,0.000133437649768732,
1.21606550458429));
#15198=CARTESIAN_POINT('Ctrl Pts',(-0.146373054956946,0.000132657382717961,
1.20893449541571));
#15199=CARTESIAN_POINT('Ctrl Pts',(-0.146020767276673,-0.0379538636644633,
1.21100690453892));
#15200=CARTESIAN_POINT('Ctrl Pts',(-0.130797424420382,-0.0762899498869128,
1.21307931366213));
#15201=CARTESIAN_POINT('Ctrl Pts',(-0.104081054125652,-0.103227285106232,
1.21515172278534));
#15202=CARTESIAN_POINT('Ctrl Pts',(-0.0699523514264828,-0.137638258418326,
1.2177991121596));
#15203=CARTESIAN_POINT('Ctrl Pts',(-0.0170685611947798,-0.153447990763203,
1.22044650153386));
#15204=CARTESIAN_POINT('Ctrl Pts',(0.0303468241642401,-0.143414812629152,
1.22309389090812));
#15205=CARTESIAN_POINT('Ctrl Pts',(0.0777622095232573,-0.133381634495101,
1.22574128028238));
#15206=CARTESIAN_POINT('Ctrl Pts',(0.119709190009594,-0.0975055458821257,
1.22838866965664));
#15207=CARTESIAN_POINT('Ctrl Pts',(0.136973893871985,-0.052219638220276,
1.2310360590309));
#15208=CARTESIAN_POINT('Ctrl Pts',(0.154238597734379,-0.00693373055842239,
1.23368344840516));
#15209=CARTESIAN_POINT('Ctrl Pts',(0.146821024972825,0.0477619961523044,
1.23633083777942));
#15210=CARTESIAN_POINT('Ctrl Pts',(0.118118804930222,0.0868140895256425,
1.23897822715368));
#15211=CARTESIAN_POINT('Ctrl Pts',(0.0894165848876198,0.125866182898978,
1.24162561652794));
#15212=CARTESIAN_POINT('Ctrl Pts',(0.0394297175639698,0.149274642934924,
1.2442730059022));
#15213=CARTESIAN_POINT('Ctrl Pts',(-0.00894524413350711,0.146317192515786,
1.24692039527646));
#15214=CARTESIAN_POINT('Ctrl Pts',(-0.0573202058309854,0.143359742096648,
1.24956778465072));
#15215=CARTESIAN_POINT('Ctrl Pts',(-0.104083261902292,0.114036381222425,
1.25221517402498));
#15216=CARTESIAN_POINT('Ctrl Pts',(-0.127814530591109,0.0717787154251623,
1.25486256339924));
#15217=CARTESIAN_POINT('Ctrl Pts',(-0.139981499518435,0.0501133037087236,
1.2562198740714));
#15218=CARTESIAN_POINT('Ctrl Pts',(-0.146094355379323,0.0250479932723348,
1.25757718474355));
#15219=CARTESIAN_POINT('Ctrl Pts',(-0.146109918970638,-1.0198006988139E-5,
1.25893449541571));
#15220=CARTESIAN_POINT('Origin',(0.,0.,0.));
#15221=CARTESIAN_POINT('',(-0.146470135615938,-0.000111966546850736,1.31606550458429));
#15222=CARTESIAN_POINT('',(-0.146410535958061,-0.000127756381200432,1.30893449541571));
#15223=CARTESIAN_POINT('',(-0.14635,-1.79227059055215E-17,0.));
#15224=CARTESIAN_POINT('Ctrl Pts',(-0.146470135615938,-0.000111966546850736,
1.31606550458429));
#15225=CARTESIAN_POINT('Ctrl Pts',(-0.146120207411574,0.0411799307449602,
1.31381483155218));
#15226=CARTESIAN_POINT('Ctrl Pts',(-0.127827491572984,0.0827431563937987,
1.31156415852007));
#15227=CARTESIAN_POINT('Ctrl Pts',(-0.0969137672218927,0.10998333351997,
1.30931348548796));
#15228=CARTESIAN_POINT('Ctrl Pts',(-0.0605655677022408,0.142012194937238,
1.30666715560886));
#15229=CARTESIAN_POINT('Ctrl Pts',(-0.00676890401288169,0.154239532672684,
1.30402082572976));
#15230=CARTESIAN_POINT('Ctrl Pts',(0.0398526445220406,0.14106870189023,
1.30137449585066));
#15231=CARTESIAN_POINT('Ctrl Pts',(0.0864741930569617,0.127897871107775,
1.29872816597155));
#15232=CARTESIAN_POINT('Ctrl Pts',(0.125920626437448,0.0893288718074177,
1.29608183609245));
#15233=CARTESIAN_POINT('Ctrl Pts',(0.14013669149516,0.0430153417578024,
1.29343550621335));
#15234=CARTESIAN_POINT('Ctrl Pts',(0.154352756552873,-0.00329818829181684,
1.29078917633425));
#15235=CARTESIAN_POINT('Ctrl Pts',(0.143338453287813,-0.0573562490906975,
1.28814284645515));
#15236=CARTESIAN_POINT('Ctrl Pts',(0.112135201594409,-0.0944156157243562,
1.28549651657604));
#15237=CARTESIAN_POINT('Ctrl Pts',(0.0809319499010078,-0.131474982358013,
1.28285018669694));
#15238=CARTESIAN_POINT('Ctrl Pts',(0.0295397497792676,-0.151535654826449,
1.28020385681784));
#15239=CARTESIAN_POINT('Ctrl Pts',(-0.0185183802362589,-0.1454155477333,
1.27755752693874));
#15240=CARTESIAN_POINT('Ctrl Pts',(-0.066576510251784,-0.139295440640151,
1.27491119705964));
#15241=CARTESIAN_POINT('Ctrl Pts',(-0.111300570161094,-0.106994553985419,
1.27226486718053));
#15242=CARTESIAN_POINT('Ctrl Pts',(-0.13221965410943,-0.0632975117719662,
1.26961853730143));
#15243=CARTESIAN_POINT('Ctrl Pts',(-0.141581826511298,-0.0437412423069929,
1.26843419306239));
#15244=CARTESIAN_POINT('Ctrl Pts',(-0.146176005022067,-0.0219023912433209,
1.26724984882334));
#15245=CARTESIAN_POINT('Ctrl Pts',(-0.146120596765396,-4.14129048147555E-5,
1.26606550458429));
#15246=CARTESIAN_POINT('Ctrl Pts',(-0.146109918970638,-1.0198006988139E-5,
1.25893449541571));
#15247=CARTESIAN_POINT('Ctrl Pts',(-0.146124711647138,-0.0238271763493914,
1.26022457411781));
#15248=CARTESIAN_POINT('Ctrl Pts',(-0.140631289159497,-0.0476377233371588,
1.26151465281992));
#15249=CARTESIAN_POINT('Ctrl Pts',(-0.129592576141605,-0.0685164391025303,
1.26280473152202));
#15250=CARTESIAN_POINT('Ctrl Pts',(-0.106939871696956,-0.111361957112663,
1.26545212089628));
#15251=CARTESIAN_POINT('Ctrl Pts',(-0.0609349815013302,-0.141861022412626,
1.26809951027054));
#15252=CARTESIAN_POINT('Ctrl Pts',(-0.0126505083952331,-0.146043496451057,
1.2707468996448));
#15253=CARTESIAN_POINT('Ctrl Pts',(0.0356339647108625,-0.150225970489488,
1.27339428901906));
#15254=CARTESIAN_POINT('Ctrl Pts',(0.0861980207274291,-0.128091853266388,
1.27604167839332));
#15255=CARTESIAN_POINT('Ctrl Pts',(0.11588072467734,-0.0897797074320025,
1.27868906776758));
#15256=CARTESIAN_POINT('Ctrl Pts',(0.145563428627253,-0.0514675615976161,
1.28133645714184));
#15257=CARTESIAN_POINT('Ctrl Pts',(0.154364780510509,0.00302261284805656,
1.2839838465161));
#15258=CARTESIAN_POINT('Ctrl Pts',(0.138253309066183,0.0487315170146188,
1.28663123589036));
#15259=CARTESIAN_POINT('Ctrl Pts',(0.122141837621857,0.0944404211811797,
1.28927862526462));
#15260=CARTESIAN_POINT('Ctrl Pts',(0.0811175428499519,0.131368055068631,
1.29192601463888));
#15261=CARTESIAN_POINT('Ctrl Pts',(0.0339716590485425,0.142599665496764,
1.29457340401314));
#15262=CARTESIAN_POINT('Ctrl Pts',(-0.013174224752867,0.153831275924897,
1.2972207933874));
#15263=CARTESIAN_POINT('Ctrl Pts',(-0.0664416975837803,0.139366862893713,
1.29986818276166));
#15264=CARTESIAN_POINT('Ctrl Pts',(-0.101431520699135,0.105831870563862,
1.30251557213592));
#15265=CARTESIAN_POINT('Ctrl Pts',(-0.129710573305276,0.0787286237393239,
1.30465521322918));
#15266=CARTESIAN_POINT('Ctrl Pts',(-0.146050663974784,0.0391684733249047,
1.30679485432245));
#15267=CARTESIAN_POINT('Ctrl Pts',(-0.146410535958061,-0.000127756381200432,
1.30893449541571));
#15268=CARTESIAN_POINT('Origin',(0.,0.,0.));
#15269=CARTESIAN_POINT('',(-0.146471469669193,0.000111495080380188,1.36606550458429));
#15270=CARTESIAN_POINT('',(-0.146526884620975,8.5711493927648E-5,1.35893449541571));
#15271=CARTESIAN_POINT('',(-0.14635,-1.79227059055215E-17,0.));
#15272=CARTESIAN_POINT('Ctrl Pts',(-0.146471469669193,0.000111495080380188,
1.36606550458429));
#15273=CARTESIAN_POINT('Ctrl Pts',(-0.146532402405025,0.0073220458586883,
1.36567247403923));
#15274=CARTESIAN_POINT('Ctrl Pts',(-0.146045973070864,0.0145243451116175,
1.36527944349416));
#15275=CARTESIAN_POINT('Ctrl Pts',(-0.144983764805735,0.0216407019395156,
1.3648864129491));
#15276=CARTESIAN_POINT('Ctrl Pts',(-0.137831767320671,0.0695561322809842,
1.36224008307));
#15277=CARTESIAN_POINT('Ctrl Pts',(-0.104576727819841,0.113575347233418,
1.3595937531909));
#15278=CARTESIAN_POINT('Ctrl Pts',(-0.060440002550743,0.133550058215342,
1.3569474233118));
#15279=CARTESIAN_POINT('Ctrl Pts',(-0.0163032772816473,0.153524769197265,
1.35430109343269));
#15280=CARTESIAN_POINT('Ctrl Pts',(0.0387151337557165,0.149454976208681,
1.35165476355359));
#15281=CARTESIAN_POINT('Ctrl Pts',(0.0794324390145508,0.123203488242689,
1.34900843367449));
#15282=CARTESIAN_POINT('Ctrl Pts',(0.120149744273387,0.0969520002766962,
1.34636210379539));
#15283=CARTESIAN_POINT('Ctrl Pts',(0.146565943753694,0.048518817333291,
1.34371577391629));
#15284=CARTESIAN_POINT('Ctrl Pts',(0.14658992694451,7.25688577880009E-5,
1.34106944403718));
#15285=CARTESIAN_POINT('Ctrl Pts',(0.146613910135327,-0.0483736796177136,
1.33842311415808));
#15286=CARTESIAN_POINT('Ctrl Pts',(0.120245677036657,-0.0968329936253116,
1.33577678427898));
#15287=CARTESIAN_POINT('Ctrl Pts',(0.0795543829983497,-0.123124782547022,
1.33313045439988));
#15288=CARTESIAN_POINT('Ctrl Pts',(0.0388630889600415,-0.149416571468734,
1.33048412452078));
#15289=CARTESIAN_POINT('Ctrl Pts',(-0.0161512660179049,-0.153540835304554,
1.32783779464168));
#15290=CARTESIAN_POINT('Ctrl Pts',(-0.0603077462478081,-0.133609833714981,
1.32519146476257));
#15291=CARTESIAN_POINT('Ctrl Pts',(-0.10446422647771,-0.113678832125408,
1.32254513488347));
#15292=CARTESIAN_POINT('Ctrl Pts',(-0.137762831959571,-0.0696925651104417,
1.31989880500437));
#15293=CARTESIAN_POINT('Ctrl Pts',(-0.144962267025529,-0.0217842390534145,
1.31725247512527));
#15294=CARTESIAN_POINT('Ctrl Pts',(-0.146038665626028,-0.0146213916011371,
1.31685681827827));
#15295=CARTESIAN_POINT('Ctrl Pts',(-0.146531651210624,-0.00737087161912708,
1.31646116143128));
#15296=CARTESIAN_POINT('Ctrl Pts',(-0.146470135615938,-0.000111966546850736,
1.31606550458429));
#15297=CARTESIAN_POINT('Ctrl Pts',(-0.146410535958061,-0.000127756381200432,
1.30893449541571));
#15298=CARTESIAN_POINT('Ctrl Pts',(-0.146495935505426,-0.00945296197092968,
1.30944224369671));
#15299=CARTESIAN_POINT('Ctrl Pts',(-0.145681427739287,-0.018763305174839,
1.3099499919777));
#15300=CARTESIAN_POINT('Ctrl Pts',(-0.143913007029536,-0.0278887903271487,
1.3104577402587));
#15301=CARTESIAN_POINT('Ctrl Pts',(-0.134692496844786,-0.0754688872597875,
1.31310512963296));
#15302=CARTESIAN_POINT('Ctrl Pts',(-0.0995393030754929,-0.118023509496548,
1.31575251900722));
#15303=CARTESIAN_POINT('Ctrl Pts',(-0.0545553941775042,-0.136060454153345,
1.31839990838148));
#15304=CARTESIAN_POINT('Ctrl Pts',(-0.00957148527951295,-0.154097398810142,
1.32104729775574));
#15305=CARTESIAN_POINT('Ctrl Pts',(0.0452431387471776,-0.14761666588697,
1.32369468713));
#15306=CARTESIAN_POINT('Ctrl Pts',(0.0847805644327026,-0.119586763955155,
1.32634207650426));
#15307=CARTESIAN_POINT('Ctrl Pts',(0.124317990118227,-0.09155686202334,
1.32898946587852));
#15308=CARTESIAN_POINT('Ctrl Pts',(0.148578217462589,-0.041977791082884,
1.33163685525278));
#15309=CARTESIAN_POINT('Ctrl Pts',(0.146448816178573,0.00644068764408242,
1.33428424462704));
#15310=CARTESIAN_POINT('Ctrl Pts',(0.144319414894557,0.0548591663710502,
1.3369316340013));
#15311=CARTESIAN_POINT('Ctrl Pts',(0.115800384982161,0.102117052884526,
1.33957902337556));
#15312=CARTESIAN_POINT('Ctrl Pts',(0.0739549070570988,0.126567807678519,
1.34222641274982));
#15313=CARTESIAN_POINT('Ctrl Pts',(0.0321094291320376,0.151018562472512,
1.34487380212408));
#15314=CARTESIAN_POINT('Ctrl Pts',(-0.0230624968056921,0.152662185547021,
1.34752119149834));
#15315=CARTESIAN_POINT('Ctrl Pts',(-0.0662892946253695,0.1307458130856,
1.3501685808726));
#15316=CARTESIAN_POINT('Ctrl Pts',(-0.109516092445046,0.10882944062418,
1.35281597024686));
#15317=CARTESIAN_POINT('Ctrl Pts',(-0.140797762146673,0.0633530726268328,
1.35546335962112));
#15318=CARTESIAN_POINT('Ctrl Pts',(-0.145805692234247,0.0151472216574969,
1.35811074899538));
#15319=CARTESIAN_POINT('Ctrl Pts',(-0.146325105122407,0.0101474034011793,
1.35838533113549));
#15320=CARTESIAN_POINT('Ctrl Pts',(-0.146561879835735,0.00511822289583405,
1.3586599132756));
#15321=CARTESIAN_POINT('Ctrl Pts',(-0.146526884620975,8.5711493927648E-5,
1.35893449541571));
#15322=CARTESIAN_POINT('Origin',(0.,0.,0.));
#15323=CARTESIAN_POINT('',(-0.146120987371435,4.2191387702159E-5,1.41606550458429));
#15324=CARTESIAN_POINT('',(-0.146148882937928,7.6306569664006E-5,1.40893449541571));
#15325=CARTESIAN_POINT('',(-0.14635,-1.79227059055215E-17,0.));
#15326=CARTESIAN_POINT('Ctrl Pts',(-0.146120987371435,4.2191387702159E-5,
1.41606550458429));
#15327=CARTESIAN_POINT('Ctrl Pts',(-0.146177309023295,0.021854523983563,
1.41488378664717));
#15328=CARTESIAN_POINT('Ctrl Pts',(-0.141604359564088,0.0436444172696427,
1.41370206871005));
#15329=CARTESIAN_POINT('Ctrl Pts',(-0.132282279973341,0.0631665524487371,
1.41252035077294));
#15330=CARTESIAN_POINT('Ctrl Pts',(-0.1114064880593,0.106884268839086,1.40987402089383));
#15331=CARTESIAN_POINT('Ctrl Pts',(-0.0667143915920224,0.139229456738304,
1.40722769101473));
#15332=CARTESIAN_POINT('Ctrl Pts',(-0.0186623352932378,0.145397151366753,
1.40458136113563));
#15333=CARTESIAN_POINT('Ctrl Pts',(0.0293897210055454,0.151564845995202,
1.40193503125653));
#15334=CARTESIAN_POINT('Ctrl Pts',(0.0808017371358351,0.131555047352884,
1.39928870137743));
#15335=CARTESIAN_POINT('Ctrl Pts',(0.112041660826149,0.0945265884816804,
1.39664237149832));
#15336=CARTESIAN_POINT('Ctrl Pts',(0.143281584516463,0.0574981296104763,
1.39399604161922));
#15337=CARTESIAN_POINT('Ctrl Pts',(0.154349415766802,0.00345101051038574,
1.39134971174012));
#15338=CARTESIAN_POINT('Ctrl Pts',(0.140179214932283,-0.0428765696854336,
1.38870338186102));
#15339=CARTESIAN_POINT('Ctrl Pts',(0.126009014097764,-0.089204149881253,
1.38605705198192));
#15340=CARTESIAN_POINT('Ctrl Pts',(0.0866007811783877,-0.127812191172801,
1.38341072210282));
#15341=CARTESIAN_POINT('Ctrl Pts',(0.0399922944706322,-0.14102917638501,
1.38076439222371));
#15342=CARTESIAN_POINT('Ctrl Pts',(-0.00661619223712474,-0.15424616159722,
1.37811806234461));
#15343=CARTESIAN_POINT('Ctrl Pts',(-0.060424932733261,-0.142072090730089,
1.37547173246551));
#15344=CARTESIAN_POINT('Ctrl Pts',(-0.0968048252466797,-0.110079232431271,
1.37282540258641));
#15345=CARTESIAN_POINT('Ctrl Pts',(-0.127781608685608,-0.08283792481198,
1.37057210325237));
#15346=CARTESIAN_POINT('Ctrl Pts',(-0.146122133733866,-0.0412276055847571,
1.36831880391833));
#15347=CARTESIAN_POINT('Ctrl Pts',(-0.146471469669193,0.000111495080380188,
1.36606550458429));
#15348=CARTESIAN_POINT('Ctrl Pts',(-0.146526884620975,8.5711493927648E-5,
1.35893449541571));
#15349=CARTESIAN_POINT('Ctrl Pts',(-0.146224472749943,-0.0434028397118431,
1.36130730264986));
#15350=CARTESIAN_POINT('Ctrl Pts',(-0.125627402569456,-0.0871401285467012,
1.36368010988401));
#15351=CARTESIAN_POINT('Ctrl Pts',(-0.0917490966422633,-0.114327780902106,
1.36605291711816));
#15352=CARTESIAN_POINT('Ctrl Pts',(-0.0539503804891888,-0.144661598551044,
1.36870030649242));
#15353=CARTESIAN_POINT('Ctrl Pts',(0.00038124229047478,-0.154393899907594,
1.37134769586668));
#15354=CARTESIAN_POINT('Ctrl Pts',(0.0463590973565905,-0.139066790892088,
1.37399508524094));
#15355=CARTESIAN_POINT('Ctrl Pts',(0.0923369524227062,-0.123739681876581,
1.3766424746152));
#15356=CARTESIAN_POINT('Ctrl Pts',(0.129961039775272,-0.083353162489017,
1.37928986398946));
#15357=CARTESIAN_POINT('Ctrl Pts',(0.141997595260484,-0.0364063334065561,
1.38193725336372));
#15358=CARTESIAN_POINT('Ctrl Pts',(0.154034150745695,0.0105404956759021,
1.38458464273798));
#15359=CARTESIAN_POINT('Ctrl Pts',(0.140483174363557,0.0640476344532581,
1.38723203211224));
#15360=CARTESIAN_POINT('Ctrl Pts',(0.10755170844225,0.0996060653705087,
1.3898794214865));
#15361=CARTESIAN_POINT('Ctrl Pts',(0.0746202425209409,0.135164496287762,
1.39252681086076));
#15362=CARTESIAN_POINT('Ctrl Pts',(0.0223082870604623,0.152774219344908,
1.39517420023502));
#15363=CARTESIAN_POINT('Ctrl Pts',(-0.025422593472234,0.144369075867769,
1.39782158960928));
#15364=CARTESIAN_POINT('Ctrl Pts',(-0.073153474004929,0.135963932390631,
1.40046897898354));
#15365=CARTESIAN_POINT('Ctrl Pts',(-0.11630327960984,0.101543922379208,
1.4031163683578));
#15366=CARTESIAN_POINT('Ctrl Pts',(-0.135107186188192,0.0568751802851974,
1.40576375773206));
#15367=CARTESIAN_POINT('Ctrl Pts',(-0.142614236437708,0.0390421576584788,
1.40682067029328));
#15368=CARTESIAN_POINT('Ctrl Pts',(-0.14624095998336,0.0195756595648056,
1.40787758285449));
#15369=CARTESIAN_POINT('Ctrl Pts',(-0.146148882937928,7.6306569664006E-5,
1.40893449541571));
#15370=CARTESIAN_POINT('Origin',(0.,0.,0.));
#15371=CARTESIAN_POINT('',(-0.14631473222987,-0.000131398079681141,1.46606550458429));
#15372=CARTESIAN_POINT('',(-0.146248097568756,-0.000123763188177425,1.45893449541571));
#15373=CARTESIAN_POINT('',(-0.14635,-1.79227059055215E-17,0.));
#15374=CARTESIAN_POINT('Ctrl Pts',(-0.14631473222987,-0.000131398079681141,
1.46606550458429));
#15375=CARTESIAN_POINT('Ctrl Pts',(-0.145989697979493,0.0361157155227289,
1.46409509925512));
#15376=CARTESIAN_POINT('Ctrl Pts',(-0.132370868650209,0.0725796635271419,
1.46212469392594));
#15377=CARTESIAN_POINT('Ctrl Pts',(-0.107973319296019,0.0991484059484618,
1.46015428859677));
#15378=CARTESIAN_POINT('Ctrl Pts',(-0.0752064754000165,0.134831245351468,
1.45750795871767));
#15379=CARTESIAN_POINT('Ctrl Pts',(-0.0229974942306327,0.152665588379184,
1.45486162883857));
#15380=CARTESIAN_POINT('Ctrl Pts',(0.0247535192036911,0.144485406820094,
1.45221529895946));
#15381=CARTESIAN_POINT('Ctrl Pts',(0.0725045326380122,0.136305225261004,
1.44956896908036));
#15382=CARTESIAN_POINT('Ctrl Pts',(0.115797578337275,0.102110519115111,
1.44692263920126));
#15383=CARTESIAN_POINT('Ctrl Pts',(0.134818450998255,0.0575543070937695,
1.44427630932216));
#15384=CARTESIAN_POINT('Ctrl Pts',(0.153839323659235,0.0129980950724284,
1.44162997944306));
#15385=CARTESIAN_POINT('Ctrl Pts',(0.148588023281934,-0.0419196228243577,
1.43898364956396));
#15386=CARTESIAN_POINT('Ctrl Pts',(0.121467255745355,-0.082062966762292,
1.43633731968485));
#15387=CARTESIAN_POINT('Ctrl Pts',(0.0943464882087764,-0.122206310700226,
1.43369098980575));
#15388=CARTESIAN_POINT('Ctrl Pts',(0.0453562535129183,-0.147575280679306,
1.43104465992665));
#15389=CARTESIAN_POINT('Ctrl Pts',(-0.00307937473935208,-0.146557666176543,
1.42839833004755));
#15390=CARTESIAN_POINT('Ctrl Pts',(-0.0515150029916225,-0.14554005167378,
1.42575200016845));
#15391=CARTESIAN_POINT('Ctrl Pts',(-0.0993960248003067,-0.118135852689175,
1.42310567028934));
#15392=CARTESIAN_POINT('Ctrl Pts',(-0.124806792024246,-0.0768886307561326,
1.42045934041024));
#15393=CARTESIAN_POINT('Ctrl Pts',(-0.138870387581649,-0.0540603453281256,
1.41899472846826));
#15394=CARTESIAN_POINT('Ctrl Pts',(-0.146051182757901,-0.0269918425378075,
1.41753011652627));
#15395=CARTESIAN_POINT('Ctrl Pts',(-0.146120987371435,4.2191387702159E-5,
1.41606550458429));
#15396=CARTESIAN_POINT('Ctrl Pts',(-0.146148882937928,7.6306569664006E-5,
1.40893449541571));
#15397=CARTESIAN_POINT('Ctrl Pts',(-0.146010322369016,-0.0292669616874671,
1.41052497222875));
#15398=CARTESIAN_POINT('Ctrl Pts',(-0.137450455640384,-0.0586846305953837,
1.4121154490418));
#15399=CARTESIAN_POINT('Ctrl Pts',(-0.121019719714466,-0.0827222215753489,
1.41370592585484));
#15400=CARTESIAN_POINT('Ctrl Pts',(-0.0936703391105966,-0.122733407165291,
1.4163533152291));
#15401=CARTESIAN_POINT('Ctrl Pts',(-0.0445135703510636,-0.147838304168576,
1.41900070460336));
#15402=CARTESIAN_POINT('Ctrl Pts',(0.00393424939099551,-0.146537573651384,
1.42164809397762));
#15403=CARTESIAN_POINT('Ctrl Pts',(0.0523820691330518,-0.145236843134192,
1.42429548335188));
#15404=CARTESIAN_POINT('Ctrl Pts',(0.100120939857634,-0.117530485096527,
1.42694287272614));
#15405=CARTESIAN_POINT('Ctrl Pts',(0.125284029446909,-0.0761094471358441,
1.4295902621004));
#15406=CARTESIAN_POINT('Ctrl Pts',(0.150447119036187,-0.0346884091751576,
1.43223765147466));
#15407=CARTESIAN_POINT('Ctrl Pts',(0.153034427490153,0.020447308708549,
1.43488504084892));
#15408=CARTESIAN_POINT('Ctrl Pts',(0.13186079120536,0.0640427391611241,
1.43753243022318));
#15409=CARTESIAN_POINT('Ctrl Pts',(0.110687154920568,0.107638169613697,
1.44017981959744));
#15410=CARTESIAN_POINT('Ctrl Pts',(0.0657525738970213,0.139693312635139,
1.4428272089717));
#15411=CARTESIAN_POINT('Ctrl Pts',(0.0176394768514684,0.145525221357757,
1.44547459834596));
#15412=CARTESIAN_POINT('Ctrl Pts',(-0.0304736201940859,0.151357130080375,
1.44812198772022));
#15413=CARTESIAN_POINT('Ctrl Pts',(-0.0817652332616461,0.130965804504167,
1.45076937709448));
#15414=CARTESIAN_POINT('Ctrl Pts',(-0.112741325423428,0.0936916042199666,
1.45341676646874));
#15415=CARTESIAN_POINT('Ctrl Pts',(-0.134261605244105,0.0677957870194472,
1.45525600945106));
#15416=CARTESIAN_POINT('Ctrl Pts',(-0.145976367207401,0.0337512577971725,
1.45709525243339));
#15417=CARTESIAN_POINT('Ctrl Pts',(-0.146248097568756,-0.000123763188177425,
1.45893449541571));
#15418=CARTESIAN_POINT('Origin',(0.,0.,-0.0924367114736175));
#15419=CARTESIAN_POINT('',(-0.117746618301147,-0.000105742458702955,1.48256328852638));
#15420=CARTESIAN_POINT('',(-0.117971241274414,-5.28325160115065E-6,1.49243671147361));
#15421=CARTESIAN_POINT('',(-0.117775,2.85464118895969E-14,-0.0924367114736175));
#15422=CARTESIAN_POINT('',(-0.117668597464313,0.00500517689812599,1.532225));
#15423=CARTESIAN_POINT('Ctrl Pts',(-0.117746618301147,-0.000105742458702949,
1.48256328852638));
#15424=CARTESIAN_POINT('Ctrl Pts',(-0.117836347163251,-0.0101121102621826,
1.48323921307631));
#15425=CARTESIAN_POINT('Ctrl Pts',(-0.112089674709738,-0.0591937430214443,
1.48656146750534));
#15426=CARTESIAN_POINT('Ctrl Pts',(-0.0435804807853106,-0.132222740314769,
1.49253005181348));
#15427=CARTESIAN_POINT('Ctrl Pts',(0.0874774386997331,-0.108286040948335,
1.50046904145078));
#15428=CARTESIAN_POINT('Ctrl Pts',(0.138385550162814,0.0147146982980264,
1.50840803108809));
#15429=CARTESIAN_POINT('Ctrl Pts',(0.0627460642121078,0.124368470664037,
1.51634702072539));
#15430=CARTESIAN_POINT('Ctrl Pts',(-0.0706026869052757,0.119928391791904,
1.5242860103627));
#15431=CARTESIAN_POINT('Ctrl Pts',(-0.116004137797729,0.0441355889673283,
1.5295786701209));
#15432=CARTESIAN_POINT('Ctrl Pts',(-0.117668597464313,0.00500517689812487,
1.532225));
#15433=CARTESIAN_POINT('',(-0.0334019664627544,0.1129391839063,1.53222500000001));
#15434=CARTESIAN_POINT('Origin',(0.,0.,1.532225));
#15435=CARTESIAN_POINT('Ctrl Pts',(-0.117971276761593,-5.28420699491729E-6,
1.49243671147361));
#15436=CARTESIAN_POINT('Ctrl Pts',(-0.117971582784674,-0.000385634193345565,
1.49246252744444));
#15437=CARTESIAN_POINT('Ctrl Pts',(-0.117794795258817,-0.0397700451254522,
1.49513573278954));
#15438=CARTESIAN_POINT('Ctrl Pts',(-0.0742871760264013,-0.117748889605885,
1.50045632750888));
#15439=CARTESIAN_POINT('Ctrl Pts',(0.0586284551779338,-0.126233948370975,
1.50839849563167));
#15440=CARTESIAN_POINT('Ctrl Pts',(0.137995068118234,-0.019163470063063,
1.51634066375444));
#15441=CARTESIAN_POINT('Ctrl Pts',(0.0906261803825392,0.105639137646141,
1.52428283187723));
#15442=CARTESIAN_POINT('Ctrl Pts',(0.00417072711528833,0.124051375507138,
1.52957761062575));
#15443=CARTESIAN_POINT('Ctrl Pts',(-0.0334019664627544,0.1129391839063,
1.53222500000001));
#15444=CARTESIAN_POINT('Origin',(0.,0.,-0.0924367114736175));
#15445=CARTESIAN_POINT('',(-0.117590702341447,3.3953472435133E-5,1.43256328852638));
#15446=CARTESIAN_POINT('',(-0.117692994131604,-9.95982882293356E-5,1.44243671147361));
#15447=CARTESIAN_POINT('',(-0.117775,2.85464118895969E-14,-0.0924367114736175));
#15448=CARTESIAN_POINT('Ctrl Pts',(-0.117590702341447,3.39534724351446E-5,
1.43256328852638));
#15449=CARTESIAN_POINT('Ctrl Pts',(-0.117534527156218,-0.0217216553118358,
1.43402790046837));
#15450=CARTESIAN_POINT('Ctrl Pts',(-0.101314495966545,-0.0828641818343832,
1.43813884228945));
#15451=CARTESIAN_POINT('Ctrl Pts',(-0.00292444232197888,-0.139176693688359,
1.44489611398964));
#15452=CARTESIAN_POINT('Ctrl Pts',(0.115350068603298,-0.0779297424218237,
1.45283510362695));
#15453=CARTESIAN_POINT('Ctrl Pts',(0.128028003046829,0.0546551750765237,
1.46077409326425));
#15454=CARTESIAN_POINT('Ctrl Pts',(0.0235079116789307,0.137209630484779,
1.46871308290156));
#15455=CARTESIAN_POINT('Ctrl Pts',(-0.0918059616614023,0.0978189523496558,
1.47597614798894));
#15456=CARTESIAN_POINT('Ctrl Pts',(-0.117485047349053,0.0290640819657798,
1.48059288319721));
#15457=CARTESIAN_POINT('Ctrl Pts',(-0.117746618301147,-0.000105742458702949,
1.48256328852638));
#15458=CARTESIAN_POINT('Ctrl Pts',(-0.117692994131604,-9.9598288229346E-5,
1.44243671147361));
#15459=CARTESIAN_POINT('Ctrl Pts',(-0.117789077779518,-0.0120777797952868,
1.44324485786555));
#15460=CARTESIAN_POINT('Ctrl Pts',(-0.110597905189529,-0.0631824179582176,
1.44670039363175));
#15461=CARTESIAN_POINT('Ctrl Pts',(-0.0368790902657646,-0.134252921254984,
1.45280331877221));
#15462=CARTESIAN_POINT('Ctrl Pts',(0.0928396680879532,-0.103751556080299,
1.46074548689499));
#15463=CARTESIAN_POINT('Ctrl Pts',(0.137511141307062,0.0217950526079239,
1.46868765501776));
#15464=CARTESIAN_POINT('Ctrl Pts',(0.0562018483347667,0.127378648737854,
1.47662982314055));
#15465=CARTESIAN_POINT('Ctrl Pts',(-0.0761502833827582,0.1162998103107,
1.48454617529249));
#15466=CARTESIAN_POINT('Ctrl Pts',(-0.117940200573233,0.0386186906477724,
1.48981513807018));
#15467=CARTESIAN_POINT('Ctrl Pts',(-0.117971276761593,-5.28420699491729E-6,
1.49243671147361));
#15468=CARTESIAN_POINT('Origin',(0.,0.,-0.0924367114736175));
#15469=CARTESIAN_POINT('',(-0.117872752581409,8.97255421561373E-5,1.38256328852638));
#15470=CARTESIAN_POINT('',(-0.117613151267609,6.14076272390171E-5,1.39243671147361));
#15471=CARTESIAN_POINT('',(-0.117775,2.85464118895969E-14,-0.0924367114736175));
#15472=CARTESIAN_POINT('Ctrl Pts',(-0.117872752581409,8.97255421561322E-5,
1.38256328852638));
#15473=CARTESIAN_POINT('Ctrl Pts',(-0.117591624875346,-0.0331778698171688,
1.38481658786042));
#15474=CARTESIAN_POINT('Ctrl Pts',(-0.0854981695600773,-0.105990339321694,
1.38971621707357));
#15475=CARTESIAN_POINT('Ctrl Pts',(0.0379781508110965,-0.133926497290667,
1.39726217616581));
#15476=CARTESIAN_POINT('Ctrl Pts',(0.133119345865688,-0.0407171622080862,
1.40520116580311));
#15477=CARTESIAN_POINT('Ctrl Pts',(0.106398871137127,0.0897659150453452,
1.41314015544042));
#15478=CARTESIAN_POINT('Ctrl Pts',(-0.0177224175491345,0.138074504763813,
1.42107914507772));
#15479=CARTESIAN_POINT('Ctrl Pts',(-0.105714817800915,0.0743914165933911,
1.42755352277305));
#15480=CARTESIAN_POINT('Ctrl Pts',(-0.11763602712824,0.0175874039095825,
1.43138157058926));
#15481=CARTESIAN_POINT('Ctrl Pts',(-0.117590702341447,3.39534724351446E-5,
1.43256328852638));
#15482=CARTESIAN_POINT('Ctrl Pts',(-0.117613151267609,6.1407627239024E-5,
1.39243671147361));
#15483=CARTESIAN_POINT('Ctrl Pts',(-0.117501644803633,-0.0235525549213426,
1.39402718828666));
#15484=CARTESIAN_POINT('Ctrl Pts',(-0.0991469449676741,-0.0866320980727062,
1.39826505447396));
#15485=CARTESIAN_POINT('Ctrl Pts',(0.00373660876362508,-0.139175849115243,
1.40515031003553));
#15486=CARTESIAN_POINT('Ctrl Pts',(0.118990018389619,-0.0722858665142316,
1.41309247815831));
#15487=CARTESIAN_POINT('Ctrl Pts',(0.125236419206141,0.0608253567263532,
1.42103464628109));
#15488=CARTESIAN_POINT('Ctrl Pts',(0.0167532566496359,0.13821437898841,
1.42897681440387));
#15489=CARTESIAN_POINT('Ctrl Pts',(-0.0944771051913143,0.0939940009069027,
1.43611083613471));
#15490=CARTESIAN_POINT('Ctrl Pts',(-0.117474319425011,0.0271612872365273,
1.44059746849129));
#15491=CARTESIAN_POINT('Ctrl Pts',(-0.117692994131604,-9.9598288229346E-5,
1.44243671147361));
#15492=CARTESIAN_POINT('Origin',(0.,0.,-0.0924367114736175));
#15493=CARTESIAN_POINT('',(-0.117871679003533,-9.01049542302267E-5,1.33256328852638));
#15494=CARTESIAN_POINT('',(-0.117917347702326,6.89762296073142E-5,1.34243671147361));
#15495=CARTESIAN_POINT('',(-0.117775,2.85464118895969E-14,-0.0924367114736175));
#15496=CARTESIAN_POINT('Ctrl Pts',(-0.117871679003533,-9.01049542302501E-5,
1.33256328852638));
#15497=CARTESIAN_POINT('Ctrl Pts',(-0.117921183610054,-0.00593170075121234,
1.33295894537338));
#15498=CARTESIAN_POINT('Ctrl Pts',(-0.114870949065289,-0.0507926200311143,
1.33600093209947));
#15499=CARTESIAN_POINT('Ctrl Pts',(-0.0572704544775333,-0.126880813469472,
1.34168924870467));
#15500=CARTESIAN_POINT('Ctrl Pts',(0.0755477687720905,-0.116923823242002,
1.34962823834197));
#15501=CARTESIAN_POINT('Ctrl Pts',(0.13920718769651,6.89141801743488E-5,
1.35756722797928));
#15502=CARTESIAN_POINT('Ctrl Pts',(0.0754319660950179,0.116998564767658,
1.36550621761658));
#15503=CARTESIAN_POINT('Ctrl Pts',(-0.0573960494825499,0.126824048933643,
1.37344520725389));
#15504=CARTESIAN_POINT('Ctrl Pts',(-0.11489462347839,0.0507140179075799,
1.37913089755716));
#15505=CARTESIAN_POINT('Ctrl Pts',(-0.117921788132912,0.00589240827474643,
1.38217025798132));
#15506=CARTESIAN_POINT('Ctrl Pts',(-0.117872752581409,8.97255421561322E-5,
1.38256328852638));
#15507=CARTESIAN_POINT('Ctrl Pts',(-0.117917347702326,6.89762296073276E-5,
1.34243671147361));
#15508=CARTESIAN_POINT('Ctrl Pts',(-0.117673982084908,-0.0349283870656527,
1.34480951870776));
#15509=CARTESIAN_POINT('Ctrl Pts',(-0.0826049238592893,-0.109396528181867,
1.34982971531618));
#15510=CARTESIAN_POINT('Ctrl Pts',(0.0440301174146577,-0.132080378229483,
1.35749730129884));
#15511=CARTESIAN_POINT('Ctrl Pts',(0.13486394497766,-0.0345773583278084,
1.36543946942163));
#15512=CARTESIAN_POINT('Ctrl Pts',(0.102148545386143,0.0946020732301706,
1.3733816375444));
#15513=CARTESIAN_POINT('Ctrl Pts',(-0.0241454188302812,0.137116288461919,
1.38132380566719));
#15514=CARTESIAN_POINT('Ctrl Pts',(-0.107458038693719,0.07065895059964,
1.38767549697692));
#15515=CARTESIAN_POINT('Ctrl Pts',(-0.117687250167678,0.015753490298928,
1.3913797989124));
#15516=CARTESIAN_POINT('Ctrl Pts',(-0.117613151267609,6.1407627239024E-5,
1.39243671147361));
#15517=CARTESIAN_POINT('Origin',(0.,0.,-0.0924367114736175));
#15518=CARTESIAN_POINT('',(-0.117590388001671,-3.33269891443968E-5,1.28256328852638));
#15519=CARTESIAN_POINT('',(-0.117823716245033,-0.000102811805890834,1.29243671147362));
#15520=CARTESIAN_POINT('',(-0.117775,2.85464118895969E-14,-0.0924367114736175));
#15521=CARTESIAN_POINT('Ctrl Pts',(-0.117590388001671,-3.33269891444124E-5,
1.28256328852638));
#15522=CARTESIAN_POINT('Ctrl Pts',(-0.117634977734708,-0.017625925033684,
1.28374763276543));
#15523=CARTESIAN_POINT('Ctrl Pts',(-0.105676786131388,-0.0744702911817869,
1.28757830688358));
#15524=CARTESIAN_POINT('Ctrl Pts',(-0.0175857351491984,-0.138091953858251,
1.29405531088083));
#15525=CARTESIAN_POINT('Ctrl Pts',(0.106487712804436,-0.089660542174548,
1.30199430051814));
#15526=CARTESIAN_POINT('Ctrl Pts',(0.133078957772855,0.0408489510387311,
1.30993329015544));
#15527=CARTESIAN_POINT('Ctrl Pts',(0.0378455373822902,0.133964029124136,
1.31787227979275));
#15528=CARTESIAN_POINT('Ctrl Pts',(-0.0855601048685178,0.105915403748908,
1.32541561258306));
#15529=CARTESIAN_POINT('Ctrl Pts',(-0.117590074669608,0.0331395035428114,
1.33031261549427));
#15530=CARTESIAN_POINT('Ctrl Pts',(-0.117871679003533,-9.01049542302501E-5,
1.33256328852638));
#15531=CARTESIAN_POINT('Ctrl Pts',(-0.117823716245033,-0.000102811805890825,
1.29243671147362));
#15532=CARTESIAN_POINT('Ctrl Pts',(-0.117892441435953,-0.00760726064997237,
1.29294445975461));
#15533=CARTESIAN_POINT('Ctrl Pts',(-0.113819337750002,-0.0541654333254181,
1.29609959740987));
#15534=CARTESIAN_POINT('Ctrl Pts',(-0.0518146499729274,-0.129225073214149,
1.30190212443939));
#15535=CARTESIAN_POINT('Ctrl Pts',(0.0805213734929343,-0.11357898534207,
1.30984429256217));
#15536=CARTESIAN_POINT('Ctrl Pts',(0.1390915465469,0.0061171215252809,1.31778646068495));
#15537=CARTESIAN_POINT('Ctrl Pts',(0.0702395735793815,0.120209316621791,
1.32572862880773));
#15538=CARTESIAN_POINT('Ctrl Pts',(-0.0629590648350173,0.124177428154433,
1.33367079693051));
#15539=CARTESIAN_POINT('Ctrl Pts',(-0.115917830154768,0.0471875384414626,
1.33924015781913));
#15540=CARTESIAN_POINT('Ctrl Pts',(-0.117945510062545,0.00411888419242175,
1.3421621293335));
#15541=CARTESIAN_POINT('Ctrl Pts',(-0.117917347702326,6.89762296073276E-5,
1.34243671147361));
#15542=CARTESIAN_POINT('Origin',(0.,0.,-0.0924367114736175));
#15543=CARTESIAN_POINT('',(-0.11774949833287,0.000107383800510985,1.23256328852638));
#15544=CARTESIAN_POINT('',(-0.117581795058195,-8.20683476789735E-6,1.24243671147361));
#15545=CARTESIAN_POINT('',(-0.117775,2.85464118895969E-14,-0.0924367114736175));
#15546=CARTESIAN_POINT('Ctrl Pts',(-0.11774949833287,0.000107383800510997,
1.23256328852638));
#15547=CARTESIAN_POINT('Ctrl Pts',(-0.1174869159147,-0.0291008736543001,
1.23453632015749));
#15548=CARTESIAN_POINT('Ctrl Pts',(-0.0917482398636095,-0.0978979247776974,
1.23915568166769));
#15549=CARTESIAN_POINT('Ctrl Pts',(0.0236422145726536,-0.137184880695923,
1.246421373057));
#15550=CARTESIAN_POINT('Ctrl Pts',(0.128082862902196,-0.0545291301253663,
1.2543603626943));
#15551=CARTESIAN_POINT('Ctrl Pts',(0.115272428336817,0.0780443019497631,
1.26229935233161));
#15552=CARTESIAN_POINT('Ctrl Pts',(-0.00306201423577413,0.139173524314926,
1.27023834196891));
#15553=CARTESIAN_POINT('Ctrl Pts',(-0.101358337705897,0.08278581645186,
1.27699298736717));
#15554=CARTESIAN_POINT('Ctrl Pts',(-0.117535345263889,0.02168343817453,
1.28110130288633));
#15555=CARTESIAN_POINT('Ctrl Pts',(-0.117590388001671,-3.33269891444124E-5,
1.28256328852638));
#15556=CARTESIAN_POINT('Ctrl Pts',(-0.117581795058195,-8.20683476789562E-6,
1.24243671147361));
#15557=CARTESIAN_POINT('Ctrl Pts',(-0.117593699448189,-0.0191748937105988,
1.24372679017572));
#15558=CARTESIAN_POINT('Ctrl Pts',(-0.104100832827715,-0.0776580224685839,
1.24766425825208));
#15559=CARTESIAN_POINT('Ctrl Pts',(-0.0120149744006178,-0.138706589206355,
1.25424911570271));
#15560=CARTESIAN_POINT('Ctrl Pts',(0.110059129405696,-0.0852693704304675,
1.26219128382548));
#15561=CARTESIAN_POINT('Ctrl Pts',(0.13130776387206,0.0462833517151888,
1.27013345194827));
#15562=CARTESIAN_POINT('Ctrl Pts',(0.0322649968732001,0.135435768819968,
1.27807562007105));
#15563=CARTESIAN_POINT('Ctrl Pts',(-0.0881142830049797,0.102747609761224,
1.28551003991283));
#15564=CARTESIAN_POINT('Ctrl Pts',(-0.117534109666069,0.0315207854174475,
1.29029707038035));
#15565=CARTESIAN_POINT('Ctrl Pts',(-0.117823716245033,-0.000102811805890825,
1.29243671147362));
#15566=CARTESIAN_POINT('Origin',(0.,0.,-0.0924367114736175));
#15567=CARTESIAN_POINT('',(-0.117957988745754,-3.12301727557783E-5,1.18256328852638));
#15568=CARTESIAN_POINT('',(-0.117793553451004,0.000106755881474893,1.19243671147362));
#15569=CARTESIAN_POINT('',(-0.117775,2.85464118895969E-14,-0.0924367114736175));
#15570=CARTESIAN_POINT('Ctrl Pts',(-0.117957988745754,-3.12301727557569E-5,
1.18256328852638));
#15571=CARTESIAN_POINT('Ctrl Pts',(-0.117964007145535,-0.00173159226684161,
1.18267867767044));
#15572=CARTESIAN_POINT('Ctrl Pts',(-0.117160216762375,-0.0424221720604921,
1.1854403966936));
#15573=CARTESIAN_POINT('Ctrl Pts',(-0.0703321751825429,-0.12013338809653,
1.19084844559586));
#15574=CARTESIAN_POINT('Ctrl Pts',(0.0627954496153871,-0.124239193932754,
1.19878743523316));
#15575=CARTESIAN_POINT('Ctrl Pts',(0.138438143943654,-0.0146125323915816,
1.20672642487047));
#15576=CARTESIAN_POINT('Ctrl Pts',(0.0873502052771435,0.108390901091839,
1.21466541450777));
#15577=CARTESIAN_POINT('Ctrl Pts',(-0.043700859820065,0.132169893139269,
1.22260440414508));
#15578=CARTESIAN_POINT('Ctrl Pts',(-0.112119660921406,0.0591163174148552,
1.22857036215128));
#15579=CARTESIAN_POINT('Ctrl Pts',(-0.117839104743291,0.0100747194789664,
1.23188999027838));
#15580=CARTESIAN_POINT('Ctrl Pts',(-0.11774949833287,0.000107383800510997,
1.23256328852638));
#15581=CARTESIAN_POINT('Ctrl Pts',(-0.117793553451004,0.000106755881474891,
1.19243671147362));
#15582=CARTESIAN_POINT('Ctrl Pts',(-0.117510050331475,-0.0305433296418112,
1.19450912059683));
#15583=CARTESIAN_POINT('Ctrl Pts',(-0.0896091397727994,-0.100804620014092,
1.19922891909429));
#15584=CARTESIAN_POINT('Ctrl Pts',(0.0288222657999454,-0.136209964735594,
1.20659610696603));
#15585=CARTESIAN_POINT('Ctrl Pts',(0.130092623711363,-0.0495962373069701,
1.21453827508881));
#15586=CARTESIAN_POINT('Ctrl Pts',(0.112184773380136,0.082452738709893,
1.22248044321158));
#15587=CARTESIAN_POINT('Ctrl Pts',(-0.00849585454694533,0.138966535376798,
1.23042261133437));
#15588=CARTESIAN_POINT('Ctrl Pts',(-0.103054997843392,0.079672038485689,
1.23707470075504));
#15589=CARTESIAN_POINT('Ctrl Pts',(-0.11756927027536,0.0201573447738481,
1.24107940080146));
#15590=CARTESIAN_POINT('Ctrl Pts',(-0.117581795058195,-8.20683476789562E-6,
1.24243671147361));
#15591=CARTESIAN_POINT('Origin',(0.,0.,-0.0924367114736175));
#15592=CARTESIAN_POINT('',(-0.117657565919426,-8.78585414499747E-5,1.13256328852638));
#15593=CARTESIAN_POINT('',(-0.117937823388479,-5.4172489969917E-5,1.14243671147362));
#15594=CARTESIAN_POINT('',(-0.117775,2.85464118895969E-14,-0.0924367114736175));
#15595=CARTESIAN_POINT('Ctrl Pts',(-0.117657565919426,-8.78585414499974E-5,
1.13256328852638));
#15596=CARTESIAN_POINT('Ctrl Pts',(-0.11775046973706,-0.0134980674796043,
1.13346736506249));
#15597=CARTESIAN_POINT('Ctrl Pts',(-0.109441032251172,-0.0660497484721492,
1.13701777147771));
#15598=CARTESIAN_POINT('Ctrl Pts',(-0.0320511128216771,-0.13546723577438,
1.14321450777202));
#15599=CARTESIAN_POINT('Ctrl Pts',(0.0964380908528195,-0.100390938007982,
1.15115349740933));
#15600=CARTESIAN_POINT('Ctrl Pts',(0.136644831685568,0.0265863832644056,
1.15909248704664));
#15601=CARTESIAN_POINT('Ctrl Pts',(0.0517625939920979,0.129225692742072,
1.16703147668394));
#15602=CARTESIAN_POINT('Ctrl Pts',(-0.0785823129332351,0.113795317289389,
1.17485507717719));
#15603=CARTESIAN_POINT('Ctrl Pts',(-0.117825981412732,0.0372644419932696,
1.18003234779134));
#15604=CARTESIAN_POINT('Ctrl Pts',(-0.117957988745754,-3.12301727557569E-5,
1.18256328852638));
#15605=CARTESIAN_POINT('Ctrl Pts',(-0.117937823388479,-5.41724899699178E-5,
1.14243671147362));
#15606=CARTESIAN_POINT('Ctrl Pts',(-0.117955293269658,-0.0031110520517566,
1.14264406164367));
#15607=CARTESIAN_POINT('Ctrl Pts',(-0.116460933142332,-0.0451799670343263,
1.14549880118799));
#15608=CARTESIAN_POINT('Ctrl Pts',(-0.0660858892268601,-0.122541963197144,
1.15100093010657));
#15609=CARTESIAN_POINT('Ctrl Pts',(0.0671705316110708,-0.121950798202395,
1.15894309822935));
#15610=CARTESIAN_POINT('Ctrl Pts',(0.138891844802359,-0.00964017357273747,
1.16688526635212));
#15611=CARTESIAN_POINT('Ctrl Pts',(0.0833739592533277,0.111501840422208,
1.17482743447491));
#15612=CARTESIAN_POINT('Ctrl Pts',(-0.0485230383040216,0.130496713571114,
1.18276960259768));
#15613=CARTESIAN_POINT('Ctrl Pts',(-0.113150295826959,0.0561813708375219,
1.18863936159726));
#15614=CARTESIAN_POINT('Ctrl Pts',(-0.117872210070015,0.00861047923971886,
1.19186173122257));
#15615=CARTESIAN_POINT('Ctrl Pts',(-0.117793553451004,0.000106755881474891,
1.19243671147362));
#15616=CARTESIAN_POINT('Origin',(0.,0.,-0.0924367114736175));
#15617=CARTESIAN_POINT('',(-0.117641451221435,8.0229283111194E-5,1.08256328852638));
#15618=CARTESIAN_POINT('',(-0.117630591849015,-7.42484764288953E-5,1.09243671147362));
#15619=CARTESIAN_POINT('',(-0.117775,2.85464118895969E-14,-0.0924367114736175));
#15620=CARTESIAN_POINT('Ctrl Pts',(-0.117641451221435,8.02292831111745E-5,
1.08256328852638));
#15621=CARTESIAN_POINT('Ctrl Pts',(-0.117483998834985,-0.0250372639622414,
1.08425605245455));
#15622=CARTESIAN_POINT('Ctrl Pts',(-0.0972946570053161,-0.0896524615425008,
1.08859514626182));
#15623=CARTESIAN_POINT('Ctrl Pts',(0.00904258428980543,-0.13891320121148,
1.09558056994819));
#15624=CARTESIAN_POINT('Ctrl Pts',(0.121617839487272,-0.067732908692211,
1.1035195595855));
#15625=CARTESIAN_POINT('Ctrl Pts',(0.122860297649024,0.0654522196953821,
1.1114585492228));
#15626=CARTESIAN_POINT('Ctrl Pts',(0.0116325734791967,0.138720326685422,
1.11939753886011));
#15627=CARTESIAN_POINT('Ctrl Pts',(-0.096364912740844,0.0911171059582243,
1.1264324519613));
#15628=CARTESIAN_POINT('Ctrl Pts',(-0.117478530206868,0.0257550656131636,
1.13082103518339));
#15629=CARTESIAN_POINT('Ctrl Pts',(-0.117657565919426,-8.78585414499974E-5,
1.13256328852638));
#15630=CARTESIAN_POINT('Ctrl Pts',(-0.117630591849015,-7.42484764288814E-5,
1.09243671147362));
#15631=CARTESIAN_POINT('Ctrl Pts',(-0.117715241483118,-0.0147626739157663,
1.09342639206478));
#15632=CARTESIAN_POINT('Ctrl Pts',(-0.108350501834675,-0.0686384992808382,
1.0970634620302));
#15633=CARTESIAN_POINT('Ctrl Pts',(-0.0276126195379174,-0.136460326620484,
1.10334792136989));
#15634=CARTESIAN_POINT('Ctrl Pts',(0.0997182217817603,-0.0971604536002107,
1.11129008949267));
#15635=CARTESIAN_POINT('Ctrl Pts',(0.135696927507188,0.0311483765905046,
1.11923225761545));
#15636=CARTESIAN_POINT('Ctrl Pts',(0.0473633069609982,0.130922093830007,
1.12717442573822));
#15637=CARTESIAN_POINT('Ctrl Pts',(-0.0809210029008042,0.111284164335459,
1.13490924369095));
#15638=CARTESIAN_POINT('Ctrl Pts',(-0.117732242679493,0.0359183370635313,
1.13999667226941));
#15639=CARTESIAN_POINT('Ctrl Pts',(-0.117937823388479,-5.41724899699178E-5,
1.14243671147362));
#15640=CARTESIAN_POINT('Origin',(0.,0.,-0.0924367114736175));
#15641=CARTESIAN_POINT('',(-0.117948158721073,4.38502512853227E-5,1.03256328852638));
#15642=CARTESIAN_POINT('',(-0.117667547954054,9.20194976846214E-5,1.04243671147362));
#15643=CARTESIAN_POINT('',(-0.117775,2.85464118895969E-14,-0.0924367114736175));
#15644=CARTESIAN_POINT('Ctrl Pts',(-0.117948158721073,4.38502512853157E-5,
1.03256328852638));
#15645=CARTESIAN_POINT('Ctrl Pts',(-0.117773439871091,-0.0365306738650768,
1.03504473984661));
#15646=CARTESIAN_POINT('Ctrl Pts',(-0.0798690478914953,-0.112422454385097,
1.04017252104593));
#15647=CARTESIAN_POINT('Ctrl Pts',(0.0493427524230464,-0.130168884856471,
1.04794663212436));
#15648=CARTESIAN_POINT('Ctrl Pts',(0.136125055048066,-0.0291310004912345,
1.05588562176166));
#15649=CARTESIAN_POINT('Ctrl Pts',(0.0982941990358779,0.0985743183458784,
1.06382461139897));
#15650=CARTESIAN_POINT('Ctrl Pts',(-0.0295182596522469,0.136041604476578,
1.07176360103627));
#15651=CARTESIAN_POINT('Ctrl Pts',(-0.108818061611988,0.067537217334308,
1.07800982674541));
#15652=CARTESIAN_POINT('Ctrl Pts',(-0.11773014713001,0.0142293884972668,
1.08160972257545));
#15653=CARTESIAN_POINT('Ctrl Pts',(-0.117641451221435,8.02292831111745E-5,
1.08256328852638));
#15654=CARTESIAN_POINT('Ctrl Pts',(-0.117667547954054,9.20194976846197E-5,
1.04243671147362));
#15655=CARTESIAN_POINT('Ctrl Pts',(-0.117475882803567,-0.0261866690710452,
1.04420872248589));
#15656=CARTESIAN_POINT('Ctrl Pts',(-0.0957916308421219,-0.0920126959480487,
1.04862812287242));
#15657=CARTESIAN_POINT('Ctrl Pts',(0.0132451643780021,-0.13859452774087,
1.05569491263321));
#15658=CARTESIAN_POINT('Ctrl Pts',(0.123654649330263,-0.0639797248987874,
1.06363708075599));
#15659=CARTESIAN_POINT('Ctrl Pts',(0.120783771971213,0.0692470788374567,
1.07157924887876));
#15660=CARTESIAN_POINT('Ctrl Pts',(0.00726255089817806,0.139036444335888,
1.07952141700155));
#15661=CARTESIAN_POINT('Ctrl Pts',(-0.0979368667310299,0.0886295245336828,
1.08647390453316));
#15662=CARTESIAN_POINT('Ctrl Pts',(-0.117488804242801,0.0245287720112504,
1.09077900269052));
#15663=CARTESIAN_POINT('Ctrl Pts',(-0.117630591849015,-7.42484764288814E-5,
1.09243671147362));
#15664=CARTESIAN_POINT('Origin',(0.,0.,-0.0924367114736175));
#15665=CARTESIAN_POINT('',(-0.117771476475648,-0.000107683352847938,0.982563288526384));
#15666=CARTESIAN_POINT('',(-0.11796176292438,2.53781033017321E-5,0.992436711473616));
#15667=CARTESIAN_POINT('',(-0.117775,2.85464118895969E-14,-0.0924367114736175));
#15668=CARTESIAN_POINT('Ctrl Pts',(-0.117771476475648,-0.000107683352847945,
0.982563288526384));
#15669=CARTESIAN_POINT('Ctrl Pts',(-0.117856103358663,-0.00933799346614349,
0.983187097359559));
#15670=CARTESIAN_POINT('Ctrl Pts',(-0.112646870919438,-0.057630810124202,
0.986457236071836));
#15671=CARTESIAN_POINT('Ctrl Pts',(-0.0461590140787468,-0.131331607851033,
0.992373704663214));
#15672=CARTESIAN_POINT('Ctrl Pts',(0.0853128637208732,-0.110001641284132,
1.00031269430052));
#15673=CARTESIAN_POINT('Ctrl Pts',(0.138686661656432,0.0120272889735618,
1.00825168393783));
#15674=CARTESIAN_POINT('Ctrl Pts',(0.0651023256631918,0.123046060459907,
1.01619067357513));
#15675=CARTESIAN_POINT('Ctrl Pts',(-0.0680787277209358,0.121424596492465,
1.02412966321244));
#15676=CARTESIAN_POINT('Ctrl Pts',(-0.116790117880403,0.0438975063746073,
1.02958720152952));
#15677=CARTESIAN_POINT('Ctrl Pts',(-0.11795976781127,0.00247402277930658,
1.0323984099675));
#15678=CARTESIAN_POINT('Ctrl Pts',(-0.117948158721073,4.38502512853157E-5,
1.03256328852638));
#15679=CARTESIAN_POINT('Ctrl Pts',(-0.11796176292438,2.53781033017319E-5,
0.992436711473616));
#15680=CARTESIAN_POINT('Ctrl Pts',(-0.117851518882229,-0.0376119105440478,
0.994991052906992));
#15681=CARTESIAN_POINT('Ctrl Pts',(-0.077958511321084,-0.114458475672252,
1.00019278371463));
#15682=CARTESIAN_POINT('Ctrl Pts',(0.0529591494285269,-0.128760265574912,
1.00804190389653));
#15683=CARTESIAN_POINT('Ctrl Pts',(0.136912761112491,-0.0252739657289669,
1.0159840720193));
#15684=CARTESIAN_POINT('Ctrl Pts',(0.0954402180350474,0.101365883217864,
1.02392624014209));
#15685=CARTESIAN_POINT('Ctrl Pts',(-0.0334653697086341,0.135144169424284,
1.03186840826486));
#15686=CARTESIAN_POINT('Ctrl Pts',(-0.109792739119276,0.0652029671457737,
1.03803856537538));
#15687=CARTESIAN_POINT('Ctrl Pts',(-0.117762231070763,0.0130737646421874,
1.04156133311163));
#15688=CARTESIAN_POINT('Ctrl Pts',(-0.117667547954054,9.20194976846197E-5,
1.04243671147362));
#15689=CARTESIAN_POINT('Origin',(0.,0.,-0.0924367114736175));
#15690=CARTESIAN_POINT('',(-0.117585265278523,2.16484251076657E-5,0.932563288526384));
#15691=CARTESIAN_POINT('',(-0.117742563953077,-0.000107211314308964,0.942436711473616));
#15692=CARTESIAN_POINT('',(-0.117775,2.85464118895969E-14,-0.0924367114736175));
#15693=CARTESIAN_POINT('Ctrl Pts',(-0.117585265278523,2.16484251076635E-5,
0.932563288526384));
#15694=CARTESIAN_POINT('Ctrl Pts',(-0.117550805757046,-0.0209622679161363,
0.933975784751614));
#15695=CARTESIAN_POINT('Ctrl Pts',(-0.102172791552808,-0.0813069697478888,
0.938034610855947));
#15696=CARTESIAN_POINT('Ctrl Pts',(-0.00565790085648466,-0.139092177922979,
0.944739766839381));
#15697=CARTESIAN_POINT('Ctrl Pts',(0.113796373024222,-0.0801812402497705,
0.952678756476687));
#15698=CARTESIAN_POINT('Ctrl Pts',(0.129077866376032,0.0521301276928276,
0.960617746113992));
#15699=CARTESIAN_POINT('Ctrl Pts',(0.026197419344502,0.13671993644362,0.968556735751298));
#15700=CARTESIAN_POINT('Ctrl Pts',(-0.0906967139502387,0.0993396518733501,
0.975871916555428));
#15701=CARTESIAN_POINT('Ctrl Pts',(-0.117497098103867,0.02981894716558,
0.980540767480457));
#15702=CARTESIAN_POINT('Ctrl Pts',(-0.117771476475648,-0.000107683352847945,
0.982563288526384));
#15703=CARTESIAN_POINT('Ctrl Pts',(-0.117742563953077,-0.000107211314308957,
0.942436711473616));
#15704=CARTESIAN_POINT('Ctrl Pts',(-0.117833632602859,-0.0103126986533654,
0.943125993953839));
#15705=CARTESIAN_POINT('Ctrl Pts',(-0.111944766202914,-0.0596118697348184,
0.946462665808322));
#15706=CARTESIAN_POINT('Ctrl Pts',(-0.0428565117498991,-0.132465832952297,
0.952446727037066));
#15707=CARTESIAN_POINT('Ctrl Pts',(0.0880997963686447,-0.107806787258123,
0.960388895159846));
#15708=CARTESIAN_POINT('Ctrl Pts',(0.138347640177547,0.0156143509765511,
0.968331063282625));
#15709=CARTESIAN_POINT('Ctrl Pts',(0.061854832590724,0.124731139593481,
0.976273231405407));
#15710=CARTESIAN_POINT('Ctrl Pts',(-0.0713033562375951,0.119581390225944,
0.984215399528185));
#15711=CARTESIAN_POINT('Ctrl Pts',(-0.117322772537986,0.0417718924351975,
0.989603226217589));
#15712=CARTESIAN_POINT('Ctrl Pts',(-0.11796577882491,0.00139640554830399,
0.992343663532733));
#15713=CARTESIAN_POINT('Ctrl Pts',(-0.11796176292438,2.53781033017319E-5,
0.992436711473616));
#15714=CARTESIAN_POINT('Origin',(0.,0.,-0.0924367114736175));
#15715=CARTESIAN_POINT('',(-0.117850913371472,9.6525574830472E-5,0.882563288526384));
#15716=CARTESIAN_POINT('',(-0.117591231449503,3.54948526558943E-5,0.892436711473616));
#15717=CARTESIAN_POINT('',(-0.117775,2.85464118895969E-14,-0.0924367114736175));
#15718=CARTESIAN_POINT('Ctrl Pts',(-0.117850913371472,9.65255748304767E-5,
0.882563288526384));
#15719=CARTESIAN_POINT('Ctrl Pts',(-0.117563006813672,-0.0324172738354332,
0.884764472143669));
#15720=CARTESIAN_POINT('Ctrl Pts',(-0.0867151192651892,-0.104499852648429,
0.889611985640057));
#15721=CARTESIAN_POINT('Ctrl Pts',(0.0353397195745277,-0.134646760160997,
0.897105829015547));
#15722=CARTESIAN_POINT('Ctrl Pts',(0.132293719443212,-0.0433245611326863,
0.905044818652852));
#15723=CARTESIAN_POINT('Ctrl Pts',(0.108141885842356,0.0876583043865096,
0.912983808290157));
#15724=CARTESIAN_POINT('Ctrl Pts',(-0.0150064327997127,0.138395999855801,
0.920922797927463));
#15725=CARTESIAN_POINT('Ctrl Pts',(-0.104951114476159,0.0759553573435841,
0.927449291339539));
#15726=CARTESIAN_POINT('Ctrl Pts',(-0.117615366114572,0.01835136974357,
0.931329454872513));
#15727=CARTESIAN_POINT('Ctrl Pts',(-0.117585265278523,2.16484251076635E-5,
0.932563288526384));
#15728=CARTESIAN_POINT('Ctrl Pts',(-0.117591231449503,3.54948526559117E-5,
0.892436711473616));
#15729=CARTESIAN_POINT('Ctrl Pts',(-0.117532234588281,-0.0218238662162972,
0.893908324374946));
#15730=CARTESIAN_POINT('Ctrl Pts',(-0.101194437785642,-0.0830895288483654,
0.898027326650536));
#15731=CARTESIAN_POINT('Ctrl Pts',(-0.00250162451743248,-0.139203517821528,
0.904793718300386));
#15732=CARTESIAN_POINT('Ctrl Pts',(0.115632500949424,-0.0775435504945224,
0.912735886423165));
#15733=CARTESIAN_POINT('Ctrl Pts',(0.127835376168433,0.0551542754370876,
0.920678054545947));
#15734=CARTESIAN_POINT('Ctrl Pts',(0.0229279137899797,0.137325118854324,
0.928620222668725));
#15735=CARTESIAN_POINT('Ctrl Pts',(-0.0920562790907298,0.0974788594069619,
0.935873108311283));
#15736=CARTESIAN_POINT('Ctrl Pts',(-0.117483857027998,0.0288844367965532,
0.94047860457958));
#15737=CARTESIAN_POINT('Ctrl Pts',(-0.117742563953077,-0.000107211314308957,
0.942436711473616));
#15738=CARTESIAN_POINT('Origin',(0.,0.,-0.0924367114736175));
#15739=CARTESIAN_POINT('',(-0.11789232318732,-8.18790992476613E-5,0.832563288526384));
#15740=CARTESIAN_POINT('',(-0.117872825429845,8.99519344067963E-5,0.842436711473616));
#15741=CARTESIAN_POINT('',(-0.117775,2.85464118895969E-14,-0.0924367114736175));
#15742=CARTESIAN_POINT('Ctrl Pts',(-0.11789232318732,-8.18790992476734E-5,
0.832563288526384));
#15743=CARTESIAN_POINT('Ctrl Pts',(-0.117932494517479,-0.00515170743829337,
0.832906829656623));
#15744=CARTESIAN_POINT('Ctrl Pts',(-0.115332713682068,-0.0492334187378749,
0.835896700665964));
#15745=CARTESIAN_POINT('Ctrl Pts',(-0.059752088941783,-0.125731196083361,
0.841532901554406));
#15746=CARTESIAN_POINT('Ctrl Pts',(0.0732361146625898,-0.118385460722959,
0.849471891191712));
#15747=CARTESIAN_POINT('Ctrl Pts',(0.139181674492094,-0.00266594955618734,
0.857410880829018));
#15748=CARTESIAN_POINT('Ctrl Pts',(0.077715950067195,0.115494055719818,
0.865349870466323));
#15749=CARTESIAN_POINT('Ctrl Pts',(-0.0548934004223171,0.127927168308903,
0.87328886010363));
#15750=CARTESIAN_POINT('Ctrl Pts',(-0.114416768398411,0.0522742940766184,
0.879026666123649));
#15751=CARTESIAN_POINT('Ctrl Pts',(-0.117909136832228,0.0066718045071592,
0.882118142264567));
#15752=CARTESIAN_POINT('Ctrl Pts',(-0.117850913371472,9.65255748304767E-5,
0.882563288526384));
#15753=CARTESIAN_POINT('Ctrl Pts',(-0.117872825429845,8.99519344067998E-5,
0.842436711473616));
#15754=CARTESIAN_POINT('Ctrl Pts',(-0.117591169542271,-0.0331870933343037,
0.844690654796053));
#15755=CARTESIAN_POINT('Ctrl Pts',(-0.0854771005934613,-0.106025606004136,
0.84959198749275));
#15756=CARTESIAN_POINT('Ctrl Pts',(0.0380692928980519,-0.133920149482284,
0.857140709563706));
#15757=CARTESIAN_POINT('Ctrl Pts',(0.133179650076608,-0.0405839661022353,
0.865082877686486));
#15758=CARTESIAN_POINT('Ctrl Pts',(0.106283765719693,0.0899312995767124,
0.873025045809266));
#15759=CARTESIAN_POINT('Ctrl Pts',(-0.0179789669825735,0.138060255849953,
0.880967213932046));
#15760=CARTESIAN_POINT('Ctrl Pts',(-0.105798194743126,0.0742290978659706,
0.887437769153496));
#15761=CARTESIAN_POINT('Ctrl Pts',(-0.117638368248411,0.0175004969839459,
0.891260935000686));
#15762=CARTESIAN_POINT('Ctrl Pts',(-0.117591231449503,3.54948526559117E-5,
0.892436711473616));
#15763=CARTESIAN_POINT('Origin',(0.,0.,-0.0924367114736175));
#15764=CARTESIAN_POINT('',(-0.117598114366551,-4.51832715892789E-5,0.782563288526384));
#15765=CARTESIAN_POINT('',(-0.117874685330111,-8.92836445515327E-5,0.792436711473617));
#15766=CARTESIAN_POINT('',(-0.117775,2.85464118895969E-14,-0.0924367114736175));
#15767=CARTESIAN_POINT('Ctrl Pts',(-0.117598114366551,-4.518327158929E-5,
0.782563288526384));
#15768=CARTESIAN_POINT('Ctrl Pts',(-0.117656123976761,-0.0168608793038394,
0.783695517048678));
#15769=CARTESIAN_POINT('Ctrl Pts',(-0.106420815930739,-0.0729055463807818,
0.787474075450074));
#15770=CARTESIAN_POINT('Ctrl Pts',(-0.0202952816069424,-0.137719814645367,
0.793898963730571));
#15771=CARTESIAN_POINT('Ctrl Pts',(0.104705698854998,-0.0917352845351548,
0.801837953367879));
#15772=CARTESIAN_POINT('Ctrl Pts',(0.133855787965376,0.0382266115373486,
0.809776943005182));
#15773=CARTESIAN_POINT('Ctrl Pts',(0.0404700769297216,0.133194664588195,
0.81771593264249));
#15774=CARTESIAN_POINT('Ctrl Pts',(-0.0843190215395119,0.107398870964955,
0.825311381149555));
#15775=CARTESIAN_POINT('Ctrl Pts',(-0.117623050954756,0.0339016606582783,
0.830260499777521));
#15776=CARTESIAN_POINT('Ctrl Pts',(-0.11789232318732,-8.18790992476734E-5,
0.832563288526384));
#15777=CARTESIAN_POINT('Ctrl Pts',(-0.117874685330111,-8.9283644551537E-5,
0.792436711473617));
#15778=CARTESIAN_POINT('Ctrl Pts',(-0.11792303416021,-0.00583050672374999,
0.7928255958429));
#15779=CARTESIAN_POINT('Ctrl Pts',(-0.114931453360353,-0.0506053896743902,
0.795861869586443));
#15780=CARTESIAN_POINT('Ctrl Pts',(-0.0575513573065257,-0.126774282767806,
0.801545532704245));
#15781=CARTESIAN_POINT('Ctrl Pts',(0.0753527000357912,-0.117071978271622,
0.809487700827026));
#15782=CARTESIAN_POINT('Ctrl Pts',(0.139225942868322,-0.000119714417332432,
0.817429868949805));
#15783=CARTESIAN_POINT('Ctrl Pts',(0.0755539188089132,0.116942220141962,
0.825372037072586));
#15784=CARTESIAN_POINT('Ctrl Pts',(-0.0573332568284509,0.12687306712048,
0.833314205195366));
#15785=CARTESIAN_POINT('Ctrl Pts',(-0.114890414736801,0.0507419104293215,
0.839002429995709));
#15786=CARTESIAN_POINT('Ctrl Pts',(-0.117921990994851,0.00589875908008548,
0.842043265421793));
#15787=CARTESIAN_POINT('Ctrl Pts',(-0.117872825429845,8.99519344067998E-5,
0.842436711473616));
#15788=CARTESIAN_POINT('Origin',(0.,0.,-0.0924367114736175));
#15789=CARTESIAN_POINT('',(-0.11772691567491,0.000105512987197037,0.732563288526384));
#15790=CARTESIAN_POINT('',(-0.117591850253004,-3.65476421498312E-5,0.742436711473616));
#15791=CARTESIAN_POINT('',(-0.117775,2.85464118895969E-14,-0.0924367114736175));
#15792=CARTESIAN_POINT('Ctrl Pts',(-0.11772691567491,0.000105512987197042,
0.732563288526384));
#15793=CARTESIAN_POINT('Ctrl Pts',(-0.117479624464894,-0.0283451130369189,
0.734484204440733));
#15794=CARTESIAN_POINT('Ctrl Pts',(-0.0928318426870313,-0.096374559506161,
0.739051450234184));
#15795=CARTESIAN_POINT('Ctrl Pts',(0.0209425314183671,-0.137622876656644,
0.746265025906738));
#15796=CARTESIAN_POINT('Ctrl Pts',(0.126986869252672,-0.0570349089493802,
0.754204015544043));
#15797=CARTESIAN_POINT('Ctrl Pts',(0.11678343126468,0.0757646090434518,
0.762143005181349));
#15798=CARTESIAN_POINT('Ctrl Pts',(-0.000327234354877375,0.139206819944772,
0.770081994818654));
#15799=CARTESIAN_POINT('Ctrl Pts',(-0.100479183608201,0.0843410365921374,
0.776888755933667));
#15800=CARTESIAN_POINT('Ctrl Pts',(-0.117520539541507,0.0224420334666934,
0.781049187169576));
#15801=CARTESIAN_POINT('Ctrl Pts',(-0.117598114366551,-4.518327158929E-5,
0.782563288526384));
#15802=CARTESIAN_POINT('Ctrl Pts',(-0.117591850253004,-3.65476421498364E-5,
0.742436711473616));
#15803=CARTESIAN_POINT('Ctrl Pts',(-0.117640211257931,-0.0174335619022046,
0.743607926264006));
#15804=CARTESIAN_POINT('Ctrl Pts',(-0.105863856762799,-0.0740921523660566,
0.747426530428656));
#15805=CARTESIAN_POINT('Ctrl Pts',(-0.0182163644075178,-0.138029133036789,
0.753892523967566));
#15806=CARTESIAN_POINT('Ctrl Pts',(0.106128952536144,-0.0901139441634624,
0.761834692090347));
#15807=CARTESIAN_POINT('Ctrl Pts',(0.133249245915149,0.0403548753208232,
0.769776860213125));
#15808=CARTESIAN_POINT('Ctrl Pts',(0.0382995408207276,0.133854483197375,
0.777719028335907));
#15809=CARTESIAN_POINT('Ctrl Pts',(-0.0853693283863186,0.106155717082476,
0.785272312089402));
#15810=CARTESIAN_POINT('Ctrl Pts',(-0.117593892160246,0.0332537408718532,
0.79017820646864));
#15811=CARTESIAN_POINT('Ctrl Pts',(-0.117874685330111,-8.9283644551537E-5,
0.792436711473617));
#15812=CARTESIAN_POINT('Origin',(0.,0.,-0.0924367114736175));
#15813=CARTESIAN_POINT('',(-0.117964947617991,-1.73329198795185E-5,0.682563288526384));
#15814=CARTESIAN_POINT('',(-0.117740574064672,0.000107068518266168,0.692436711473616));
#15815=CARTESIAN_POINT('',(-0.117775,2.85464118895969E-14,-0.0924367114736175));
#15816=CARTESIAN_POINT('Ctrl Pts',(-0.117964947617991,-1.73329198795367E-5,
0.682563288526384));
#15817=CARTESIAN_POINT('Ctrl Pts',(-0.117966864156947,-0.000949576032666658,
0.682626561953687));
#15818=CARTESIAN_POINT('Ctrl Pts',(-0.117534558560489,-0.0408698671952461,
0.685336165260092));
#15819=CARTESIAN_POINT('Ctrl Pts',(-0.0726787294560835,-0.118728463672822,
0.690692098445597));
#15820=CARTESIAN_POINT('Ctrl Pts',(0.0603425395611779,-0.125448888878168,
0.698631088082904));
#15821=CARTESIAN_POINT('Ctrl Pts',(0.138124349154501,-0.0173294538893964,
0.706570077720209));
#15822=CARTESIAN_POINT('Ctrl Pts',(0.0894627833767505,0.106653908470079,
0.714509067357515));
#15823=CARTESIAN_POINT('Ctrl Pts',(-0.0410958292974484,0.133002927094911,
0.72244805699482));
#15824=CARTESIAN_POINT('Ctrl Pts',(-0.111546724107196,0.0606813038481789,
0.728466130717777));
#15825=CARTESIAN_POINT('Ctrl Pts',(-0.117820302634623,0.0108495967181263,
0.731837874561632));
#15826=CARTESIAN_POINT('Ctrl Pts',(-0.11772691567491,0.000105512987197042,
0.732563288526384));
#15827=CARTESIAN_POINT('Ctrl Pts',(-0.117740574064672,0.000107068518266165,
0.692436711473616));
#15828=CARTESIAN_POINT('Ctrl Pts',(-0.117483171888848,-0.0288182833237499,
0.694390256685113));
#15829=CARTESIAN_POINT('Ctrl Pts',(-0.0921515028359353,-0.0973455904149804,
0.698991191270869));
#15830=CARTESIAN_POINT('Ctrl Pts',(0.022691720100341,-0.137364345221032,
0.706239515230886));
#15831=CARTESIAN_POINT('Ctrl Pts',(0.127740337615313,-0.0553740340325759,
0.714181683353665));
#15832=CARTESIAN_POINT('Ctrl Pts',(0.115765682611161,0.077344581120379,
0.722123851476446));
#15833=CARTESIAN_POINT('Ctrl Pts',(-0.00226223072526165,0.139207614056346,
0.730066019599226));
#15834=CARTESIAN_POINT('Ctrl Pts',(-0.101117998472899,0.083225715609228,
0.736836972931616));
#15835=CARTESIAN_POINT('Ctrl Pts',(-0.117530897055598,0.0218902846491045,
0.740960536889746));
#15836=CARTESIAN_POINT('Ctrl Pts',(-0.117591850253004,-3.65476421498364E-5,
0.742436711473616));
#15837=CARTESIAN_POINT('Origin',(0.,0.,-0.0924367114736175));
#15838=CARTESIAN_POINT('',(-0.117676160015555,-9.46906955630148E-5,0.632563288526383));
#15839=CARTESIAN_POINT('',(-0.117962383120995,-2.41598447144192E-5,0.642436711473616));
#15840=CARTESIAN_POINT('',(-0.117775,2.85464118895969E-14,-0.0924367114736175));
#15841=CARTESIAN_POINT('Ctrl Pts',(-0.117676160015555,-9.46906955630045E-5,
0.632563288526383));
#15842=CARTESIAN_POINT('Ctrl Pts',(-0.117771520970562,-0.0127268345011372,
0.633415249345741));
#15843=CARTESIAN_POINT('Ctrl Pts',(-0.110078248258936,-0.064483421762156,
0.636913540044201));
#15844=CARTESIAN_POINT('Ctrl Pts',(-0.0347063025259737,-0.134811417789573,
0.643058160621763));
#15845=CARTESIAN_POINT('Ctrl Pts',(0.0944472082050275,-0.102266175560326,
0.65099715025907));
#15846=CARTESIAN_POINT('Ctrl Pts',(0.137140772714236,0.0238967416356601,
0.658936139896373));
#15847=CARTESIAN_POINT('Ctrl Pts',(0.054291358674537,0.128183829614862,
0.666875129533682));
#15848=CARTESIAN_POINT('Ctrl Pts',(-0.0772016597727435,0.11523146575827,
0.674750845743682));
#15849=CARTESIAN_POINT('Ctrl Pts',(-0.117886707375211,0.0380402955314478,
0.679980232074585));
#15850=CARTESIAN_POINT('Ctrl Pts',(-0.117964947617991,-1.73329198795367E-5,
0.682563288526384));
#15851=CARTESIAN_POINT('Ctrl Pts',(-0.117962383120995,-2.41598447144253E-5,
0.642436711473616));
#15852=CARTESIAN_POINT('Ctrl Pts',(-0.117966033213387,-0.0013279541977536,
0.642525197731959));
#15853=CARTESIAN_POINT('Ctrl Pts',(-0.117355585052125,-0.0416360146359673,
0.645261073364563));
#15854=CARTESIAN_POINT('Ctrl Pts',(-0.0715088964667609,-0.119458592094588,
0.650644338371427));
#15855=CARTESIAN_POINT('Ctrl Pts',(0.0616402393688536,-0.124837327709565,
0.658586506494205));
#15856=CARTESIAN_POINT('Ctrl Pts',(0.138320583400205,-0.0158522461166236,
0.666528674616987));
#15857=CARTESIAN_POINT('Ctrl Pts',(0.0882850628235238,0.107655121482266,
0.674470842739765));
#15858=CARTESIAN_POINT('Ctrl Pts',(-0.0426286451686149,0.132539337972556,
0.682413010862546));
#15859=CARTESIAN_POINT('Ctrl Pts',(-0.111894847147975,0.059748848130285,
0.68840163377383));
#15860=CARTESIAN_POINT('Ctrl Pts',(-0.117831996057943,0.0103805377030848,
0.691742867310853));
#15861=CARTESIAN_POINT('Ctrl Pts',(-0.117740574064672,0.000107068518266165,
0.692436711473616));
#15862=CARTESIAN_POINT('Origin',(0.,0.,-0.0924367114736175));
#15863=CARTESIAN_POINT('',(-0.117626285855324,7.11112359239178E-5,0.582563288526384));
#15864=CARTESIAN_POINT('',(-0.11766919235599,-9.26074537421634E-5,0.592436711473616));
#15865=CARTESIAN_POINT('',(-0.117775,2.85464118895969E-14,-0.0924367114736175));
#15866=CARTESIAN_POINT('Ctrl Pts',(-0.117626285855324,7.11112359239024E-5,
0.582563288526383));
#15867=CARTESIAN_POINT('Ctrl Pts',(-0.117492102008102,-0.0242809575267813,
0.584203936737797));
#15868=CARTESIAN_POINT('Ctrl Pts',(-0.0982512120079041,-0.0881067492982899,
0.588490914828312));
#15869=CARTESIAN_POINT('Ctrl Pts',(0.00631176444456456,-0.139064040754811,
0.595424222797929));
#15870=CARTESIAN_POINT('Ctrl Pts',(0.120263693490807,-0.0701091280034811,
0.603363212435234));
#15871=CARTESIAN_POINT('Ctrl Pts',(0.124122453355413,0.0630258865426945,
0.611302202072541));
#15872=CARTESIAN_POINT('Ctrl Pts',(0.0143556138404206,0.138465021405133,
0.619241191709845));
#15873=CARTESIAN_POINT('Ctrl Pts',(-0.0953630726970595,0.0926558297308384,
0.626328220527794));
#15874=CARTESIAN_POINT('Ctrl Pts',(-0.117475314221613,0.0265106736450616,
0.630768919466639));
#15875=CARTESIAN_POINT('Ctrl Pts',(-0.117676160015555,-9.46906955630045E-5,
0.632563288526383));
#15876=CARTESIAN_POINT('Ctrl Pts',(-0.11766919235599,-9.26074537421669E-5,
0.592436711473616));
#15877=CARTESIAN_POINT('Ctrl Pts',(-0.117764072896019,-0.0130062487266101,
0.593307528153066));
#15878=CARTESIAN_POINT('Ctrl Pts',(-0.109848366281979,-0.0650658641993071,
0.596825734206776));
#15879=CARTESIAN_POINT('Ctrl Pts',(-0.0336977294021144,-0.135086418755761,
0.602991329634746));
#15880=CARTESIAN_POINT('Ctrl Pts',(0.0952657566843092,-0.101529863106778,
0.610933497757526));
#15881=CARTESIAN_POINT('Ctrl Pts',(0.136956022624868,0.025038477707157,
0.618875665880307));
#15882=CARTESIAN_POINT('Ctrl Pts',(0.0531805018142573,0.128669000640787,
0.626817834003085));
#15883=CARTESIAN_POINT('Ctrl Pts',(-0.0778376600742765,0.114584191752874,
0.634671515867523));
#15884=CARTESIAN_POINT('Ctrl Pts',(-0.117856827377429,0.0376798124439797,
0.639877808357699));
#15885=CARTESIAN_POINT('Ctrl Pts',(-0.117962383120995,-2.41598447144253E-5,
0.642436711473616));
#15886=CARTESIAN_POINT('Origin',(0.,0.,-0.0924367114736175));
#15887=CARTESIAN_POINT('',(-0.117934829819181,5.63106208242181E-5,0.532563288526383));
#15888=CARTESIAN_POINT('',(-0.117629301205424,7.34277634442948E-5,0.542436711473615));
#15889=CARTESIAN_POINT('',(-0.117775,2.85464118895969E-14,-0.0924367114736175));
#15890=CARTESIAN_POINT('Ctrl Pts',(-0.117934829819181,5.63106208242166E-5,
0.532563288526383));
#15891=CARTESIAN_POINT('Ctrl Pts',(-0.117723349859012,-0.0357608023914865,
0.534992624129852));
#15892=CARTESIAN_POINT('Ctrl Pts',(-0.0811985738067347,-0.110967619805887,
0.540068289612422));
#15893=CARTESIAN_POINT('Ctrl Pts',(0.0467759446245483,-0.131113145053959,
0.547790284974095));
#15894=CARTESIAN_POINT('Ctrl Pts',(0.135526478334676,-0.031799677225719,
0.555729274611401));
#15895=CARTESIAN_POINT('Ctrl Pts',(0.100211809365564,0.0966242157284558,
0.563668264248707));
#15896=CARTESIAN_POINT('Ctrl Pts',(-0.0268399031138932,0.136595261273209,
0.571607253886012));
#15897=CARTESIAN_POINT('Ctrl Pts',(-0.108142973925314,0.0691035501437442,
0.577905595311905));
#15898=CARTESIAN_POINT('Ctrl Pts',(-0.117708537635025,0.0149983997031143,
0.581557606858695));
#15899=CARTESIAN_POINT('Ctrl Pts',(-0.117626285855324,7.11112359239024E-5,
0.582563288526383));
#15900=CARTESIAN_POINT('Ctrl Pts',(-0.117629301205424,7.34277634442983E-5,
0.542436711473615));
#15901=CARTESIAN_POINT('Ctrl Pts',(-0.11748956090956,-0.0244625652698295,
0.544089858574172));
#15902=CARTESIAN_POINT('Ctrl Pts',(-0.0980201725405651,-0.0884941619373469,
0.548390395048989));
#15903=CARTESIAN_POINT('Ctrl Pts',(0.00702343738442799,-0.139048728244533,
0.555338320898066));
#15904=CARTESIAN_POINT('Ctrl Pts',(0.12066450826877,-0.0694546898587181,
0.563280489020846));
#15905=CARTESIAN_POINT('Ctrl Pts',(0.123764493242992,0.063766979789076,
0.571222657143626));
#15906=CARTESIAN_POINT('Ctrl Pts',(0.0134834875971477,0.13857154491934,
0.579164825266405));
#15907=CARTESIAN_POINT('Ctrl Pts',(-0.0957036897026042,0.092147346049863,
0.586236176709736));
#15908=CARTESIAN_POINT('Ctrl Pts',(-0.117475624432153,0.0262528025703711,
0.590660138778806));
#15909=CARTESIAN_POINT('Ctrl Pts',(-0.11766919235599,-9.26074537421669E-5,
0.592436711473616));
#15910=CARTESIAN_POINT('Origin',(0.,0.,-0.0924367114736175));
#15911=CARTESIAN_POINT('',(-0.117794891956694,-0.000106411733115368,0.482563288526384));
#15912=CARTESIAN_POINT('',(-0.117936566864074,5.52347650140707E-5,0.492436711473616));
#15913=CARTESIAN_POINT('',(-0.117775,2.85464118895969E-14,-0.0924367114736175));
#15914=CARTESIAN_POINT('Ctrl Pts',(-0.117794891956694,-0.000106411733115381,
0.482563288526384));
#15915=CARTESIAN_POINT('Ctrl Pts',(-0.117872998614688,-0.00856127641466401,
0.483134981642805));
#15916=CARTESIAN_POINT('Ctrl Pts',(-0.113184542395844,-0.0560672187853419,
0.486353004638329));
#15917=CARTESIAN_POINT('Ctrl Pts',(-0.0487302328423073,-0.130399425645183,
0.492217357512954));
#15918=CARTESIAN_POINT('Ctrl Pts',(0.0831353173341669,-0.111656458896056,
0.50015634715026));
#15919=CARTESIAN_POINT('Ctrl Pts',(0.13889618212661,0.00930034365552528,
0.508095336787567));
#15920=CARTESIAN_POINT('Ctrl Pts',(0.0675071113591811,0.12174331898465,
0.516034326424871));
#15921=CARTESIAN_POINT('Ctrl Pts',(-0.0656800932930844,0.122738629397884,
0.523973316062178));
#15922=CARTESIAN_POINT('Ctrl Pts',(-0.116384786286051,0.04545243224792,
0.529482970096015));
#15923=CARTESIAN_POINT('Ctrl Pts',(-0.117953719733239,0.00325558390455253,
0.53234629425075));
#15924=CARTESIAN_POINT('Ctrl Pts',(-0.117934829819181,5.63106208242166E-5,
0.532563288526383));
#15925=CARTESIAN_POINT('Ctrl Pts',(-0.117936566864074,5.52347650140663E-5,
0.492436711473616));
#15926=CARTESIAN_POINT('Ctrl Pts',(-0.117728017843002,-0.0358510361847084,
0.494872188995279));
#15927=CARTESIAN_POINT('Ctrl Pts',(-0.0810366231971402,-0.111156550628637,
0.499955055891203));
#15928=CARTESIAN_POINT('Ctrl Pts',(0.0471380885036503,-0.131003351527116,
0.507685312161385));
#15929=CARTESIAN_POINT('Ctrl Pts',(0.135643160584381,-0.031381690295376,
0.515627480284167));
#15930=CARTESIAN_POINT('Ctrl Pts',(0.0998851624184703,0.0969888232104648,
0.523569648406945));
#15931=CARTESIAN_POINT('Ctrl Pts',(-0.0273779061153799,0.136507610615132,
0.531511816529727));
#15932=CARTESIAN_POINT('Ctrl Pts',(-0.108290992649607,0.0687756007668377,
0.537800837551949));
#15933=CARTESIAN_POINT('Ctrl Pts',(-0.117713344367368,0.0148299618267192,
0.541442469199912));
#15934=CARTESIAN_POINT('Ctrl Pts',(-0.117629301205424,7.34277634442983E-5,
0.542436711473615));
#15935=CARTESIAN_POINT('Origin',(0.,0.,-0.0924367114736175));
#15936=CARTESIAN_POINT('',(-0.117582256074849,9.06819982020624E-6,0.432563288526383));
#15937=CARTESIAN_POINT('',(-0.11779560903417,-0.000106574656651148,0.442436711473616));
#15938=CARTESIAN_POINT('',(-0.117775,2.85464118895969E-14,-0.0924367114736175));
#15939=CARTESIAN_POINT('Ctrl Pts',(-0.117582256074849,9.06819982019261E-6,
0.432563288526383));
#15940=CARTESIAN_POINT('Ctrl Pts',(-0.117568373935691,-0.020201912089319,
0.43392366903486));
#15941=CARTESIAN_POINT('Ctrl Pts',(-0.10300922874285,-0.0797477867736473,
0.437930379422439));
#15942=CARTESIAN_POINT('Ctrl Pts',(-0.00838939967687663,-0.138954178686792,
0.44458341968912));
#15943=CARTESIAN_POINT('Ctrl Pts',(0.11219917790857,-0.0824013973067221,
0.452522409326426));
#15944=CARTESIAN_POINT('Ctrl Pts',(0.13007709763057,0.0495842159710775,
0.460461398963732));
#15945=CARTESIAN_POINT('Ctrl Pts',(0.0288783492374893,0.136178877755608,
0.468400388601037));
#15946=CARTESIAN_POINT('Ctrl Pts',(-0.0895654556576369,0.100852400902523,
0.475767685121922));
#15947=CARTESIAN_POINT('Ctrl Pts',(-0.117511448025972,0.0305757367622385,
0.480488651763704));
#15948=CARTESIAN_POINT('Ctrl Pts',(-0.117794891956694,-0.000106411733115381,
0.482563288526384));
#15949=CARTESIAN_POINT('Ctrl Pts',(-0.11779560903417,-0.000106574656651151,
0.442436711473616));
#15950=CARTESIAN_POINT('Ctrl Pts',(-0.117873644338608,-0.00854245500997505,
0.443007130042126));
#15951=CARTESIAN_POINT('Ctrl Pts',(-0.113196618671047,-0.056044542179559,
0.446224937984896));
#15952=CARTESIAN_POINT('Ctrl Pts',(-0.0487473834415776,-0.130413074907061,
0.452090135301926));
#15953=CARTESIAN_POINT('Ctrl Pts',(0.0831820848081396,-0.111645054821459,
0.460032303424706));
#15954=CARTESIAN_POINT('Ctrl Pts',(0.138908217753341,0.00940130521287039,
0.467974471547486));
#15955=CARTESIAN_POINT('Ctrl Pts',(0.0673801526530663,0.121835103839429,
0.475916639670265));
#15956=CARTESIAN_POINT('Ctrl Pts',(-0.0658750545035054,0.12265543075329,
0.483858807793047));
#15957=CARTESIAN_POINT('Ctrl Pts',(-0.116424939330292,0.0453161125527027,
0.489365498394162));
#15958=CARTESIAN_POINT('Ctrl Pts',(-0.11795471279604,0.00317945345687678,
0.492224799621019));
#15959=CARTESIAN_POINT('Ctrl Pts',(-0.117936566864074,5.52347650140663E-5,
0.492436711473616));
#15960=CARTESIAN_POINT('Origin',(0.,0.,-0.0924367114736175));
#15961=CARTESIAN_POINT('',(-0.117828183671793,0.000101754196006455,0.382563288526383));
#15962=CARTESIAN_POINT('',(-0.117581664177921,7.09484545444172E-6,0.392436711473616));
#15963=CARTESIAN_POINT('',(-0.117775,2.85464118895969E-14,-0.0924367114736175));
#15964=CARTESIAN_POINT('Ctrl Pts',(-0.117828183671793,0.000101754196006446,
0.382563288526384));
#15965=CARTESIAN_POINT('Ctrl Pts',(-0.117538790254565,-0.0316580736410773,
0.384712356426916));
#15966=CARTESIAN_POINT('Ctrl Pts',(-0.0879068326507716,-0.103002379129266,
0.38950775420655));
#15967=CARTESIAN_POINT('Ctrl Pts',(0.0326876424682324,-0.135315053971568,
0.396949481865287));
#15968=CARTESIAN_POINT('Ctrl Pts',(0.13141703692502,-0.0459152284901983,
0.404888471502591));
#15969=CARTESIAN_POINT('Ctrl Pts',(0.109843140674695,0.0855168418978295,
0.412827461139898));
#15970=CARTESIAN_POINT('Ctrl Pts',(-0.0122846228212416,0.13866410438033,
0.420766450777203));
#15971=CARTESIAN_POINT('Ctrl Pts',(-0.104166535924894,0.0775181589932739,
0.427345059906032));
#15972=CARTESIAN_POINT('Ctrl Pts',(-0.117595378674006,0.0191142356295008,
0.431277339155758));
#15973=CARTESIAN_POINT('Ctrl Pts',(-0.117582256074849,9.06819982019261E-6,
0.432563288526383));
#15974=CARTESIAN_POINT('Ctrl Pts',(-0.117581664177921,7.09484545444172E-6,
0.392436711473616));
#15975=CARTESIAN_POINT('Ctrl Pts',(-0.117570873504463,-0.0200907396801347,
0.393789460463232));
#15976=CARTESIAN_POINT('Ctrl Pts',(-0.10312708440739,-0.079535468422451,
0.397789598827109));
#15977=CARTESIAN_POINT('Ctrl Pts',(-0.00873482453528946,-0.138951719454826,
0.404437126565246));
#15978=CARTESIAN_POINT('Ctrl Pts',(0.112042812448737,-0.0826455423945668,
0.412379294688026));
#15979=CARTESIAN_POINT('Ctrl Pts',(0.130177722634257,0.049372441998279,
0.420321462810806));
#15980=CARTESIAN_POINT('Ctrl Pts',(0.0290564652212241,0.136160197297018,
0.428263630933586));
#15981=CARTESIAN_POINT('Ctrl Pts',(-0.0895090212855029,0.100936776489487,
0.435635380487856));
#15982=CARTESIAN_POINT('Ctrl Pts',(-0.117511471984497,0.0306096014671689,
0.440359740667866));
#15983=CARTESIAN_POINT('Ctrl Pts',(-0.11779560903417,-0.000106574656651151,
0.442436711473616));
#15984=CARTESIAN_POINT('Origin',(0.,0.,-0.0924367114736175));
#15985=CARTESIAN_POINT('',(-0.117911328466355,-7.22474488887591E-5,0.332563288526384));
#15986=CARTESIAN_POINT('',(-0.117821685414254,0.000103165543095151,0.342436711473616));
#15987=CARTESIAN_POINT('',(-0.117775,2.85464118895969E-14,-0.0924367114736175));
#15988=CARTESIAN_POINT('Ctrl Pts',(-0.117911328466355,-7.22474488887752E-5,
0.332563288526384));
#15989=CARTESIAN_POINT('Ctrl Pts',(-0.117942332027964,-0.00437115939612809,
0.332854713939869));
#15990=CARTESIAN_POINT('Ctrl Pts',(-0.115777752883067,-0.0476754067323583,
0.335792469232457));
#15991=CARTESIAN_POINT('Ctrl Pts',(-0.0622106591311991,-0.12453304658572,
0.341376554404146));
#15992=CARTESIAN_POINT('Ctrl Pts',(0.0708961914151981,-0.119801401679107,
0.349315544041452));
#15993=CARTESIAN_POINT('Ctrl Pts',(0.1391024375543,-0.00539978406154301,
0.357254533678757));
#15994=CARTESIAN_POINT('Ctrl Pts',(0.0799699354250877,0.113944965792994,
0.365193523316063));
#15995=CARTESIAN_POINT('Ctrl Pts',(-0.0523695618881846,0.128980908622551,
0.373132512953369));
#15996=CARTESIAN_POINT('Ctrl Pts',(-0.113921748517257,0.0538356345748906,
0.378922434690143));
#15997=CARTESIAN_POINT('Ctrl Pts',(-0.117895144954496,0.00745050051778832,
0.382066026547814));
#15998=CARTESIAN_POINT('Ctrl Pts',(-0.117828183671793,0.000101754196006446,
0.382563288526384));
#15999=CARTESIAN_POINT('Ctrl Pts',(-0.117821685414254,0.000103165543095145,
0.342436711473616));
#16000=CARTESIAN_POINT('Ctrl Pts',(-0.117532262555972,-0.0314544122979593,
0.344571790884339));
#16001=CARTESIAN_POINT('Ctrl Pts',(-0.0882170202347594,-0.102616110661261,
0.349354259669323));
#16002=CARTESIAN_POINT('Ctrl Pts',(0.0320320385160992,-0.135491055083419,
0.356784117828566));
#16003=CARTESIAN_POINT('Ctrl Pts',(0.131227975626944,-0.0465090949381858,
0.364726285951346));
#16004=CARTESIAN_POINT('Ctrl Pts',(0.110205605501345,0.0850799742312894,
0.372668454074126));
#16005=CARTESIAN_POINT('Ctrl Pts',(-0.0117764211155082,0.138727046407055,
0.380610622196906));
#16006=CARTESIAN_POINT('Ctrl Pts',(-0.10403099481448,0.0777947493501838,
0.387200041330069));
#16007=CARTESIAN_POINT('Ctrl Pts',(-0.117591991327853,0.019241607989002,
0.391142071088973));
#16008=CARTESIAN_POINT('Ctrl Pts',(-0.117581664177921,7.09484545444172E-6,
0.392436711473616));
#16009=CARTESIAN_POINT('Origin',(0.,0.,-0.0924367114736175));
#16010=CARTESIAN_POINT('',(-0.117608153246896,-5.64262068778628E-5,0.282563288526383));
#16011=CARTESIAN_POINT('',(-0.117918861549493,-6.80329776671096E-5,0.292436711473615));
#16012=CARTESIAN_POINT('',(-0.117775,2.85464118895969E-14,-0.0924367114736175));
#16013=CARTESIAN_POINT('Ctrl Pts',(-0.117608153246896,-5.64262068778604E-5,
0.282563288526383));
#16014=CARTESIAN_POINT('Ctrl Pts',(-0.117677606263852,-0.0160946837114709,
0.283643401331924));
#16015=CARTESIAN_POINT('Ctrl Pts',(-0.107144424846824,-0.0713401098021974,
0.287369844016567));
#16016=CARTESIAN_POINT('Ctrl Pts',(-0.0229969941138309,-0.137294515779738,
0.293742616580312));
#16017=CARTESIAN_POINT('Ctrl Pts',(0.102883268653204,-0.0937746172089793,
0.301681606217617));
#16018=CARTESIAN_POINT('Ctrl Pts',(0.134580950019115,0.0355895166223291,
0.309620595854923));
#16019=CARTESIAN_POINT('Ctrl Pts',(0.0430789950773988,0.13237388709478,
0.317559585492229));
#16020=CARTESIAN_POINT('Ctrl Pts',(-0.0830523456774332,0.10887452531409,
0.325207149716049));
#16021=CARTESIAN_POINT('Ctrl Pts',(-0.11766079978112,0.0346657214219864,
0.330208384060767));
#16022=CARTESIAN_POINT('Ctrl Pts',(-0.117911328466355,-7.22474488887752E-5,
0.332563288526384));
#16023=CARTESIAN_POINT('Ctrl Pts',(-0.117918861549493,-6.80329776671157E-5,
0.292436711473616));
#16024=CARTESIAN_POINT('Ctrl Pts',(-0.117946256357307,-0.00405052459867665,
0.292706731931186));
#16025=CARTESIAN_POINT('Ctrl Pts',(-0.11595553950755,-0.0470512577090033,
0.295624141763016));
#16026=CARTESIAN_POINT('Ctrl Pts',(-0.0631725212350128,-0.124068972994571,
0.301188940969106));
#16027=CARTESIAN_POINT('Ctrl Pts',(0.0700327441786229,-0.12032993078169,
0.309131109091886));
#16028=CARTESIAN_POINT('Ctrl Pts',(0.139080821187468,-0.00635631000930847,
0.317073277214666));
#16029=CARTESIAN_POINT('Ctrl Pts',(0.0807165776729536,0.11344034374014,
0.325015445337446));
#16030=CARTESIAN_POINT('Ctrl Pts',(-0.0515923433190751,0.129313988454311,
0.332957613460226));
#16031=CARTESIAN_POINT('Ctrl Pts',(-0.113774867115171,0.0543021652640841,
0.338764702172283));
#16032=CARTESIAN_POINT('Ctrl Pts',(-0.117891132111753,0.00767537174388221,
0.341924401510079));
#16033=CARTESIAN_POINT('Ctrl Pts',(-0.117821685414254,0.000103165543095145,
0.342436711473616));
#16034=CARTESIAN_POINT('Origin',(0.,0.,-0.0924367114736175));
#16035=CARTESIAN_POINT('',(-0.117705188630573,0.000102098618198066,0.232563288526383));
#16036=CARTESIAN_POINT('',(-0.1176142238744,-6.23262858038681E-5,0.242436711473616));
#16037=CARTESIAN_POINT('',(-0.117775,2.85464118895969E-14,-0.0924367114736175));
#16038=CARTESIAN_POINT('Ctrl Pts',(-0.117705188630573,0.000102098618198071,
0.232563288526383));
#16039=CARTESIAN_POINT('Ctrl Pts',(-0.117475649963863,-0.0275896003179174,
0.234432088723979));
#16040=CARTESIAN_POINT('Ctrl Pts',(-0.0938913217252411,-0.0948462909608301,
0.238947218800678));
#16041=CARTESIAN_POINT('Ctrl Pts',(0.0182347644767634,-0.138007750384372,
0.246108678756477));
#16042=CARTESIAN_POINT('Ctrl Pts',(0.125841858853055,-0.0595186723796334,
0.254047668393783));
#16043=CARTESIAN_POINT('Ctrl Pts',(0.118249355954961,0.073455671106145,
0.261986658031089));
#16044=CARTESIAN_POINT('Ctrl Pts',(0.00240767183786234,0.139186381940956,
0.269925647668394));
#16045=CARTESIAN_POINT('Ctrl Pts',(-0.0995777503027144,0.0858938305448248,
0.27678452450016));
#16046=CARTESIAN_POINT('Ctrl Pts',(-0.117507442931816,0.0231998416616275,
0.280997071452822));
#16047=CARTESIAN_POINT('Ctrl Pts',(-0.117608153246896,-5.64262068778604E-5,
0.282563288526383));
#16048=CARTESIAN_POINT('Ctrl Pts',(-0.1176142238744,-6.2326285803882E-5,
0.242436711473616));
#16049=CARTESIAN_POINT('Ctrl Pts',(-0.117689148257971,-0.0156863246439697,
0.243489062352292));
#16050=CARTESIAN_POINT('Ctrl Pts',(-0.107519643382358,-0.0705218816827611,
0.247188802605229));
#16051=CARTESIAN_POINT('Ctrl Pts',(-0.024381182195918,-0.137074561658528,
0.253535932232426));
#16052=CARTESIAN_POINT('Ctrl Pts',(0.101985705091022,-0.094777599970642,
0.261478100355206));
#16053=CARTESIAN_POINT('Ctrl Pts',(0.134923209124943,0.0343453801629359,
0.269420268477986));
#16054=CARTESIAN_POINT('Ctrl Pts',(0.0442571924125319,0.132004463632409,
0.277362436600766));
#16055=CARTESIAN_POINT('Ctrl Pts',(-0.0824920331482911,0.109525057495754,
0.285034584265976));
#16056=CARTESIAN_POINT('Ctrl Pts',(-0.117677666622401,0.0349954280503056,
0.290059342556926));
#16057=CARTESIAN_POINT('Ctrl Pts',(-0.117918861549493,-6.80329776671157E-5,
0.292436711473616));
#16058=CARTESIAN_POINT('Origin',(0.,0.,-0.0924367114736175));
#16059=CARTESIAN_POINT('',(-0.117967994073432,-3.0724305424694E-6,0.182563288526383));
#16060=CARTESIAN_POINT('',(-0.117691121003631,9.91971943564221E-5,0.192436711473615));
#16061=CARTESIAN_POINT('',(-0.117775,2.85464118895969E-14,-0.0924367114736175));
#16062=CARTESIAN_POINT('Ctrl Pts',(-0.117967994073432,-3.07243054247449E-6,
0.182563288526383));
#16063=CARTESIAN_POINT('Ctrl Pts',(-0.117968057042159,-0.000167453844217198,
0.182574446236933));
#16064=CARTESIAN_POINT('Ctrl Pts',(-0.117893299674953,-0.0393189363008842,
0.185231933826584));
#16065=CARTESIAN_POINT('Ctrl Pts',(-0.0749972298318695,-0.11727771015962,
0.190535751295337));
#16066=CARTESIAN_POINT('Ctrl Pts',(0.0578663373665801,-0.126610160769685,
0.198474740932643));
#16067=CARTESIAN_POINT('Ctrl Pts',(0.13775723856723,-0.0200396862227523,
0.206413730569949));
#16068=CARTESIAN_POINT('Ctrl Pts',(0.091540828968026,0.104875747581476,
0.214352720207254));
#16069=CARTESIAN_POINT('Ctrl Pts',(-0.0384749358425138,0.133784622116252,
0.22229170984456));
#16070=CARTESIAN_POINT('Ctrl Pts',(-0.110955338697302,0.0622468391270206,
0.22836189928427));
#16071=CARTESIAN_POINT('Ctrl Pts',(-0.11780069007939,0.0116234575531164,
0.231785758844877));
#16072=CARTESIAN_POINT('Ctrl Pts',(-0.117705188630573,0.000102098618198071,
0.232563288526383));
#16073=CARTESIAN_POINT('Ctrl Pts',(-0.117691121003631,9.91971943564221E-5,
0.192436711473615));
#16074=CARTESIAN_POINT('Ctrl Pts',(-0.117474218986382,-0.0270951350261672,
0.194271392773399));
#16075=CARTESIAN_POINT('Ctrl Pts',(-0.0945676524372527,-0.0938598508209937,
0.198753463447442));
#16076=CARTESIAN_POINT('Ctrl Pts',(0.0165156171993534,-0.138242945169174,
0.205882923495746));
#16077=CARTESIAN_POINT('Ctrl Pts',(0.125131592687617,-0.061040658666823,
0.213825091618526));
#16078=CARTESIAN_POINT('Ctrl Pts',(0.119114174013628,0.0720811421096423,
0.221767259741306));
#16079=CARTESIAN_POINT('Ctrl Pts',(0.0039759348809324,0.139169211541763,
0.229709427864086));
#16080=CARTESIAN_POINT('Ctrl Pts',(-0.0990660356104632,0.0867677816679632,
0.236599245108189));
#16081=CARTESIAN_POINT('Ctrl Pts',(-0.117500661679058,0.0236188235484957,
0.240841672978032));
#16082=CARTESIAN_POINT('Ctrl Pts',(-0.1176142238744,-6.2326285803882E-5,
0.242436711473616));
#16083=CARTESIAN_POINT('Origin',(0.,0.,-0.0924367114736175));
#16084=CARTESIAN_POINT('',(-0.117696212882312,-0.000100181105204699,0.132563288526383));
#16085=CARTESIAN_POINT('',(-0.117967699956222,8.3697257429456E-6,0.142436711473616));
#16086=CARTESIAN_POINT('',(-0.117775,2.85464118895969E-14,-0.0924367114736175));
#16087=CARTESIAN_POINT('Ctrl Pts',(-0.117696212882312,-0.000100181105204706,
0.132563288526383));
#16088=CARTESIAN_POINT('Ctrl Pts',(-0.117792074781153,-0.0119544960022407,
0.133363133628988));
#16089=CARTESIAN_POINT('Ctrl Pts',(-0.110696412003459,-0.0629173266909915,
0.136809308610694));
#16090=CARTESIAN_POINT('Ctrl Pts',(-0.0373480950846616,-0.134103559412242,
0.142901813471503));
#16091=CARTESIAN_POINT('Ctrl Pts',(0.0924198687735613,-0.104101940294199,
0.150840803108809));
#16092=CARTESIAN_POINT('Ctrl Pts',(0.137583777756591,0.0211978768359354,
0.158779792746114));
#16093=CARTESIAN_POINT('Ctrl Pts',(0.0567991668878991,0.127092487218924,
0.16671878238342));
#16094=CARTESIAN_POINT('Ctrl Pts',(-0.0757945745091616,0.116657324056303,
0.174646614310176));
#16095=CARTESIAN_POINT('Ctrl Pts',(-0.117953122434976,0.0388197061692436,
0.179928116357831));
#16096=CARTESIAN_POINT('Ctrl Pts',(-0.117967994073432,-3.07243054247449E-6,
0.182563288526383));
#16097=CARTESIAN_POINT('Ctrl Pts',(-0.117967699956222,8.3697257429579E-6,
0.142436711473616));
#16098=CARTESIAN_POINT('Ctrl Pts',(-0.117928252023989,-0.038547130539091,
0.145053723194506));
#16099=CARTESIAN_POINT('Ctrl Pts',(-0.0762804946418446,-0.116178754198862,
0.150318124289656));
#16100=CARTESIAN_POINT('Ctrl Pts',(0.0559861945572589,-0.127473226882309,
0.158229914759066));
#16101=CARTESIAN_POINT('Ctrl Pts',(0.137471621702818,-0.0220324926503626,
0.166172082881846));
#16102=CARTESIAN_POINT('Ctrl Pts',(0.0930189202108026,0.103592267873211,
0.174114251004626));
#16103=CARTESIAN_POINT('Ctrl Pts',(-0.0366486683060043,0.134315868829211,
0.182056419127406));
#16104=CARTESIAN_POINT('Ctrl Pts',(-0.110544190454925,0.0633195416932908,
0.188163905950403));
#16105=CARTESIAN_POINT('Ctrl Pts',(-0.11778720200735,0.0121454601492482,
0.191624003399139));
#16106=CARTESIAN_POINT('Ctrl Pts',(-0.117691121003631,9.91971943564221E-5,
0.192436711473615));
#16107=CARTESIAN_POINT('Origin',(0.,0.,-0.0924367114736175));
#16108=CARTESIAN_POINT('',(-0.117613109409711,6.11591708146705E-5,0.0825632885263832));
#16109=CARTESIAN_POINT('',(-0.117715749944134,-0.000104199409386274,0.0924367114736155));
#16110=CARTESIAN_POINT('',(-0.117775,2.85464118895969E-14,-0.0924367114736175));
#16111=CARTESIAN_POINT('Ctrl Pts',(-0.117613109409711,6.11591708146765E-5,
0.0825632885263832));
#16112=CARTESIAN_POINT('Ctrl Pts',(-0.117502393620717,-0.0235240259785673,
0.0841518210210431));
#16113=CARTESIAN_POINT('Ctrl Pts',(-0.0991849320095013,-0.0865581493706475,
0.088386683394805));
#16114=CARTESIAN_POINT('Ctrl Pts',(0.00357853460314598,-0.139161043603659,
0.0952678756476685));
#16115=CARTESIAN_POINT('Ctrl Pts',(0.118863112008681,-0.0724583686054966,
0.103206865284975));
#16116=CARTESIAN_POINT('Ctrl Pts',(0.125336705278751,0.0605752693714656,
0.11114585492228));
#16117=CARTESIAN_POINT('Ctrl Pts',(0.0170731091066207,0.138156245709763,
0.119084844559586));
#16118=CARTESIAN_POINT('Ctrl Pts',(-0.094337657277608,0.0941904991302726,
0.126223989094287));
#16119=CARTESIAN_POINT('Ctrl Pts',(-0.11747491061231,0.0272661325996615,
0.130716803749886));
#16120=CARTESIAN_POINT('Ctrl Pts',(-0.117696212882312,-0.000100181105204706,
0.132563288526383));
#16121=CARTESIAN_POINT('Ctrl Pts',(-0.117715749944134,-0.000104199409386274,
0.0924367114736155));
#16122=CARTESIAN_POINT('Ctrl Pts',(-0.117810584636384,-0.011244028442556,
0.0931886642413524));
#16123=CARTESIAN_POINT('Ctrl Pts',(-0.111246641208053,-0.0614941526881817,
0.0965880063833492));
#16124=CARTESIAN_POINT('Ctrl Pts',(-0.0397151780004399,-0.133441281507892,
0.102634737899606));
#16125=CARTESIAN_POINT('Ctrl Pts',(0.0906220264938673,-0.105695447092796,
0.110576906022386));
#16126=CARTESIAN_POINT('Ctrl Pts',(0.137940159127448,0.0188783162799928,
0.118519074145166));
#16127=CARTESIAN_POINT('Ctrl Pts',(0.0588909273047484,0.126157580947307,
0.126461242267946));
#16128=CARTESIAN_POINT('Ctrl Pts',(-0.074108440039672,0.117863552156501,
0.134403410390726));
#16129=CARTESIAN_POINT('Ctrl Pts',(-0.117763087033452,0.0399060678969832,
0.139728566792616));
#16130=CARTESIAN_POINT('Ctrl Pts',(-0.117968157858494,0.000455912857932787,
0.142406333820246));
#16131=CARTESIAN_POINT('Ctrl Pts',(-0.117967699956222,8.3697257429579E-6,
0.142436711473616));
#16132=CARTESIAN_POINT('Origin',(0.,0.,-0.0924367114736175));
#16133=CARTESIAN_POINT('',(-0.117917485785546,7.60014832213593E-5,0.0325632885263832));
#16134=CARTESIAN_POINT('',(-0.117600989619072,5.04992496179954E-5,0.0424367114736154));
#16135=CARTESIAN_POINT('',(-0.117775,2.85464118895969E-14,-0.0924367114736175));
#16136=CARTESIAN_POINT('Ctrl Pts',(-0.117917485785546,7.60014832213644E-5,
0.0325632885263832));
#16137=CARTESIAN_POINT('Ctrl Pts',(-0.117676727567847,-0.0349830640657269,
0.0349405084130983));
#16138=CARTESIAN_POINT('Ctrl Pts',(-0.0825043195215805,-0.109517225708346,
0.0399640581789154));
#16139=CARTESIAN_POINT('Ctrl Pts',(0.0441923146003338,-0.131999388615902,
0.0476339378238343));
#16140=CARTESIAN_POINT('Ctrl Pts',(0.134874939024977,-0.034459980695041,
0.0555729274611401));
#16141=CARTESIAN_POINT('Ctrl Pts',(0.102091080224759,0.094638871230671,
0.0635119170984456));
#16142=CARTESIAN_POINT('Ctrl Pts',(-0.0241513666277066,0.137095110112719,
0.0714509067357516));
#16143=CARTESIAN_POINT('Ctrl Pts',(-0.107448046275642,0.0706698818446754,
0.0778013638783972));
#16144=CARTESIAN_POINT('Ctrl Pts',(-0.117686834607281,0.0157664388843013,
0.0815054911419412));
#16145=CARTESIAN_POINT('Ctrl Pts',(-0.117613109409711,6.11591708146765E-5,
0.0825632885263832));
#16146=CARTESIAN_POINT('Ctrl Pts',(-0.117600989619072,5.04992496179954E-5,
0.0424367114736154));
#16147=CARTESIAN_POINT('Ctrl Pts',(-0.117514779739531,-0.0227353060542692,
0.043970994662459));
#16148=CARTESIAN_POINT('Ctrl Pts',(-0.100129952091853,-0.0849605109884783,
0.0481526672255625));
#16149=CARTESIAN_POINT('Ctrl Pts',(0.000787973702835166,-0.139222729671589,
0.054981729162926));
#16150=CARTESIAN_POINT('Ctrl Pts',(0.117431922513572,-0.0747907597173192,
0.0629238972857061));
#16151=CARTESIAN_POINT('Ctrl Pts',(0.126496838785129,0.0581591461343325,
0.070866065408486));
#16152=CARTESIAN_POINT('Ctrl Pts',(0.0196773008918215,0.137828289815661,
0.0788082335312661));
#16153=CARTESIAN_POINT('Ctrl Pts',(-0.0933482651079043,0.0956446566614129,
0.085998448886309));
#16154=CARTESIAN_POINT('Ctrl Pts',(-0.11747670148927,0.0279758085988667,
0.0905412748670923));
#16155=CARTESIAN_POINT('Ctrl Pts',(-0.117715749944134,-0.000104199409386274,
0.0924367114736155));
#16156=CARTESIAN_POINT('Origin',(0.,0.,1.55));
#16157=CARTESIAN_POINT('',(-0.143211704627722,-5.70397197726547E-6,1.50700023576178));
#16158=CARTESIAN_POINT('Ctrl Pts',(-0.0334019664626774,0.112939183906323,
1.532225));
#16159=CARTESIAN_POINT('Ctrl Pts',(-0.0250606930336426,0.115799676338094,
1.53184761307169));
#16160=CARTESIAN_POINT('Ctrl Pts',(-0.0164287086124659,0.117635554524944,
1.53147359869818));
#16161=CARTESIAN_POINT('Ctrl Pts',(-0.00767226928320402,0.118510614220874,
1.53110056493424));
#16162=CARTESIAN_POINT('Ctrl Pts',(-0.0042150196872779,0.118856108509867,
1.53095328237096));
#16163=CARTESIAN_POINT('Ctrl Pts',(-0.000736351480830917,0.119051293525916,
1.53080607672538));
#16164=CARTESIAN_POINT('Ctrl Pts',(0.00274830211697625,0.119097943881266,
1.53065904037218));
#16165=CARTESIAN_POINT('Ctrl Pts',(0.00972321854123044,0.119191319684798,
1.53036473098213));
#16166=CARTESIAN_POINT('Ctrl Pts',(0.0166907125456733,0.118690968429664,
1.53007241075126));
#16167=CARTESIAN_POINT('Ctrl Pts',(0.0235721318645625,0.11762150546261,
1.52978094357425));
#16168=CARTESIAN_POINT('Ctrl Pts',(0.0273478463565568,0.117034709826966,
1.52962102062912));
#16169=CARTESIAN_POINT('Ctrl Pts',(0.0310977188904398,0.116276259986281,
1.52946135449799));
#16170=CARTESIAN_POINT('Ctrl Pts',(0.0348087249896146,0.115347945392283,
1.52930175751644));
#16171=CARTESIAN_POINT('Ctrl Pts',(0.0378768737129624,0.114580442682688,
1.52916980751093));
#16172=CARTESIAN_POINT('Ctrl Pts',(0.0409182562642153,0.113696477767379,
1.52903790896105));
#16173=CARTESIAN_POINT('Ctrl Pts',(0.0439120268522727,0.112701821307647,
1.52890655030309));
#16174=CARTESIAN_POINT('Ctrl Pts',(0.0504861734289241,0.110517613410832,
1.52861809430882));
#16175=CARTESIAN_POINT('Ctrl Pts',(0.0568477403450367,0.107796947733889,
1.528331525126));
#16176=CARTESIAN_POINT('Ctrl Pts',(0.0629211062797432,0.10455513280498,
1.52804576869741));
#16177=CARTESIAN_POINT('Ctrl Pts',(0.0667529140263229,0.102509807084265,
1.52786547926507));
#16178=CARTESIAN_POINT('Ctrl Pts',(0.0704699809867569,0.100256700264741,
1.52768551335768));
#16179=CARTESIAN_POINT('Ctrl Pts',(0.0740519796445933,0.0977963961590643,
1.52750560123222));
#16180=CARTESIAN_POINT('Ctrl Pts',(0.0761474027326905,0.0963571499395001,
1.52740035495562));
#16181=CARTESIAN_POINT('Ctrl Pts',(0.0781972522873126,0.0948464165467323,
1.52729509152825));
#16182=CARTESIAN_POINT('Ctrl Pts',(0.0801950758490376,0.0932655888959708,
1.52718986717129));
#16183=CARTESIAN_POINT('Ctrl Pts',(0.0872135629190184,0.0877120362002772,
1.52682020700562));
#16184=CARTESIAN_POINT('Ctrl Pts',(0.0935342345834078,0.0813437113039547,
1.52645409167081));
#16185=CARTESIAN_POINT('Ctrl Pts',(0.0991216768718319,0.0743433873765979,
1.52608928877518));
#16186=CARTESIAN_POINT('Ctrl Pts',(0.101857856375295,0.0709153174549959,
1.52591064420861));
#16187=CARTESIAN_POINT('Ctrl Pts',(0.104417791592617,0.0673349702414553,
1.52573231437502));
#16188=CARTESIAN_POINT('Ctrl Pts',(0.106794530290299,0.0636205708890664,
1.52555403711528));
#16189=CARTESIAN_POINT('Ctrl Pts',(0.108394385735532,0.0611202951812291,
1.52543403324399));
#16190=CARTESIAN_POINT('Ctrl Pts',(0.109912312880749,0.0585571637778213,
1.52531395827658));
#16191=CARTESIAN_POINT('Ctrl Pts',(0.111341951189028,0.0559432008961949,
1.5251940432238));
#16192=CARTESIAN_POINT('Ctrl Pts',(0.115894033640165,0.0476201345006791,
1.52481222412716));
#16193=CARTESIAN_POINT('Ctrl Pts',(0.119530893641226,0.0388304356906876,
1.52443409356659));
#16194=CARTESIAN_POINT('Ctrl Pts',(0.122195159250079,0.0297595052710396,
1.52405718851832));
#16195=CARTESIAN_POINT('Ctrl Pts',(0.123464283518865,0.0254385629829291,
1.52387764960816));
#16196=CARTESIAN_POINT('Ctrl Pts',(0.124512110981915,0.0210533134598664,
1.52369838877875));
#16197=CARTESIAN_POINT('Ctrl Pts',(0.12532867129748,0.0166220814218575,
1.52351913980531));
#16198=CARTESIAN_POINT('Ctrl Pts',(0.126067828800149,0.012610891624201,
1.52335688207487));
#16199=CARTESIAN_POINT('Ctrl Pts',(0.12661735951473,0.00855739899605222,
1.52319445303817));
#16200=CARTESIAN_POINT('Ctrl Pts',(0.126966826155483,0.00450415768051923,
1.52303280899981));
#16201=CARTESIAN_POINT('Ctrl Pts',(0.127602972227412,-0.00287409603749457,
1.52273856283131));
#16202=CARTESIAN_POINT('Ctrl Pts',(0.12758177643555,-0.010267620141741,
1.52244625042084));
#16203=CARTESIAN_POINT('Ctrl Pts',(0.126865581413421,-0.0175939782534482,
1.52215473434257));
#16204=CARTESIAN_POINT('Ctrl Pts',(0.126426462283551,-0.0220859726121444,
1.52197599770985));
#16205=CARTESIAN_POINT('Ctrl Pts',(0.12572570473317,-0.0265528301690258,
1.52179756043894));
#16206=CARTESIAN_POINT('Ctrl Pts',(0.124776542651163,-0.0309793260681717,
1.52161916036391));
#16207=CARTESIAN_POINT('Ctrl Pts',(0.124151644840291,-0.0338935887106027,
1.52150170748789));
#16208=CARTESIAN_POINT('Ctrl Pts',(0.123418330834614,-0.0367926408403149,
1.52138417707714));
#16209=CARTESIAN_POINT('Ctrl Pts',(0.122581975874549,-0.0396644408336013,
1.52126680258073));
#16210=CARTESIAN_POINT('Ctrl Pts',(0.120074191833131,-0.0482754427851461,
1.52091485884509));
#16211=CARTESIAN_POINT('Ctrl Pts',(0.116656903439717,-0.0566007293654626,
1.52056600333313));
#16212=CARTESIAN_POINT('Ctrl Pts',(0.112443760417108,-0.0645262187619275,
1.52021830866717));
#16213=CARTESIAN_POINT('Ctrl Pts',(0.109356904590302,-0.0703330102694749,
1.51996356219884));
#16214=CARTESIAN_POINT('Ctrl Pts',(0.105841781173658,-0.0759253337267248,
1.51970943888381));
#16215=CARTESIAN_POINT('Ctrl Pts',(0.101930367117466,-0.0812537151913617,
1.51945518067311));
#16216=CARTESIAN_POINT('Ctrl Pts',(0.100130771446666,-0.0837052409256295,
1.51933819945644));
#16217=CARTESIAN_POINT('Ctrl Pts',(0.0982476276828181,-0.0860996963839449,
1.51922123442864));
#16218=CARTESIAN_POINT('Ctrl Pts',(0.0962924325256194,-0.0884227179472683,
1.51910469697823));
#16219=CARTESIAN_POINT('Ctrl Pts',(0.0906946176521128,-0.0950736369671782,
1.51877104482549));
#16220=CARTESIAN_POINT('Ctrl Pts',(0.0844921899154374,-0.101162815315101,
1.51843983772287));
#16221=CARTESIAN_POINT('Ctrl Pts',(0.0777644521522082,-0.106582693579069,
1.51810941878));
#16222=CARTESIAN_POINT('Ctrl Pts',(0.0731067700043679,-0.110334931124879,
1.5178806663426));
#16223=CARTESIAN_POINT('Ctrl Pts',(0.0681966627772886,-0.113766151308436,
1.51765229166508));
#16224=CARTESIAN_POINT('Ctrl Pts',(0.0630541948599911,-0.116833686038022,
1.5174237449583));
#16225=CARTESIAN_POINT('Ctrl Pts',(0.0607686815400033,-0.118197018118406,
1.51732216988754));
#16226=CARTESIAN_POINT('Ctrl Pts',(0.0584414404741937,-0.119485783651375,
1.51722075040181));
#16227=CARTESIAN_POINT('Ctrl Pts',(0.0560784264268894,-0.12069488199044,
1.51711960151386));
#16228=CARTESIAN_POINT('Ctrl Pts',(0.0475595529450054,-0.125053787850271,
1.51675495087613));
#16229=CARTESIAN_POINT('Ctrl Pts',(0.038563113830939,-0.128389854466075,
1.51639315730301));
#16230=CARTESIAN_POINT('Ctrl Pts',(0.0292711048986314,-0.130741856378471,
1.51603205677802));
#16231=CARTESIAN_POINT('Ctrl Pts',(0.0254547302664753,-0.13170786066222,
1.51588374709674));
#16232=CARTESIAN_POINT('Ctrl Pts',(0.0215881861914954,-0.132507324978224,
1.51573555432397));
#16233=CARTESIAN_POINT('Ctrl Pts',(0.0176832233642019,-0.13314066674995,
1.51558732853105));
#16234=CARTESIAN_POINT('Ctrl Pts',(0.0144414794405867,-0.133666441752394,
1.51546427740745));
#16235=CARTESIAN_POINT('Ctrl Pts',(0.0111713231872828,-0.134077605234841,
1.5153411329761));
#16236=CARTESIAN_POINT('Ctrl Pts',(0.00789687394913892,-0.134372952697723,
1.51521845803943));
#16237=CARTESIAN_POINT('Ctrl Pts',(-0.00208492598009478,-0.135273287095873,
1.51484449692866));
#16238=CARTESIAN_POINT('Ctrl Pts',(-0.0121386692885745,-0.135107999768821,
1.51447364169918));
#16239=CARTESIAN_POINT('Ctrl Pts',(-0.0220717676774029,-0.133899092645375,
1.51410356562093));
#16240=CARTESIAN_POINT('Ctrl Pts',(-0.0271373055616968,-0.133282591671289,
1.51391483957382));
#16241=CARTESIAN_POINT('Ctrl Pts',(-0.0321716696217597,-0.132393849601707,
1.51372631615657));
#16242=CARTESIAN_POINT('Ctrl Pts',(-0.0371491047637803,-0.131230566976147,
1.51353768678866));
#16243=CARTESIAN_POINT('Ctrl Pts',(-0.0401763453142056,-0.130523066780721,
1.51342296375255));
#16244=CARTESIAN_POINT('Ctrl Pts',(-0.0431793745847511,-0.129714439573166,
1.51330831773957));
#16245=CARTESIAN_POINT('Ctrl Pts',(-0.0461427198170546,-0.128807808452418,
1.51319405707679));
#16246=CARTESIAN_POINT('Ctrl Pts',(-0.0557912886485991,-0.125855842991896,
1.51282202756853));
#16247=CARTESIAN_POINT('Ctrl Pts',(-0.0650506639775802,-0.121862017750276,
1.51245293010828));
#16248=CARTESIAN_POINT('Ctrl Pts',(-0.0737251756215706,-0.116823260910032,
1.51208446868514));
#16249=CARTESIAN_POINT('Ctrl Pts',(-0.0774533877539874,-0.114657657224767,
1.51192610791459));
#16250=CARTESIAN_POINT('Ctrl Pts',(-0.0810733781510443,-0.112298364258586,
1.51176786463208));
#16251=CARTESIAN_POINT('Ctrl Pts',(-0.0845783705992567,-0.109758519633299,
1.51160955655689));
#16252=CARTESIAN_POINT('Ctrl Pts',(-0.0871260289206952,-0.107912394030924,
1.51149448786814));
#16253=CARTESIAN_POINT('Ctrl Pts',(-0.0896122610481647,-0.105970921032248,
1.51137940572563));
#16254=CARTESIAN_POINT('Ctrl Pts',(-0.0920243025666997,-0.10394826075131,
1.51126473391974));
#16255=CARTESIAN_POINT('Ctrl Pts',(-0.0995315444015674,-0.0976529296958118,
1.51090782920982));
#16256=CARTESIAN_POINT('Ctrl Pts',(-0.106349817996106,-0.090554906599088,
1.51055366538392));
#16257=CARTESIAN_POINT('Ctrl Pts',(-0.112409916721278,-0.0828189535999138,
1.51020021897155));
#16258=CARTESIAN_POINT('Ctrl Pts',(-0.11567060314877,-0.0786565598680515,
1.51001004419521));
#16259=CARTESIAN_POINT('Ctrl Pts',(-0.118711357121208,-0.0743087544864998,
1.50982007711492));
#16260=CARTESIAN_POINT('Ctrl Pts',(-0.121517490738653,-0.0697974244982526,
1.50963000253165));
#16261=CARTESIAN_POINT('Ctrl Pts',(-0.123184827969132,-0.0671169005197731,
1.50951706477726));
#16262=CARTESIAN_POINT('Ctrl Pts',(-0.124768226583796,-0.064379797453554,
1.50940414472167));
#16263=CARTESIAN_POINT('Ctrl Pts',(-0.12625918933752,-0.0616017405091787,
1.50929161182319));
#16264=CARTESIAN_POINT('Ctrl Pts',(-0.131254477666307,-0.0522942005345653,
1.50891458411209));
#16265=CARTESIAN_POINT('Ctrl Pts',(-0.135235816373665,-0.0424980109473837,
1.50854057440173));
#16266=CARTESIAN_POINT('Ctrl Pts',(-0.138100316247284,-0.0323932585971084,
1.50816719719795));
#16267=CARTESIAN_POINT('Ctrl Pts',(-0.139428601593765,-0.027707625827389,
1.5079940600046));
#16268=CARTESIAN_POINT('Ctrl Pts',(-0.140516076092011,-0.0229552175461711,
1.50782105881478));
#16269=CARTESIAN_POINT('Ctrl Pts',(-0.14134846970832,-0.01815262603916,
1.50764795577689));
#16270=CARTESIAN_POINT('Ctrl Pts',(-0.141840021659925,-0.0153165600461233,
1.5075457335416));
#16271=CARTESIAN_POINT('Ctrl Pts',(-0.142241997144177,-0.0124651428186592,
1.50744355431084));
#16272=CARTESIAN_POINT('Ctrl Pts',(-0.142550993842162,-0.00961078035088443,
1.50734168592779));
#16273=CARTESIAN_POINT('Ctrl Pts',(-0.142847161918882,-0.00687492249914849,
1.50724404681617));
#16274=CARTESIAN_POINT('Ctrl Pts',(-0.143058332724879,-0.00413406598225375,
1.5071466105924));
#16275=CARTESIAN_POINT('Ctrl Pts',(-0.143182669649515,-0.00139134585336764,
1.50704933585643));
#16276=CARTESIAN_POINT('Ctrl Pts',(-0.143203595382121,-0.00092974984559876,
1.50703296465278));
#16277=CARTESIAN_POINT('Ctrl Pts',(-0.143222061023464,-0.000468100854706259,
1.50701659802318));
#16278=CARTESIAN_POINT('Ctrl Pts',(-0.143238079070951,-6.41379011939899E-6,
1.50700023577028));
#16279=CARTESIAN_POINT('',(-0.00156744678985144,0.146109855568756,1.50365));
#16280=CARTESIAN_POINT('Ctrl Pts',(-0.00156962371672063,0.146072546381438,
1.50365));
#16281=CARTESIAN_POINT('Ctrl Pts',(-0.011711474284147,0.144648739717271,
1.50495065132295));
#16282=CARTESIAN_POINT('Ctrl Pts',(-0.0216501921041044,0.142222471223284,
1.50626105010813));
#16283=CARTESIAN_POINT('Ctrl Pts',(-0.0312062965385204,0.138804788898175,
1.50759029209282));
#16284=CARTESIAN_POINT('Ctrl Pts',(-0.0379863325344082,0.136379950477271,
1.50853338648503));
#16285=CARTESIAN_POINT('Ctrl Pts',(-0.0445735484268955,0.133455002060128,
1.5094859663039));
#16286=CARTESIAN_POINT('Ctrl Pts',(-0.0508923708069948,0.130021662144985,
1.51045128011208));
#16287=CARTESIAN_POINT('Ctrl Pts',(-0.053607485163773,0.128546401418451,
1.51086606268101));
#16288=CARTESIAN_POINT('Ctrl Pts',(-0.0562647183424556,0.126981576978965,
1.51128195276517));
#16289=CARTESIAN_POINT('Ctrl Pts',(-0.0588579379029418,0.125328026221608,
1.51169910067666));
#16290=CARTESIAN_POINT('Ctrl Pts',(-0.0624505046767585,0.123037247762191,
1.51227700458785));
#16291=CARTESIAN_POINT('Ctrl Pts',(-0.0659209207101175,0.120575889029892,
1.51285741907924));
#16292=CARTESIAN_POINT('Ctrl Pts',(-0.0692542752175272,0.117943487410649,
1.51344114883776));
#16293=CARTESIAN_POINT('Ctrl Pts',(-0.0735613784355843,0.114542101371374,
1.51419539934302));
#16294=CARTESIAN_POINT('Ctrl Pts',(-0.0776398170223455,0.110855132244726,
1.51495518495604));
#16295=CARTESIAN_POINT('Ctrl Pts',(-0.0814741368103916,0.106911749311875,
1.51572224163114));
#16296=CARTESIAN_POINT('Ctrl Pts',(-0.0845038784997064,0.103795829845314,
1.51632834224744));
#16297=CARTESIAN_POINT('Ctrl Pts',(-0.087381117690253,0.10051973853988,
1.51693898261853));
#16298=CARTESIAN_POINT('Ctrl Pts',(-0.0900959757046659,0.0970973798321736,
1.51755501917095));
#16299=CARTESIAN_POINT('Ctrl Pts',(-0.0920052356275281,0.0946905606587243,
1.51798825505079));
#16300=CARTESIAN_POINT('Ctrl Pts',(-0.093830595110286,0.092215607777745,
1.51842338946406));
#16301=CARTESIAN_POINT('Ctrl Pts',(-0.0955653742165971,0.0896840982544811,
1.51885969689116));
#16302=CARTESIAN_POINT('Ctrl Pts',(-0.0997851775729162,0.0835262696618028,
1.51992100293214));
#16303=CARTESIAN_POINT('Ctrl Pts',(-0.103479134251024,0.0770231540939269,
1.52099120961793));
#16304=CARTESIAN_POINT('Ctrl Pts',(-0.106606394578922,0.0702509006766953,
1.52207541818308));
#16305=CARTESIAN_POINT('Ctrl Pts',(-0.108879606303698,0.0653281362576702,
1.52286353153598));
#16306=CARTESIAN_POINT('Ctrl Pts',(-0.110852991156964,0.0602629640702717,
1.52365904329275));
#16307=CARTESIAN_POINT('Ctrl Pts',(-0.112503888351057,0.0550849881514033,
1.524463912762));
#16308=CARTESIAN_POINT('Ctrl Pts',(-0.113450017754745,0.0521174894567802,
1.52492518356294));
#16309=CARTESIAN_POINT('Ctrl Pts',(-0.114289979676541,0.0491121240008169,
1.52538965304266));
#16310=CARTESIAN_POINT('Ctrl Pts',(-0.115015874151616,0.0460903162170444,
1.52585530945224));
#16311=CARTESIAN_POINT('Ctrl Pts',(-0.117053612444637,0.0376074669234184,
1.52716250482259));
#16312=CARTESIAN_POINT('Ctrl Pts',(-0.118206139871793,0.0289652499882669,
1.52848357355921));
#16313=CARTESIAN_POINT('Ctrl Pts',(-0.11838625730212,0.0202925750432425,
1.52982832573377));
#16314=CARTESIAN_POINT('Ctrl Pts',(-0.118492077855379,0.015197303257165,
1.53061837930521));
#16315=CARTESIAN_POINT('Ctrl Pts',(-0.118261361656021,0.0100916471271278,
1.53141660760476));
#16316=CARTESIAN_POINT('Ctrl Pts',(-0.11766859746431,0.00500517689818842,
1.532225));
#16317=CARTESIAN_POINT('',(-0.115079981391543,0.0902137050004572,1.50365));
#16318=CARTESIAN_POINT('Origin',(0.,0.,1.50365));
#16319=CARTESIAN_POINT('Ctrl Pts',(-0.143238079070951,-6.41379011939899E-6,
1.50700023577028));
#16320=CARTESIAN_POINT('Ctrl Pts',(-0.143514357617001,0.00795674345750163,
1.50671802038504));
#16321=CARTESIAN_POINT('Ctrl Pts',(-0.14306421847979,0.0159310909218757,
1.50643710681857));
#16322=CARTESIAN_POINT('Ctrl Pts',(-0.141940608246003,0.023841490005315,
1.50615648267927));
#16323=CARTESIAN_POINT('Ctrl Pts',(-0.141317731836386,0.0282266413964,1.50600091791928));
#16324=CARTESIAN_POINT('Ctrl Pts',(-0.14048752132733,0.0325921818867556,
1.50584544210227));
#16325=CARTESIAN_POINT('Ctrl Pts',(-0.139456452513291,0.0369250818702156,
1.5056898827608));
#16326=CARTESIAN_POINT('Ctrl Pts',(-0.138790989895207,0.0397215809279161,
1.50558948313156));
#16327=CARTESIAN_POINT('Ctrl Pts',(-0.138042009924554,0.0425029011667524,
1.50548910366784));
#16328=CARTESIAN_POINT('Ctrl Pts',(-0.137214434473447,0.0452564915355094,
1.50538902890071));
#16329=CARTESIAN_POINT('Ctrl Pts',(-0.134176751889031,0.0553637675507716,
1.50502169637912));
#16330=CARTESIAN_POINT('Ctrl Pts',(-0.130076454936343,0.0651325632434767,
1.50465723703036));
#16331=CARTESIAN_POINT('Ctrl Pts',(-0.125018127980614,0.0743940890034878,
1.50429344851366));
#16332=CARTESIAN_POINT('Ctrl Pts',(-0.122034683484208,0.0798566160996726,
1.50407888293545));
#16333=CARTESIAN_POINT('Ctrl Pts',(-0.118716925567465,0.0851425936725427,
1.50386455072235));
#16334=CARTESIAN_POINT('Ctrl Pts',(-0.115078604842436,0.0902138214954005,
1.50365));
#16335=CARTESIAN_POINT('',(-0.05,-6.12323399573677E-18,1.6));
#16336=CARTESIAN_POINT('',(-0.1,-1.22464679914735E-17,1.55));
#16337=CARTESIAN_POINT('Origin',(0.,0.,1.6));
#16338=CARTESIAN_POINT('Ctrl Pts',(0.0850780204044575,-0.11908002747757,
-0.0164977839420936));
#16339=CARTESIAN_POINT('Ctrl Pts',(0.124677800165771,-0.0907875342533835,
-0.0138514540629917));
#16340=CARTESIAN_POINT('Ctrl Pts',(0.172751483861701,0.00791416360185712,
-0.00855879430478784));
#16341=CARTESIAN_POINT('Ctrl Pts',(0.0868617128612901,0.149726167188418,
-0.000619804667482127));
#16342=CARTESIAN_POINT('Ctrl Pts',(-0.078614020905812,0.154028602276276,
0.00731918496982359));
#16343=CARTESIAN_POINT('Ctrl Pts',(-0.172087192378165,0.0175525219725009,
0.0152581746071293));
#16344=CARTESIAN_POINT('Ctrl Pts',(-0.108045720411827,-0.135108484733225,
0.0231971642444351));
#16345=CARTESIAN_POINT('Ctrl Pts',(0.0549144151285058,-0.164025561655164,
0.0311361538817407));
#16346=CARTESIAN_POINT('Ctrl Pts',(0.167598788591005,-0.0428207868793744,
0.0390751435190465));
#16347=CARTESIAN_POINT('Ctrl Pts',(0.126860790413016,0.117600499296196,
0.0470141331563521));
#16348=CARTESIAN_POINT('Ctrl Pts',(-0.0300110592737492,0.170357625684536,
0.054953122793658));
#16349=CARTESIAN_POINT('Ctrl Pts',(-0.159409054995301,0.0671687418111174,
0.0628921124309635));
#16350=CARTESIAN_POINT('Ctrl Pts',(-0.142879399887002,-0.0975110083167992,
0.0708311020682695));
#16351=CARTESIAN_POINT('Ctrl Pts',(0.00444677171871267,-0.172924803493063,
0.078770091705575));
#16352=CARTESIAN_POINT('Ctrl Pts',(0.147702113712341,-0.0900384822365835,
0.0867090813428809));
#16353=CARTESIAN_POINT('Ctrl Pts',(0.155746353789385,0.0752722621313087,
0.0946480709801864));
#16354=CARTESIAN_POINT('Ctrl Pts',(0.021215449100004,0.17167621786987,0.102587060617492));
#16355=CARTESIAN_POINT('Ctrl Pts',(-0.132736728465598,0.110922462699857,
0.110526050254798));
#16356=CARTESIAN_POINT('Ctrl Pts',(-0.165177537004225,-0.0513732581591355,
0.118465039892104));
#16357=CARTESIAN_POINT('Ctrl Pts',(-0.0464096261145344,-0.166640254043574,
0.126404029529409));
#16358=CARTESIAN_POINT('Ctrl Pts',(0.114843114370719,-0.129359532685675,
0.134343019166715));
#16359=CARTESIAN_POINT('Ctrl Pts',(0.170964855654229,0.0263409830179588,
0.142282008804021));
#16360=CARTESIAN_POINT('Ctrl Pts',(0.0705799878925336,0.157928129946847,
0.150220998441327));
#16361=CARTESIAN_POINT('Ctrl Pts',(-0.0944160212638482,0.144942899583874,
0.158159988078632));
#16362=CARTESIAN_POINT('Ctrl Pts',(-0.172980633894512,-0.000727622896455919,
0.166098977715938));
#16363=CARTESIAN_POINT('Ctrl Pts',(-0.0931933312323777,-0.145732055885043,
0.174037967353244));
#16364=CARTESIAN_POINT('Ctrl Pts',(0.0719060791645076,-0.157328779695546,
0.181976956990549));
#16365=CARTESIAN_POINT('Ctrl Pts',(0.171180402159323,-0.0249017879745179,
0.189915946627855));
#16366=CARTESIAN_POINT('Ctrl Pts',(0.113750798721884,0.13032108391891,0.197854936265161));
#16367=CARTESIAN_POINT('Ctrl Pts',(-0.0478098650864174,0.16624393501773,
0.205793925902467));
#16368=CARTESIAN_POINT('Ctrl Pts',(-0.16560387403618,0.0499818570245514,
0.213732915539772));
#16369=CARTESIAN_POINT('Ctrl Pts',(-0.131798885878402,-0.112035185581475,
0.221671905177078));
#16370=CARTESIAN_POINT('Ctrl Pts',(0.0226589495323734,-0.171491694067101,
0.229610894814384));
#16371=CARTESIAN_POINT('Ctrl Pts',(0.156374069566079,-0.073959309724122,
0.237549884451689));
#16372=CARTESIAN_POINT('Ctrl Pts',(0.146939445926624,0.0912777539068999,
0.245488874088995));
#16373=CARTESIAN_POINT('Ctrl Pts',(0.00299182995941577,0.172956289510158,
0.253427863726301));
#16374=CARTESIAN_POINT('Ctrl Pts',(-0.143694601292225,0.0963051955349955,
0.261366853363607));
#16375=CARTESIAN_POINT('Ctrl Pts',(-0.15883847309497,-0.0685067047260848,
0.269305843000912));
#16376=CARTESIAN_POINT('Ctrl Pts',(-0.0285766086907934,-0.170605411881679,
0.277244832638218));
#16377=CARTESIAN_POINT('Ctrl Pts',(0.12784518248692,-0.116526556812001,
0.285183822275524));
#16378=CARTESIAN_POINT('Ctrl Pts',(0.167233470900423,0.0442243749325307,
0.293122811912829));
#16379=CARTESIAN_POINT('Ctrl Pts',(0.0535309779628647,0.164490922320707,
0.301061801550136));
#16380=CARTESIAN_POINT('Ctrl Pts',(-0.109175456582181,0.134177303623408,
0.309000791187441));
#16381=CARTESIAN_POINT('Ctrl Pts',(-0.171939242908932,-0.0189664407699395,
0.316939780824747));
#16382=CARTESIAN_POINT('Ctrl Pts',(-0.0773044361184472,-0.154747708493488,
0.324878770462053));
#16383=CARTESIAN_POINT('Ctrl Pts',(0.0880972839194656,-0.148868054644337,
0.332817760099358));
#16384=CARTESIAN_POINT('Ctrl Pts',(0.172851978230285,-0.00670989936239309,
0.340756749736664));
#16385=CARTESIAN_POINT('Ctrl Pts',(0.0993725327910066,0.141590708926387,
0.34869573937397));
#16386=CARTESIAN_POINT('Ctrl Pts',(-0.0650756559739905,0.160274727038081,
0.356634729011275));
#16387=CARTESIAN_POINT('Ctrl Pts',(-0.169951541620772,0.0322382168908211,
0.364573718648582));
#16388=CARTESIAN_POINT('Ctrl Pts',(-0.119248438453561,-0.125310171390688,
0.372512708285886));
#16389=CARTESIAN_POINT('Ctrl Pts',(0.0406184374886585,-0.168145685830938,
0.380451697923193));
#16390=CARTESIAN_POINT('Ctrl Pts',(0.163301917673335,-0.0570553486694088,
0.388390687560498));
#16391=CARTESIAN_POINT('Ctrl Pts',(0.136493684039406,0.106265249940549,
0.396329677197804));
#16392=CARTESIAN_POINT('Ctrl Pts',(-0.0152651628095069,0.172307295063139,
0.404268666835109));
#16393=CARTESIAN_POINT('Ctrl Pts',(-0.153049799296248,0.0806138205455782,
0.412207656472416));
#16394=CARTESIAN_POINT('Ctrl Pts',(-0.150727833715048,-0.0848760818555219,
0.420146646109721));
#16395=CARTESIAN_POINT('Ctrl Pts',(-0.0104248664208018,-0.172667748255674,
0.428085635747027));
#16396=CARTESIAN_POINT('Ctrl Pts',(0.139421351618932,-0.10239392482138,
0.436024625384332));
#16397=CARTESIAN_POINT('Ctrl Pts',(0.16163687742079,0.0616145192729195,
0.443963615021638));
#16398=CARTESIAN_POINT('Ctrl Pts',(0.0358849196425865,0.169219093691645,
0.451902604658944));
#16399=CARTESIAN_POINT('Ctrl Pts',(-0.122717222714247,0.121915185177559,
0.45984159429625));
#16400=CARTESIAN_POINT('Ctrl Pts',(-0.168980158036723,-0.0369937199732681,
0.467780583933555));
#16401=CARTESIAN_POINT('Ctrl Pts',(-0.0605533396431397,-0.162037409833775,
0.475719573570861));
#16402=CARTESIAN_POINT('Ctrl Pts',(0.103305911202344,-0.138746956140414,
0.483658563208167));
#16403=CARTESIAN_POINT('Ctrl Pts',(0.172595680358559,0.0115568269495825,
0.491597552845473));
#16404=CARTESIAN_POINT('Ctrl Pts',(0.0838859329010004,0.151281127008313,
0.499536542482778));
#16405=CARTESIAN_POINT('Ctrl Pts',(-0.0816156370489812,0.152517923263679,
0.507475532120084));
#16406=CARTESIAN_POINT('Ctrl Pts',(-0.172403684765527,0.0141350135070757,
0.51541452175739));
#16407=CARTESIAN_POINT('Ctrl Pts',(-0.105367974675403,-0.137187532379513,
0.523353511394695));
#16408=CARTESIAN_POINT('Ctrl Pts',(0.0581248948911363,-0.162924294448283,
0.531292501032001));
#16409=CARTESIAN_POINT('Ctrl Pts',(0.168408406744046,-0.039515030880773,
0.539231490669306));
#16410=CARTESIAN_POINT('Ctrl Pts',(0.124525564004667,0.120067535316156,
0.547170480306613));
#16411=CARTESIAN_POINT('Ctrl Pts',(-0.0333518982867267,0.169736501696743,
0.555109469943918));
#16412=CARTESIAN_POINT('Ctrl Pts',(-0.160697983451488,0.0640233335761385,
0.563048459581225));
#16413=CARTESIAN_POINT('Ctrl Pts',(-0.14093607811848,-0.100298808627811,
0.570987449218529));
#16414=CARTESIAN_POINT('Ctrl Pts',(0.00784314775175556,-0.172804265459278,
0.578926438855836));
#16415=CARTESIAN_POINT('Ctrl Pts',(0.149442509381278,-0.0871192603125336,
0.586865428493141));
#16416=CARTESIAN_POINT('Ctrl Pts',(0.154237495636292,0.0783174569774929,
0.594804418130446));
#16417=CARTESIAN_POINT('Ctrl Pts',(0.0178386252221998,0.172059909850489,
0.602743407767753));
#16418=CARTESIAN_POINT('Ctrl Pts',(-0.134890284021987,0.108293307291099,
0.610682397405058));
#16419=CARTESIAN_POINT('Ctrl Pts',(-0.164136382878957,-0.0546083962682395,
0.618621387042364));
#16420=CARTESIAN_POINT('Ctrl Pts',(-0.0431268722112106,-0.167519855601819,
0.62656037667967));
#16421=CARTESIAN_POINT('Ctrl Pts',(0.117362334288317,-0.127078368017432,
0.634499366316975));
#16422=CARTESIAN_POINT('Ctrl Pts',(0.170414367112955,0.0296946562375699,
0.642438355954282));
#16423=CARTESIAN_POINT('Ctrl Pts',(0.0674637261050104,0.159284257814778,
0.650377345591586));
#16424=CARTESIAN_POINT('Ctrl Pts',(-0.0972453325609638,0.143060037825677,
0.658316335228894));
#16425=CARTESIAN_POINT('Ctrl Pts',(-0.172932953925271,-0.00412584224812367,
0.666255324866198));
#16426=CARTESIAN_POINT('Ctrl Pts',(-0.0903123078403481,-0.147534796506203,
0.674194314503505));
#16427=CARTESIAN_POINT('Ctrl Pts',(0.0749830665657334,-0.155885755782802,
0.68213330414081));
#16428=CARTESIAN_POINT('Ctrl Pts',(0.17163658245605,-0.021533989188811,
0.690072293778116));
#16429=CARTESIAN_POINT('Ctrl Pts',(0.11116857013107,0.132530668686874,0.698011283415421));
#16430=CARTESIAN_POINT('Ctrl Pts',(-0.0510666492692211,0.165272582299639,
0.705950273052727));
#16431=CARTESIAN_POINT('Ctrl Pts',(-0.166553851089581,0.0467187736868841,
0.713889262690032));
#16432=CARTESIAN_POINT('Ctrl Pts',(-0.129572416918314,-0.114602870389546,
0.721828252327339));
#16433=CARTESIAN_POINT('Ctrl Pts',(0.0260236847639906,-0.171013440871999,
0.729767241964644));
#16434=CARTESIAN_POINT('Ctrl Pts',(0.157796886564457,-0.0708729265526718,
0.73770623160195));
#16435=CARTESIAN_POINT('Ctrl Pts',(0.145117853242075,0.0941468947867542,
0.745645221239255));
#16436=CARTESIAN_POINT('Ctrl Pts',(-0.000406629147419015,0.172981686256994,
0.753584210876562));
#16437=CARTESIAN_POINT('Ctrl Pts',(-0.145558870420566,0.0934635991681543,
0.761523200513868));
#16438=CARTESIAN_POINT('Ctrl Pts',(-0.157461941624574,-0.0716140074803496,
0.769462190151172));
#16439=CARTESIAN_POINT('Ctrl Pts',(-0.0252193968429213,-0.17113389830906,
0.777401179788479));
#16440=CARTESIAN_POINT('Ctrl Pts',(0.130109777350283,-0.113992433807847,
0.785340169425784));
#16441=CARTESIAN_POINT('Ctrl Pts',(0.166332367384696,0.0475012914327479,
0.793279159063091));
#16442=CARTESIAN_POINT('Ctrl Pts',(0.0502890745800368,0.165510839842773,
0.801218148700395));
#16443=CARTESIAN_POINT('Ctrl Pts',(-0.111790419467279,0.132006557575396,
0.809157138337702));
#16444=CARTESIAN_POINT('Ctrl Pts',(-0.171533445990104,-0.0223406811520247,
0.817096127975007));
#16445=CARTESIAN_POINT('Ctrl Pts',(-0.0742493586638003,-0.156236557391639,
0.825035117612313));
#16446=CARTESIAN_POINT('Ctrl Pts',(0.0910049278783345,-0.147108572929777,
0.832974107249618));
#16447=CARTESIAN_POINT('Ctrl Pts',(0.172950439922886,-0.00331277195964383,
0.840913096886925));
#16448=CARTESIAN_POINT('Ctrl Pts',(0.0965716772857839,0.143515644700454,
0.848852086524229));
#16449=CARTESIAN_POINT('Ctrl Pts',(-0.0682118374171683,0.158965324406771,
0.856791076161536));
#16450=CARTESIAN_POINT('Ctrl Pts',(-0.170552089827228,0.0288931442238776,
0.864730065798841));
#16451=CARTESIAN_POINT('Ctrl Pts',(-0.116763592698541,-0.127628729319482,
0.872669055436147));
#16452=CARTESIAN_POINT('Ctrl Pts',(0.0439139712140358,-0.167315248138923,
0.880608045073453));
#16453=CARTESIAN_POINT('Ctrl Pts',(0.164391304101163,-0.0538361241500125,
0.888547034710759));
#16454=CARTESIAN_POINT('Ctrl Pts',(0.134379664555536,0.108926281867684,
0.896486024348063));
#16455=CARTESIAN_POINT('Ctrl Pts',(-0.018647348250808,0.17197414204115,
0.904425013985371));
#16456=CARTESIAN_POINT('Ctrl Pts',(-0.154603991719776,0.0775914613336281,
0.912364003622676));
#16457=CARTESIAN_POINT('Ctrl Pts',(-0.149031276472826,-0.0878208845346985,
0.920302993259982));
#16458=CARTESIAN_POINT('Ctrl Pts',(-0.00703064139541984,-0.172839229369798,
0.928241982897287));
#16459=CARTESIAN_POINT('Ctrl Pts',(0.141406064038169,-0.099635105162837,
0.936180972534593));
#16460=CARTESIAN_POINT('Ctrl Pts',(0.160395209035295,0.064778129380991,
0.944119962171899));
#16461=CARTESIAN_POINT('Ctrl Pts',(0.03255353276219,0.169891426011666,0.952058951809204));
#16462=CARTESIAN_POINT('Ctrl Pts',(-0.125088671715395,0.119480765548496,
0.959997941446511));
#16463=CARTESIAN_POINT('Ctrl Pts',(-0.168220770124088,-0.040306347222682,
0.967936931083815));
#16464=CARTESIAN_POINT('Ctrl Pts',(-0.0573582824064844,-0.163195761485875,
0.975875920721122));
#16465=CARTESIAN_POINT('Ctrl Pts',(0.106011781834435,-0.136690640644722,
0.983814910358427));
#16466=CARTESIAN_POINT('Ctrl Pts',(0.17233532526783,0.014945393685262,0.991753899995733));
#16467=CARTESIAN_POINT('Ctrl Pts',(0.0808976893297158,0.152899944371113,
0.999692889633039));
#16468=CARTESIAN_POINT('Ctrl Pts',(-0.0845962369090198,0.150885074902754,
1.00763187927034));
#16469=CARTESIAN_POINT('Ctrl Pts',(-0.172648106016301,0.0107452601904448,
1.01557086890765));
#16470=CARTESIAN_POINT('Ctrl Pts',(-0.102652466413112,-0.13923110380544,
1.02350985854496));
#16471=CARTESIAN_POINT('Ctrl Pts',(0.0613144709582997,-0.161750934398167,
1.03144884818226));
#16472=CARTESIAN_POINT('Ctrl Pts',(0.169152212322519,-0.0361988700648799,
1.03938783781957));
#16473=CARTESIAN_POINT('Ctrl Pts',(0.122142696063681,0.12249077894222,1.04732682745687));
#16474=CARTESIAN_POINT('Ctrl Pts',(-0.0366800874558037,0.169048514669047,
1.05526581709418));
#16475=CARTESIAN_POINT('Ctrl Pts',(-0.161924764760067,0.0608539208677085,
1.06320480673148));
#16476=CARTESIAN_POINT('Ctrl Pts',(-0.138938417355371,-0.103048266896446,
1.07114379636879));
#16477=CARTESIAN_POINT('Ctrl Pts',(0.011236529066559,-0.172616828675865,
1.0790827860061));
#16478=CARTESIAN_POINT('Ctrl Pts',(0.151125203217684,-0.0841665140064042,
1.0870217756434));
#16479=CARTESIAN_POINT('Ctrl Pts',(0.152669111109608,0.0813324759279986,
1.09496076528071));
#16480=CARTESIAN_POINT('Ctrl Pts',(0.0144549108781955,0.172377158228925,
1.10289975491801));
#16481=CARTESIAN_POINT('Ctrl Pts',(-0.136991769602464,0.10562236594946,
1.11083874455532));
#16482=CARTESIAN_POINT('Ctrl Pts',(-0.163031873671196,-0.0578224635832477,
1.11877773419263));
#16483=CARTESIAN_POINT('Ctrl Pts',(-0.0398274706979539,-0.168334790537727,
1.12671672382993));
#16484=CARTESIAN_POINT('Ctrl Pts',(0.119836252144435,-0.124748153491552,
1.13465571346724));
#16485=CARTESIAN_POINT('Ctrl Pts',(0.169798099063322,0.0330368685268242,
1.14259470310454));
#16486=CARTESIAN_POINT('Ctrl Pts',(0.0643214233134591,0.160578901573361,
1.15053369274185));
#16487=CARTESIAN_POINT('Ctrl Pts',(-0.100037107244844,0.141121955420339,
1.15847268237915));
#16488=CARTESIAN_POINT('Ctrl Pts',(-0.172818522111203,-0.00752246920075927,
1.16641167201646));
#16489=CARTESIAN_POINT('Ctrl Pts',(-0.0873964240115842,-0.149280588817046,
1.17435066165376));
#16490=CARTESIAN_POINT('Ctrl Pts',(0.0780311106025284,-0.154382560238235,
1.18228965129107));
#16491=CARTESIAN_POINT('Ctrl Pts',(0.172026511281289,-0.01815787828917,
1.19022864092837));
#16492=CARTESIAN_POINT('Ctrl Pts',(0.10854343062882,0.134689096792963,1.19816763056568));
#16493=CARTESIAN_POINT('Ctrl Pts',(-0.0543037217972188,0.164237434607784,
1.20610662020299));
#16494=CARTESIAN_POINT('Ctrl Pts',(-0.167439538594998,0.0434376569656869,
1.21404560984029));
#16495=CARTESIAN_POINT('Ctrl Pts',(-0.127295933190098,-0.117126318651471,
1.2219845994776));
#16496=CARTESIAN_POINT('Ctrl Pts',(0.0293783748903316,-0.170469176734012,
1.2299235891149));
#16497=CARTESIAN_POINT('Ctrl Pts',(0.159158794190081,-0.0677591865323411,
1.23786257875221));
#16498=CARTESIAN_POINT('Ctrl Pts',(0.143240245273553,0.0969796950995427,
1.24580156838952));
#16499=CARTESIAN_POINT('Ctrl Pts',(-0.00380493129617075,0.172940312320012,
1.25374055802682));
#16500=CARTESIAN_POINT('Ctrl Pts',(-0.147366954032488,0.0905859259858403,
1.26167954766413));
#16501=CARTESIAN_POINT('Ctrl Pts',(-0.156024630070406,-0.074693667330688,
1.26961853730143));
#16502=CARTESIAN_POINT('Ctrl Pts',(-0.0218524503424686,-0.171596327294885,
1.27755752693874));
#16503=CARTESIAN_POINT('Ctrl Pts',(0.132324150022753,-0.111414309889572,
1.28549651657604));
#16504=CARTESIAN_POINT('Ctrl Pts',(0.165367059817933,0.0507598725070622,
1.29343550621335));
#16505=CARTESIAN_POINT('Ctrl Pts',(0.0470277596764783,0.166466870408131,
1.30137449585065));
#16506=CARTESIAN_POINT('Ctrl Pts',(-0.114362231391601,0.129784857201791,
1.30931348548797));
#16507=CARTESIAN_POINT('Ctrl Pts',(-0.171061437441431,-0.0257062980954763,
1.31725247512526));
#16508=CARTESIAN_POINT('Ctrl Pts',(-0.071165620995849,-0.157665099140374,
1.32519146476257));
#16509=CARTESIAN_POINT('Ctrl Pts',(0.0938774439379855,-0.145292307632914,
1.33313045439988));
#16510=CARTESIAN_POINT('Ctrl Pts',(0.172982143233999,8.56343898915854E-5,
1.34106944403719));
#16511=CARTESIAN_POINT('Ctrl Pts',(0.0937335447930804,0.145385183220099,
1.34900843367449));
#16512=CARTESIAN_POINT('Ctrl Pts',(-0.0713216883190155,0.157594562185848,
1.3569474233118));
#16513=CARTESIAN_POINT('Ctrl Pts',(-0.171086806821499,0.0255369173285507,
1.3648864129491));
#16514=CARTESIAN_POINT('Ctrl Pts',(-0.114233673229396,-0.129898019862958,
1.37282540258641));
#16515=CARTESIAN_POINT('Ctrl Pts',(0.0471925482590101,-0.166420232464351,
1.38076439222371));
#16516=CARTESIAN_POINT('Ctrl Pts',(0.165417247017141,-0.0505961085897048,
1.38870338186102));
#16517=CARTESIAN_POINT('Ctrl Pts',(0.132213753266125,0.111545248710567,
1.39664237149832));
#16518=CARTESIAN_POINT('Ctrl Pts',(-0.0220222951247444,0.17157464463752,
1.40458136113563));
#16519=CARTESIAN_POINT('Ctrl Pts',(-0.156098584526576,0.0745390809398717,
1.41252035077293));
#16520=CARTESIAN_POINT('Ctrl Pts',(-0.147277046608992,-0.0907316537045687,
1.42045934041024));
#16521=CARTESIAN_POINT('Ctrl Pts',(-0.00363398118293899,-0.172944250658386,
1.42839833004755));
#16522=CARTESIAN_POINT('Ctrl Pts',(0.143336722904634,-0.0968373407211472,
1.43633731968485));
#16523=CARTESIAN_POINT('Ctrl Pts',(0.159090624036536,0.0679158129692223,
1.44427630932216));
#16524=CARTESIAN_POINT('Ctrl Pts',(0.0292114869387437,0.170499931406899,
1.45221529895946));
#16525=CARTESIAN_POINT('Ctrl Pts',(-0.127415456569397,0.116996902323752,
1.46015428859677));
#16526=CARTESIAN_POINT('Ctrl Pts',(-0.167389576437263,-0.0435971050111283,
1.46809327823408));
#16527=CARTESIAN_POINT('Ctrl Pts',(-0.0541541359620402,-0.164303103757731,
1.47603226787138));
#16528=CARTESIAN_POINT('Ctrl Pts',(0.108701533888403,-0.13455879509903,
1.48397125750869));
#16529=CARTESIAN_POINT('Ctrl Pts',(0.171961157005542,0.0182848320604298,
1.49191024714599));
#16530=CARTESIAN_POINT('Ctrl Pts',(0.0779697431325927,0.154543202561513,
1.4998492367833));
#16531=CARTESIAN_POINT('Ctrl Pts',(-0.0877325682749983,0.149025855561406,
1.5077882264206));
#16532=CARTESIAN_POINT('Ctrl Pts',(-0.144149484752264,0.0548439265155397,
1.51308088617881));
#16533=CARTESIAN_POINT('Ctrl Pts',(-0.146217781693078,0.00621955116994065,
1.51572721605791));
#16534=CARTESIAN_POINT('Ctrl Pts',(0.0795408277542855,-0.111329858282327,
-0.0109985226280624));
#16535=CARTESIAN_POINT('Ctrl Pts',(0.116563307192903,-0.0848787452970238,
-0.00835219274896048));
#16536=CARTESIAN_POINT('Ctrl Pts',(0.16150817751539,0.00739908052493189,
-0.00305953299075667));
#16537=CARTESIAN_POINT('Ctrl Pts',(0.0812084309002137,0.139981433724326,
0.00487945664654907));
#16538=CARTESIAN_POINT('Ctrl Pts',(-0.0734975292821143,0.144003850402812,
0.0128184462838548));
#16539=CARTESIAN_POINT('Ctrl Pts',(-0.160887120581772,0.0164101388376342,
0.0207574359211605));
#16540=CARTESIAN_POINT('Ctrl Pts',(-0.101013704785435,-0.126315124179183,
0.0286964255584662));
#16541=CARTESIAN_POINT('Ctrl Pts',(0.0513403816191153,-0.153350170642076,
0.0366354151957719));
#16542=CARTESIAN_POINT('Ctrl Pts',(0.156690838735662,-0.0400338514845966,
0.0445744048330777));
#16543=CARTESIAN_POINT('Ctrl Pts',(0.118604220350264,0.109946623274354,
0.0525133944703833));
#16544=CARTESIAN_POINT('Ctrl Pts',(-0.0280578283917351,0.15927012049393,
0.0604523841076892));
#16545=CARTESIAN_POINT('Ctrl Pts',(-0.14903412333264,0.0627971513379326,
0.0683913737449947));
#16546=CARTESIAN_POINT('Ctrl Pts',(-0.133580279395553,-0.0911646307683348,
0.0763303633823007));
#16547=CARTESIAN_POINT('Ctrl Pts',(0.0041573593468571,-0.161670216863261,
0.0842693530196062));
#16548=CARTESIAN_POINT('Ctrl Pts',(0.138089113144455,-0.0841784443595545,
0.0922083426569122));
#16549=CARTESIAN_POINT('Ctrl Pts',(0.14560980428584,0.0703732645446943,
0.100147332294218));
#16550=CARTESIAN_POINT('Ctrl Pts',(0.0198346691022095,0.160502893816501,
0.108086321931524));
#16551=CARTESIAN_POINT('Ctrl Pts',(-0.124097730593135,0.103703218031488,
0.116025311568829));
#16552=CARTESIAN_POINT('Ctrl Pts',(-0.154427171169137,-0.0480296962598115,
0.123964301206135));
#16553=CARTESIAN_POINT('Ctrl Pts',(-0.0433891157712434,-0.155794689166463,
0.13190329084344));
#16554=CARTESIAN_POINT('Ctrl Pts',(0.107368699171666,-0.12094033522185,
0.139842280480747));
#16555=CARTESIAN_POINT('Ctrl Pts',(0.15983782968835,0.0246266142906177,
0.147781270118052));
#16556=CARTESIAN_POINT('Ctrl Pts',(0.0659863808909888,0.147649582370873,
0.155720259755358));
#16557=CARTESIAN_POINT('Ctrl Pts',(-0.0882710769349216,0.135509478890084,
0.163659249392663));
#16558=CARTESIAN_POINT('Ctrl Pts',(-0.161722413615419,-0.00068026650363694,
0.171598239029969));
#16559=CARTESIAN_POINT('Ctrl Pts',(-0.0871279640988751,-0.136247273976568,
0.179537228667275));
#16560=CARTESIAN_POINT('Ctrl Pts',(0.0672261652318651,-0.147089240053593,
0.187476218304581));
#16561=CARTESIAN_POINT('Ctrl Pts',(0.160039347628626,-0.023281087390596,
0.195415207941886));
#16562=CARTESIAN_POINT('Ctrl Pts',(0.106347475470598,0.121839305139765,
0.203354197579192));
#16563=CARTESIAN_POINT('Ctrl Pts',(-0.0446982220051161,0.15542416405057,
0.211293187216498));
#16564=CARTESIAN_POINT('Ctrl Pts',(-0.154825760608133,0.0467288526640558,
0.219232176853804));
#16565=CARTESIAN_POINT('Ctrl Pts',(-0.12322092627477,-0.104743520787053,
0.227171166491109));
#16566=CARTESIAN_POINT('Ctrl Pts',(0.0211842211805034,-0.160330379506191,
0.235110156128415));
#16567=CARTESIAN_POINT('Ctrl Pts',(0.146196665995071,-0.0691457639426259,
0.24304914576572));
#16568=CARTESIAN_POINT('Ctrl Pts',(0.137376082602736,0.0853370596399817,
0.250988135403027));
#16569=CARTESIAN_POINT('Ctrl Pts',(0.00279711058556459,0.161699653653757,
0.258927125040332));
#16570=CARTESIAN_POINT('Ctrl Pts',(-0.134342424474264,0.0900372967480426,
0.266866114677638));
#16571=CARTESIAN_POINT('Ctrl Pts',(-0.148500677015507,-0.0640480346713102,
0.274805104314944));
#16572=CARTESIAN_POINT('Ctrl Pts',(-0.0267167371651392,-0.159501779847699,
0.282744093952249));
#16573=CARTESIAN_POINT('Ctrl Pts',(0.119524544542348,-0.108942576944327,
0.290683083589556));
#16574=CARTESIAN_POINT('Ctrl Pts',(0.156349297273321,0.0413460888291301,
0.29862207322686));
#16575=CARTESIAN_POINT('Ctrl Pts',(0.0500469836677093,0.153785243912065,
0.306561062864167));
#16576=CARTESIAN_POINT('Ctrl Pts',(-0.102069913541897,0.125444547784578,
0.314500052501472));
#16577=CARTESIAN_POINT('Ctrl Pts',(-0.160748800211922,-0.0177320345633525,
0.322439042138778));
#16578=CARTESIAN_POINT('Ctrl Pts',(-0.0722731771226978,-0.144676154524232,
0.330378031776084));
#16579=CARTESIAN_POINT('Ctrl Pts',(0.082363586418043,-0.139179170322594,
0.338317021413389));
#16580=CARTESIAN_POINT('Ctrl Pts',(0.16160213133829,-0.00627319426210969,
0.346256011050695));
#16581=CARTESIAN_POINT('Ctrl Pts',(0.0929050003357002,0.132375461215256,
0.354195000688001));
#16582=CARTESIAN_POINT('Ctrl Pts',(-0.0608402912787218,0.149843454232904,
0.362133990325306));
#16583=CARTESIAN_POINT('Ctrl Pts',(-0.158890465884947,0.0301400343429239,
0.370072979962613));
#16584=CARTESIAN_POINT('Ctrl Pts',(-0.1114873084483,-0.117154521356547,
0.378011969599918));
#16585=CARTESIAN_POINT('Ctrl Pts',(0.0379748391485164,-0.157202141877815,
0.385950959237223));
#16586=CARTESIAN_POINT('Ctrl Pts',(0.152673624090564,-0.0533419752763387,
0.39388994887453));
#16587=CARTESIAN_POINT('Ctrl Pts',(0.127610169584502,0.0993491139263089,
0.401828938511835));
#16588=CARTESIAN_POINT('Ctrl Pts',(-0.014271649480085,0.16109289816887,
0.409767928149142));
#16589=CARTESIAN_POINT('Ctrl Pts',(-0.143088751545671,0.0753671745551693,
0.417706917786446));
#16590=CARTESIAN_POINT('Ctrl Pts',(-0.140917908083783,-0.0793520321139836,
0.425645907423752));
#16591=CARTESIAN_POINT('Ctrl Pts',(-0.00974637750615997,-0.161429891732714,
0.433584897061058));
#16592=CARTESIAN_POINT('Ctrl Pts',(0.130347293715478,-0.0957297489831606,
0.441523886698364));
#16593=CARTESIAN_POINT('Ctrl Pts',(0.15111695082405,0.0576044181723055,
0.449462876335669));
#16594=CARTESIAN_POINT('Ctrl Pts',(0.0335493961742207,0.158205688379633,
0.457401865972975));
#16595=CARTESIAN_POINT('Ctrl Pts',(-0.114730331382826,0.113980493419335,
0.465340855610281));
#16596=CARTESIAN_POINT('Ctrl Pts',(-0.157982303542021,-0.03458603167299,
0.473279845247587));
#16597=CARTESIAN_POINT('Ctrl Pts',(-0.0566123040428622,-0.151491415104245,
0.481218834884892));
#16598=CARTESIAN_POINT('Ctrl Pts',(0.0965823799129518,-0.129716790392294,
0.489157824522198));
#16599=CARTESIAN_POINT('Ctrl Pts',(0.161362514281243,0.0108046658515635,
0.497096814159504));
#16600=CARTESIAN_POINT('Ctrl Pts',(0.0784263257203939,0.141435191000425,
0.50503580379681));
#16601=CARTESIAN_POINT('Ctrl Pts',(-0.076303789130349,0.14259149197508,
0.512974793434115));
#16602=CARTESIAN_POINT('Ctrl Pts',(-0.161183014472451,0.0132150544797126,
0.520913783071421));
#16603=CARTESIAN_POINT('Ctrl Pts',(-0.0985102366584373,-0.128258859705,
0.528852772708727));
#16604=CARTESIAN_POINT('Ctrl Pts',(0.0543419114689404,-0.152320577983508,
0.536791762346032));
#16605=CARTESIAN_POINT('Ctrl Pts',(0.157447763940923,-0.0369432463290883,
0.544730751983338));
#16606=CARTESIAN_POINT('Ctrl Pts',(0.116420979124965,0.112253095453589,
0.552669741620643));
#16607=CARTESIAN_POINT('Ctrl Pts',(-0.0311812332291155,0.158689421555565,
0.56060873125795));
#16608=CARTESIAN_POINT('Ctrl Pts',(-0.150239163551416,0.0598564579197502,
0.568547720895255));
#16609=CARTESIAN_POINT('Ctrl Pts',(-0.131763436204723,-0.0937709907106254,
0.576486710532561));
#16610=CARTESIAN_POINT('Ctrl Pts',(0.00733268664935855,-0.161557523891122,
0.584425700169866));
#16611=CARTESIAN_POINT('Ctrl Pts',(0.139716237417787,-0.0814492162095161,
0.592364689807173));
#16612=CARTESIAN_POINT('Ctrl Pts',(0.144199148209332,0.0732202668325601,
0.600303679444478));
#16613=CARTESIAN_POINT('Ctrl Pts',(0.0166776214282734,0.160861613702037,
0.608242669081784));
#16614=CARTESIAN_POINT('Ctrl Pts',(-0.126111124778327,0.101245177793678,
0.616181658719089));
#16615=CARTESIAN_POINT('Ctrl Pts',(-0.153453779210204,-0.0510542795996006,
0.624120648356396));
#16616=CARTESIAN_POINT('Ctrl Pts',(-0.0403200156494649,-0.156617042997737,
0.6320596379937));
#16617=CARTESIAN_POINT('Ctrl Pts',(0.10972395892722,-0.118807637198397,
0.639998627631007));
#16618=CARTESIAN_POINT('Ctrl Pts',(0.159323168980049,0.0277620180369333,
0.647937617268312));
#16619=CARTESIAN_POINT('Ctrl Pts',(0.0630729369615192,0.148917448414806,
0.655876606905618));
#16620=CARTESIAN_POINT('Ctrl Pts',(-0.0909162461746061,0.133749160748195,
0.663815596542924));
#16621=CARTESIAN_POINT('Ctrl Pts',(-0.161677836835157,-0.00385731715476066,
0.671754586180229));
#16622=CARTESIAN_POINT('Ctrl Pts',(-0.0844344483789265,-0.137932685561743,
0.679693575817536));
#16623=CARTESIAN_POINT('Ctrl Pts',(0.0701028908975481,-0.145740133481257,
0.687632565454841));
#16624=CARTESIAN_POINT('Ctrl Pts',(0.1604658380222,-0.0201324774223393,
0.695571555092147));
#16625=CARTESIAN_POINT('Ctrl Pts',(0.10393330787963,0.123905081947942,0.703510544729453));
#16626=CARTESIAN_POINT('Ctrl Pts',(-0.0477430426119635,0.15451603056473,
0.711449534366758));
#16627=CARTESIAN_POINT('Ctrl Pts',(-0.155713909636705,0.0436781428746717,
0.719388524004064));
#16628=CARTESIAN_POINT('Ctrl Pts',(-0.121139364160222,-0.10714409115852,
0.72732751364137));
#16629=CARTESIAN_POINT('Ctrl Pts',(0.0243299669821161,-0.159883252800214,
0.735266503278675));
#16630=CARTESIAN_POINT('Ctrl Pts',(0.147526880793862,-0.0662602540182413,
0.743205492915981));
#16631=CARTESIAN_POINT('Ctrl Pts',(0.135673045916277,0.0880194662056535,
0.751144482553287));
#16632=CARTESIAN_POINT('Ctrl Pts',(-0.000380164216571841,0.161723397486253,
0.759083472190592));
#16633=CARTESIAN_POINT('Ctrl Pts',(-0.136085360063504,0.0873806419964673,
0.767022461827899));
#16634=CARTESIAN_POINT('Ctrl Pts',(-0.147213735311121,-0.0669531026545853,
0.774961451465203));
#16635=CARTESIAN_POINT('Ctrl Pts',(-0.023578025097595,-0.159995870421162,
0.78290044110251));
#16636=CARTESIAN_POINT('Ctrl Pts',(0.121641751185188,-0.106573384050283,
0.790839430739816));
#16637=CARTESIAN_POINT('Ctrl Pts',(0.155506840911589,0.0444097314676148,
0.798778420377121));
#16638=CARTESIAN_POINT('Ctrl Pts',(0.047016075363265,0.15473878142458,0.806717410014428));
#16639=CARTESIAN_POINT('Ctrl Pts',(-0.104514684958047,0.123415081928621,
0.814656399651731));
#16640=CARTESIAN_POINT('Ctrl Pts',(-0.16036941405942,-0.020886666885039,
0.82259538928904));
#16641=CARTESIAN_POINT('Ctrl Pts',(-0.0694169354231278,-0.146068103622213,
0.830534378926343));
#16642=CARTESIAN_POINT('Ctrl Pts',(0.085081990139753,-0.137534202194171,
0.838473368563651));
#16643=CARTESIAN_POINT('Ctrl Pts',(0.161694184779289,-0.00309716449182502,
0.846412358200955));
#16644=CARTESIAN_POINT('Ctrl Pts',(0.0902864348795877,0.134175115040242,
0.854351347838261));
#16645=CARTESIAN_POINT('Ctrl Pts',(-0.0637723584188847,0.148619272374149,
0.862290337475567));
#16646=CARTESIAN_POINT('Ctrl Pts',(-0.159451928190027,0.0270126713934565,
0.870229327112872));
#16647=CARTESIAN_POINT('Ctrl Pts',(-0.109164185657521,-0.119322178948671,
0.878168316750179));
#16648=CARTESIAN_POINT('Ctrl Pts',(0.0410558873341998,-0.156425752146281,
0.886107306387484));
#16649=CARTESIAN_POINT('Ctrl Pts',(0.153692109215179,-0.0503322698109037,
0.894046296024789));
#16650=CARTESIAN_POINT('Ctrl Pts',(0.125633738317809,0.101836956040625,
0.901985285662096));
#16651=CARTESIAN_POINT('Ctrl Pts',(-0.0174337097671096,0.160781427979367,
0.909924275299401));
#16652=CARTESIAN_POINT('Ctrl Pts',(-0.144541791370401,0.072541521673891,
0.917863264936708));
#16653=CARTESIAN_POINT('Ctrl Pts',(-0.13933176907,-0.082105176128868,0.925802254574012));
#16654=CARTESIAN_POINT('Ctrl Pts',(-0.00657306121577474,-0.161590212220858,
0.933741244211319));
#16655=CARTESIAN_POINT('Ctrl Pts',(0.132202833700187,-0.0931504835251481,
0.941680233848624));
#16656=CARTESIAN_POINT('Ctrl Pts',(0.149956094815541,0.0605621288182698,
0.949619223485929));
#16657=CARTESIAN_POINT('Ctrl Pts',(0.0304348282896272,0.158834262822317,
0.957558213123236));
#16658=CARTESIAN_POINT('Ctrl Pts',(-0.116947437700435,0.111704514835484,
0.965497202760542));
#16659=CARTESIAN_POINT('Ctrl Pts',(-0.157272339407096,-0.0376830608728604,
0.973436192397847));
#16660=CARTESIAN_POINT('Ctrl Pts',(-0.0536251929639052,-0.152574376940928,
0.981375182035153));
#16661=CARTESIAN_POINT('Ctrl Pts',(0.0991121424632477,-0.127794307524525,
0.989314171672459));
#16662=CARTESIAN_POINT('Ctrl Pts',(0.161119104064031,0.0139726921146952,
0.997253161309763));
#16663=CARTESIAN_POINT('Ctrl Pts',(0.0756325681075411,0.142948649734045,
1.00519215094707));
#16664=CARTESIAN_POINT('Ctrl Pts',(-0.0790904005129918,0.141064915432658,
1.01313114058437));
#16665=CARTESIAN_POINT('Ctrl Pts',(-0.161411527883023,0.0100459188627121,
1.02107013022168));
#16666=CARTESIAN_POINT('Ctrl Pts',(-0.095971463730607,-0.130169427934261,
1.02900911985899));
#16667=CARTESIAN_POINT('Ctrl Pts',(0.0573238981132153,-0.151223584550935,
1.03694810949629));
#16668=CARTESIAN_POINT('Ctrl Pts',(0.158143159897702,-0.0338429135403315,
1.0448870991336));
#16669=CARTESIAN_POINT('Ctrl Pts',(0.114193197054413,0.114518625410106,
1.0528260887709));
#16670=CARTESIAN_POINT('Ctrl Pts',(-0.0342928115212847,0.158046211271557,
1.06076507840821));
#16671=CARTESIAN_POINT('Ctrl Pts',(-0.151386101389109,0.0568933223281485,
1.06870406804552));
#16672=CARTESIAN_POINT('Ctrl Pts',(-0.129895790602315,-0.0963415040526547,
1.07664305768282));
#16673=CARTESIAN_POINT('Ctrl Pts',(0.0105052141409744,-0.161382286187737,
1.08458204732013));
#16674=CARTESIAN_POINT('Ctrl Pts',(0.141289415307547,-0.0786886455683398,
1.09252103695743));
#16675=CARTESIAN_POINT('Ctrl Pts',(0.14273283995608,0.076039057183793,1.10046002659474));
#16676=CARTESIAN_POINT('Ctrl Pts',(0.013514131745196,0.161158214381091,
1.10839901623204));
#16677=CARTESIAN_POINT('Ctrl Pts',(-0.128075837894479,0.0987480712062529,
1.11633800586935));
#16678=CARTESIAN_POINT('Ctrl Pts',(-0.152421155552179,-0.0540591635106084,
1.12427699550666));
#16679=CARTESIAN_POINT('Ctrl Pts',(-0.0372353514058616,-0.157378938949945,
1.13221598514396));
#16680=CARTESIAN_POINT('Ctrl Pts',(0.11203686504723,-0.116629081663695,
1.14015497478127));
#16681=CARTESIAN_POINT('Ctrl Pts',(0.158747009937404,0.0308867067726846,
1.14809396441857));
#16682=CARTESIAN_POINT('Ctrl Pts',(0.0601351468730053,0.150127831962932,
1.15603295405588));
#16683=CARTESIAN_POINT('Ctrl Pts',(-0.0935263218228598,0.13193721592339,
1.16397194369318));
#16684=CARTESIAN_POINT('Ctrl Pts',(-0.161570852667341,-0.00703287904607843,
1.17191093333049));
#16685=CARTESIAN_POINT('Ctrl Pts',(-0.0817083410685703,-0.13956485524354,
1.17984992296779));
#16686=CARTESIAN_POINT('Ctrl Pts',(0.0729525569401478,-0.144334771469742,
1.1877889126051));
#16687=CARTESIAN_POINT('Ctrl Pts',(0.160830388835411,-0.016976096323307,
1.19572790224241));
#16688=CARTESIAN_POINT('Ctrl Pts',(0.101479022178261,0.125923031559255,
1.20366689187971));
#16689=CARTESIAN_POINT('Ctrl Pts',(-0.0507694344715009,0.153548254118279,
1.21160588151702));
#16690=CARTESIAN_POINT('Ctrl Pts',(-0.15654195331917,0.0406105733811438,
1.21954487115432));
#16691=CARTESIAN_POINT('Ctrl Pts',(-0.119011042423884,-0.109503304062093,
1.22748386079163));
#16692=CARTESIAN_POINT('Ctrl Pts',(0.0274663214511058,-0.159374411387982,
1.23542285042894));
#16693=CARTESIAN_POINT('Ctrl Pts',(0.148800150427453,-0.0633491677300162,
1.24336184006624));
#16694=CARTESIAN_POINT('Ctrl Pts',(0.133917639627974,0.0906678973829495,
1.25130082970354));
#16695=CARTESIAN_POINT('Ctrl Pts',(-0.00355729227603857,0.161684716318317,
1.25923981934086));
#16696=CARTESIAN_POINT('Ctrl Pts',(-0.137775766897813,0.0846902584421788,
1.26717880897816));
#16697=CARTESIAN_POINT('Ctrl Pts',(-0.14586996931591,-0.0698323268364953,
1.27511779861547));
#16698=CARTESIAN_POINT('Ctrl Pts',(-0.0204302119447119,-0.160428202816007,
1.28305678825277));
#16699=CARTESIAN_POINT('Ctrl Pts',(0.123712004283314,-0.104163053984564,
1.29099577789008));
#16700=CARTESIAN_POINT('Ctrl Pts',(0.15460435913624,0.0474562320176185,
1.29893476752738));
#16701=CARTESIAN_POINT('Ctrl Pts',(0.043967018911749,0.155632589980133,
1.30687375716469));
#16702=CARTESIAN_POINT('Ctrl Pts',(-0.106919113837756,0.121337978043289,
1.31481274680199));
#16703=CARTESIAN_POINT('Ctrl Pts',(-0.159928125575155,-0.0240332370134145,
1.3227517364393));
#16704=CARTESIAN_POINT('Ctrl Pts',(-0.0665338988230771,-0.147403670583407,
1.33069072607661));
#16705=CARTESIAN_POINT('Ctrl Pts',(0.0877675522160205,-0.135836146169277,
1.33862971571391));
#16706=CARTESIAN_POINT('Ctrl Pts',(0.161723824721502,8.00609866524728E-5,
1.34656870535122));
#16707=CARTESIAN_POINT('Ctrl Pts',(0.0876330185603928,0.135922977069285,
1.35450769498852));
#16708=CARTESIAN_POINT('Ctrl Pts',(-0.0666798087068602,0.147337724435113,
1.36244668462583));
#16709=CARTESIAN_POINT('Ctrl Pts',(-0.159951843822013,0.0238748801740983,
1.37038567426313));
#16710=CARTESIAN_POINT('Ctrl Pts',(-0.106798922716859,-0.121443775659372,
1.37832466390044));
#16711=CARTESIAN_POINT('Ctrl Pts',(0.0441210824430389,-0.155588987406456,
1.38626365353774));
#16712=CARTESIAN_POINT('Ctrl Pts',(0.154651279966657,-0.0473031264624986,
1.39420264317505));
#16713=CARTESIAN_POINT('Ctrl Pts',(0.123608792556459,0.10428547082216,1.40214163281236));
#16714=CARTESIAN_POINT('Ctrl Pts',(-0.020589002599541,0.160407931346284,
1.41008062244966));
#16715=CARTESIAN_POINT('Ctrl Pts',(-0.145939110542184,0.0696878015005003,
1.41801961208697));
#16716=CARTESIAN_POINT('Ctrl Pts',(-0.137691710982408,-0.0848265016612731,
1.42595860172427));
#16717=CARTESIAN_POINT('Ctrl Pts',(-0.00339746822928561,-0.161688398335044,
1.43389759136158));
#16718=CARTESIAN_POINT('Ctrl Pts',(0.134007838137522,-0.0905348079547059,
1.44183658099889));
#16719=CARTESIAN_POINT('Ctrl Pts',(0.148736417039967,0.0634956003383226,
1.44977557063619));
#16720=CARTESIAN_POINT('Ctrl Pts',(0.0273102951854726,0.159403164432859,
1.4577145602735));
#16721=CARTESIAN_POINT('Ctrl Pts',(-0.119122786779006,0.109382310628272,
1.4656535499108));
#16722=CARTESIAN_POINT('Ctrl Pts',(-0.156495242883694,-0.0407596439572756,
1.47359253954811));
#16723=CARTESIAN_POINT('Ctrl Pts',(-0.0506295842364637,-0.153609649276743,
1.48153152918541));
#16724=CARTESIAN_POINT('Ctrl Pts',(0.10162683549218,-0.125801210382132,
1.48947051882272));
#16725=CARTESIAN_POINT('Ctrl Pts',(0.160769288057966,0.017094787472962,
1.49740950846002));
#16726=CARTESIAN_POINT('Ctrl Pts',(0.0728951834924312,0.144484958595688,
1.50534849809733));
#16727=CARTESIAN_POINT('Ctrl Pts',(-0.0820226078184241,0.139326700971572,
1.51328748773464));
#16728=CARTESIAN_POINT('Ctrl Pts',(-0.134767702434085,0.0512744806661359,
1.51858014749284));
#16729=CARTESIAN_POINT('Ctrl Pts',(-0.136701386950156,0.00581475974600206,
1.52122647737194));
#16730=CARTESIAN_POINT('Ctrl Pts',(0.0740036351041134,-0.103579689087085,
-0.0054992613140312));
#16731=CARTESIAN_POINT('Ctrl Pts',(0.108448814220036,-0.0789699563406641,
-0.00285293143492929));
#16732=CARTESIAN_POINT('Ctrl Pts',(0.150264871169078,0.00688399744800666,
0.00243972832327453));
#16733=CARTESIAN_POINT('Ctrl Pts',(0.0755551489391376,0.130236700260234,
0.0103787179605803));
#16734=CARTESIAN_POINT('Ctrl Pts',(-0.0683810376584167,0.133979098529349,
0.0183177075978859));
#16735=CARTESIAN_POINT('Ctrl Pts',(-0.14968704878538,0.0152677557027674,
0.0262566972351917));
#16736=CARTESIAN_POINT('Ctrl Pts',(-0.0939816891590436,-0.11752176362514,
0.0341956868724974));
#16737=CARTESIAN_POINT('Ctrl Pts',(0.0477663481097245,-0.142674779628989,
0.0421346765098031));
#16738=CARTESIAN_POINT('Ctrl Pts',(0.14578288888032,-0.0372469160898187,
0.0500736661471088));
#16739=CARTESIAN_POINT('Ctrl Pts',(0.110347650287512,0.102292747252513,
0.0580126557844146));
#16740=CARTESIAN_POINT('Ctrl Pts',(-0.0261045975097209,0.148182615303324,
0.0659516454217203));
#16741=CARTESIAN_POINT('Ctrl Pts',(-0.13865919166998,0.0584255608647477,
0.073890635059026));
#16742=CARTESIAN_POINT('Ctrl Pts',(-0.124281158904105,-0.0848182532198701,
0.0818296246963318));
#16743=CARTESIAN_POINT('Ctrl Pts',(0.00386794697500161,-0.15041563023346,
0.0897686143336374));
#16744=CARTESIAN_POINT('Ctrl Pts',(0.128476112576568,-0.0783184064825255,
0.0977076039709433));
#16745=CARTESIAN_POINT('Ctrl Pts',(0.135473254782295,0.0654742669580799,
0.105646593608249));
#16746=CARTESIAN_POINT('Ctrl Pts',(0.0184538891044151,0.149329569763132,
0.113585583245555));
#16747=CARTESIAN_POINT('Ctrl Pts',(-0.115458732720671,0.096483973363118,
0.12152457288286));
#16748=CARTESIAN_POINT('Ctrl Pts',(-0.143676805334049,-0.0446861343604874,
0.129463562520166));
#16749=CARTESIAN_POINT('Ctrl Pts',(-0.0403686054279526,-0.144949124289353,
0.137402552157472));
#16750=CARTESIAN_POINT('Ctrl Pts',(0.0998942839726139,-0.112521137758025,
0.145341541794778));
#16751=CARTESIAN_POINT('Ctrl Pts',(0.14871080372247,0.0229122455632766,
0.153280531432083));
#16752=CARTESIAN_POINT('Ctrl Pts',(0.0613927738894439,0.137371034794898,
0.161219521069389));
#16753=CARTESIAN_POINT('Ctrl Pts',(-0.0821261326059948,0.126076058196294,
0.169158510706695));
#16754=CARTESIAN_POINT('Ctrl Pts',(-0.150464193336327,-0.000632910110818063,
0.177097500344));
#16755=CARTESIAN_POINT('Ctrl Pts',(-0.0810625969653723,-0.126762492068094,
0.185036489981306));
#16756=CARTESIAN_POINT('Ctrl Pts',(0.0625462512992226,-0.136849700411639,
0.192975479618612));
#16757=CARTESIAN_POINT('Ctrl Pts',(0.148898293097928,-0.0216603868066741,
0.200914469255917));
#16758=CARTESIAN_POINT('Ctrl Pts',(0.0989441522193119,0.113357526360621,
0.208853458893223));
#16759=CARTESIAN_POINT('Ctrl Pts',(-0.0415865789238149,0.144604393083411,
0.216792448530529));
#16760=CARTESIAN_POINT('Ctrl Pts',(-0.144047647180085,0.0434758483035601,
0.224731438167835));
#16761=CARTESIAN_POINT('Ctrl Pts',(-0.114642966671137,-0.0974518559926297,
0.232670427805141));
#16762=CARTESIAN_POINT('Ctrl Pts',(0.0197094928286333,-0.149169064945282,
0.240609417442446));
#16763=CARTESIAN_POINT('Ctrl Pts',(0.136019262424063,-0.0643322181611298,
0.248548407079752));
#16764=CARTESIAN_POINT('Ctrl Pts',(0.127812719278849,0.0793963653730636,
0.256487396717058));
#16765=CARTESIAN_POINT('Ctrl Pts',(0.00260239121171357,0.150443017797356,
0.264426386354363));
#16766=CARTESIAN_POINT('Ctrl Pts',(-0.124990247656303,0.0837693979610897,
0.272365375991669));
#16767=CARTESIAN_POINT('Ctrl Pts',(-0.138162880936044,-0.0595893646165358,
0.280304365628975));
#16768=CARTESIAN_POINT('Ctrl Pts',(-0.0248568656394851,-0.148398147813718,
0.288243355266281));
#16769=CARTESIAN_POINT('Ctrl Pts',(0.111203906597776,-0.101358597076653,
0.296182344903586));
#16770=CARTESIAN_POINT('Ctrl Pts',(0.145465123646218,0.0384678027257296,
0.304121334540892));
#16771=CARTESIAN_POINT('Ctrl Pts',(0.0465629893725541,0.143079565503422,
0.312060324178198));
#16772=CARTESIAN_POINT('Ctrl Pts',(-0.0949643705016135,0.116711791945748,
0.319999313815503));
#16773=CARTESIAN_POINT('Ctrl Pts',(-0.149558357514911,-0.0164976283567656,
0.327938303452809));
#16774=CARTESIAN_POINT('Ctrl Pts',(-0.0672419181269484,-0.134604600554976,
0.335877293090115));
#16775=CARTESIAN_POINT('Ctrl Pts',(0.0766298889166206,-0.12949028600085,
0.343816282727421));
#16776=CARTESIAN_POINT('Ctrl Pts',(0.150352284446295,-0.00583648916182633,
0.351755272364726));
#16777=CARTESIAN_POINT('Ctrl Pts',(0.0864374678803939,0.123160213504125,
0.359694262002032));
#16778=CARTESIAN_POINT('Ctrl Pts',(-0.0566049265834532,0.139412181427728,
0.367633251639338));
#16779=CARTESIAN_POINT('Ctrl Pts',(-0.147829390149123,0.0280418517950267,
0.375572241276644));
#16780=CARTESIAN_POINT('Ctrl Pts',(-0.103726178443039,-0.108998871322406,
0.383511230913949));
#16781=CARTESIAN_POINT('Ctrl Pts',(0.0353312408083745,-0.146258597924691,
0.391450220551255));
#16782=CARTESIAN_POINT('Ctrl Pts',(0.142045330507792,-0.0496286018832686,
0.399389210188561));
#16783=CARTESIAN_POINT('Ctrl Pts',(0.118726655129599,0.0924329779120693,
0.407328199825866));
#16784=CARTESIAN_POINT('Ctrl Pts',(-0.0132781361506635,0.1498785012746,
0.415267189463172));
#16785=CARTESIAN_POINT('Ctrl Pts',(-0.133127703795094,0.0701205285647604,
0.423206179100478));
#16786=CARTESIAN_POINT('Ctrl Pts',(-0.131107982452518,-0.0738279823724454,
0.431145168737783));
#16787=CARTESIAN_POINT('Ctrl Pts',(-0.00906788859151817,-0.150192035209753,
0.439084158375089));
#16788=CARTESIAN_POINT('Ctrl Pts',(0.121273235812024,-0.0890655731449414,
0.447023148012395));
#16789=CARTESIAN_POINT('Ctrl Pts',(0.14059702422731,0.0535943170716914,
0.4549621376497));
#16790=CARTESIAN_POINT('Ctrl Pts',(0.031213872705855,0.14719228306762,0.462901127287006));
#16791=CARTESIAN_POINT('Ctrl Pts',(-0.106743440051405,0.106045801661112,
0.470840116924312));
#16792=CARTESIAN_POINT('Ctrl Pts',(-0.146984449047318,-0.0321783433727119,
0.478779106561618));
#16793=CARTESIAN_POINT('Ctrl Pts',(-0.0526712684425847,-0.140945420374714,
0.486718096198923));
#16794=CARTESIAN_POINT('Ctrl Pts',(0.0898588486235595,-0.120686624644175,
0.49465708583623));
#16795=CARTESIAN_POINT('Ctrl Pts',(0.150129348203927,0.0100525047535443,
0.502596075473534));
#16796=CARTESIAN_POINT('Ctrl Pts',(0.0729667185397875,0.131589254992538,
0.510535065110842));
#16797=CARTESIAN_POINT('Ctrl Pts',(-0.0709919412117167,0.132665060686482,
0.518474054748145));
#16798=CARTESIAN_POINT('Ctrl Pts',(-0.149962344179375,0.0122950954523496,
0.526413044385453));
#16799=CARTESIAN_POINT('Ctrl Pts',(-0.0916524986414713,-0.119330187030486,
0.534352034022757));
#16800=CARTESIAN_POINT('Ctrl Pts',(0.0505589280467443,-0.141716861518734,
0.542291023660064));
#16801=CARTESIAN_POINT('Ctrl Pts',(0.146487121137799,-0.0343714617774037,
0.550230013297369));
#16802=CARTESIAN_POINT('Ctrl Pts',(0.108316394245265,0.104438655591022,
0.558169002934674));
#16803=CARTESIAN_POINT('Ctrl Pts',(-0.0290105681715044,0.147642341414387,
0.566107992571982));
#16804=CARTESIAN_POINT('Ctrl Pts',(-0.139780343651344,0.0556895822633619,
0.574046982209285));
#16805=CARTESIAN_POINT('Ctrl Pts',(-0.122590794290966,-0.0872431727934394,
0.581985971846593));
#16806=CARTESIAN_POINT('Ctrl Pts',(0.00682222554696161,-0.150310782322966,
0.589924961483898));
#16807=CARTESIAN_POINT('Ctrl Pts',(0.129989965454297,-0.0757791721064987,
0.597863951121203));
#16808=CARTESIAN_POINT('Ctrl Pts',(0.134160800782372,0.0681230766876274,
0.60580294075851));
#16809=CARTESIAN_POINT('Ctrl Pts',(0.015516617634347,0.149663317553585,
0.613741930395814));
#16810=CARTESIAN_POINT('Ctrl Pts',(-0.117331965534667,0.0941970482962578,
0.621680920033121));
#16811=CARTESIAN_POINT('Ctrl Pts',(-0.142771175541451,-0.0475001629309618,
0.629619909670426));
#16812=CARTESIAN_POINT('Ctrl Pts',(-0.0375131590877193,-0.145714230393655,
0.637558899307733));
#16813=CARTESIAN_POINT('Ctrl Pts',(0.102085583566124,-0.110536906379362,
0.645497888945037));
#16814=CARTESIAN_POINT('Ctrl Pts',(0.148231970847143,0.0258293798362968,
0.653436878582344));
#16815=CARTESIAN_POINT('Ctrl Pts',(0.0586821478180281,0.138550639014834,
0.661375868219649));
#16816=CARTESIAN_POINT('Ctrl Pts',(-0.0845871597882484,0.124438283670714,
0.669314857856955));
#16817=CARTESIAN_POINT('Ctrl Pts',(-0.150422719745043,-0.00358879206139753,
0.67725384749426));
#16818=CARTESIAN_POINT('Ctrl Pts',(-0.078556588917505,-0.128330574617282,
0.685192837131567));
#16819=CARTESIAN_POINT('Ctrl Pts',(0.065222715229363,-0.135594511179713,
0.693131826768872));
#16820=CARTESIAN_POINT('Ctrl Pts',(0.149295093588351,-0.0187309656558678,
0.701070816406178));
#16821=CARTESIAN_POINT('Ctrl Pts',(0.0966980456281902,0.11527949520901,
0.709009806043483));
#16822=CARTESIAN_POINT('Ctrl Pts',(-0.044419435954706,0.14375947882982,
0.716948795680789));
#16823=CARTESIAN_POINT('Ctrl Pts',(-0.144873968183829,0.0406375120624596,
0.724887785318095));
#16824=CARTESIAN_POINT('Ctrl Pts',(-0.112706311402131,-0.099685311927494,
0.732826774955401));
#16825=CARTESIAN_POINT('Ctrl Pts',(0.0226362492002416,-0.148753064728429,
0.740765764592706));
#16826=CARTESIAN_POINT('Ctrl Pts',(0.137256875023267,-0.0616475814838108,
0.748704754230013));
#16827=CARTESIAN_POINT('Ctrl Pts',(0.126228238590478,0.0818920376245527,
0.756643743867318));
#16828=CARTESIAN_POINT('Ctrl Pts',(-0.000353699285724532,0.150465108715513,
0.764582733504624));
#16829=CARTESIAN_POINT('Ctrl Pts',(-0.126611849706441,0.0812976848247803,
0.772521723141928));
#16830=CARTESIAN_POINT('Ctrl Pts',(-0.136965528997667,-0.0622921978288208,
0.780460712779236));
#16831=CARTESIAN_POINT('Ctrl Pts',(-0.0219366533522686,-0.148857842533265,
0.788399702416541));
#16832=CARTESIAN_POINT('Ctrl Pts',(0.113173725020093,-0.0991543342927188,
0.796338692053846));
#16833=CARTESIAN_POINT('Ctrl Pts',(0.144681314438483,0.0413181715024817,
0.804277681691154));
#16834=CARTESIAN_POINT('Ctrl Pts',(0.0437430761464933,0.143966723006387,
0.812216671328456));
#16835=CARTESIAN_POINT('Ctrl Pts',(-0.0972389504488157,0.114823606281847,
0.820155660965765));
#16836=CARTESIAN_POINT('Ctrl Pts',(-0.149205382128735,-0.0194326526180533,
0.828094650603069));
#16837=CARTESIAN_POINT('Ctrl Pts',(-0.0645845121824554,-0.135899649852787,
0.836033640240376));
#16838=CARTESIAN_POINT('Ctrl Pts',(0.0791590524011713,-0.127959831458565,
0.843972629877681));
#16839=CARTESIAN_POINT('Ctrl Pts',(0.150437929635691,-0.00288155702400619,
0.851911619514986));
#16840=CARTESIAN_POINT('Ctrl Pts',(0.0840011924733913,0.12483458538003,
0.859850609152293));
#16841=CARTESIAN_POINT('Ctrl Pts',(-0.0593328794206009,0.138273220341526,
0.867789598789597));
#16842=CARTESIAN_POINT('Ctrl Pts',(-0.148351766552825,0.0251321985630355,
0.875728588426904));
#16843=CARTESIAN_POINT('Ctrl Pts',(-0.1015647786165,-0.111015628577859,
0.883667578064211));
#16844=CARTESIAN_POINT('Ctrl Pts',(0.0381978034543637,-0.145536256153639,
0.891606567701514));
#16845=CARTESIAN_POINT('Ctrl Pts',(0.142992914329196,-0.046828415471795,
0.899545557338823));
#16846=CARTESIAN_POINT('Ctrl Pts',(0.116887812080083,0.0947476302135675,
0.907484546976125));
#16847=CARTESIAN_POINT('Ctrl Pts',(-0.0162200712834111,0.149588713917584,
0.915423536613434));
#16848=CARTESIAN_POINT('Ctrl Pts',(-0.134479591021026,0.067491582014154,
0.923362526250738));
#16849=CARTESIAN_POINT('Ctrl Pts',(-0.129632261667175,-0.0763894677230377,
0.931301515888044));
#16850=CARTESIAN_POINT('Ctrl Pts',(-0.00611548103612966,-0.150341195071919,
0.93924050552535));
#16851=CARTESIAN_POINT('Ctrl Pts',(0.122999603362204,-0.0866658618874593,
0.947179495162656));
#16852=CARTESIAN_POINT('Ctrl Pts',(0.139516980595786,0.0563461282555487,
0.95511848479996));
#16853=CARTESIAN_POINT('Ctrl Pts',(0.0283161238170646,0.147777099632969,
0.963057474437267));
#16854=CARTESIAN_POINT('Ctrl Pts',(-0.108806203685475,0.103928264122473,
0.970996464074573));
#16855=CARTESIAN_POINT('Ctrl Pts',(-0.146323908690103,-0.0350597745230392,
0.978935453711877));
#16856=CARTESIAN_POINT('Ctrl Pts',(-0.049892103521326,-0.14195299239598,
0.986874443349185));
#16857=CARTESIAN_POINT('Ctrl Pts',(0.0922125030920605,-0.118897974404329,
0.994813432986488));
#16858=CARTESIAN_POINT('Ctrl Pts',(0.149902882860231,0.0129999905441286,
1.0027524226238));
#16859=CARTESIAN_POINT('Ctrl Pts',(0.0703674468853664,0.132997355096976,
1.0106914122611));
#16860=CARTESIAN_POINT('Ctrl Pts',(-0.0735845641169637,0.131244755962562,
1.01863040189841));
#16861=CARTESIAN_POINT('Ctrl Pts',(-0.150174949749745,0.00934657753497952,
1.02656939153571));
#16862=CARTESIAN_POINT('Ctrl Pts',(-0.0892904610481016,-0.121107752063083,
1.03450838117302));
#16863=CARTESIAN_POINT('Ctrl Pts',(0.0533333252681307,-0.140696234703703,
1.04244737081032));
#16864=CARTESIAN_POINT('Ctrl Pts',(0.147134107472884,-0.031486957015783,
1.05038636044763));
#16865=CARTESIAN_POINT('Ctrl Pts',(0.106243698045146,0.106546471877992,
1.05832535008494));
#16866=CARTESIAN_POINT('Ctrl Pts',(-0.0319055355867657,0.147043907874068,
1.06626433972224));
#16867=CARTESIAN_POINT('Ctrl Pts',(-0.14084743801815,0.0529327237885883,
1.07420332935955));
#16868=CARTESIAN_POINT('Ctrl Pts',(-0.120853163849259,-0.0896347412088629,
1.08214231899685));
#16869=CARTESIAN_POINT('Ctrl Pts',(0.00977389921538986,-0.150147743699608,
1.09008130863416));
#16870=CARTESIAN_POINT('Ctrl Pts',(0.13145362739741,-0.0732107771302755,
1.09802029827146));
#16871=CARTESIAN_POINT('Ctrl Pts',(0.132796568802552,0.0707456384395876,
1.10595928790877));
#16872=CARTESIAN_POINT('Ctrl Pts',(0.0125733526121963,0.149939270533256,
1.11389827754607));
#16873=CARTESIAN_POINT('Ctrl Pts',(-0.119159906186493,0.0918737764630459,
1.12183726718338));
#16874=CARTESIAN_POINT('Ctrl Pts',(-0.141810437433163,-0.0502958634379693,
1.12977625682069));
#16875=CARTESIAN_POINT('Ctrl Pts',(-0.0346432321137694,-0.146423087362162,
1.13771524645799));
#16876=CARTESIAN_POINT('Ctrl Pts',(0.104237477950025,-0.108510009835838,
1.1456542360953));
#16877=CARTESIAN_POINT('Ctrl Pts',(0.147695920811486,0.0287365450185451,
1.1535932257326));
#16878=CARTESIAN_POINT('Ctrl Pts',(0.0559488704325515,0.139676762352502,
1.16153221536991));
#16879=CARTESIAN_POINT('Ctrl Pts',(-0.0870155364008756,0.12275247642644,
1.16947120500722));
#16880=CARTESIAN_POINT('Ctrl Pts',(-0.150323183223479,-0.00654328889139735,
1.17741019464452));
#16881=CARTESIAN_POINT('Ctrl Pts',(-0.0760202581255566,-0.129849121670035,
1.18534918428183));
#16882=CARTESIAN_POINT('Ctrl Pts',(0.0678740032777675,-0.134286982701248,
1.19328817391913));
#16883=CARTESIAN_POINT('Ctrl Pts',(0.149634266389533,-0.0157943143574443,
1.20122716355644));
#16884=CARTESIAN_POINT('Ctrl Pts',(0.0944146137277022,0.117156966325547,
1.20916615319374));
#16885=CARTESIAN_POINT('Ctrl Pts',(-0.047235147145783,0.142859073628774,
1.21710514283105));
#16886=CARTESIAN_POINT('Ctrl Pts',(-0.145644368043342,0.037783489796601,
1.22504413246835));
#16887=CARTESIAN_POINT('Ctrl Pts',(-0.11072615165767,-0.101880289472715,
1.23298312210566));
#16888=CARTESIAN_POINT('Ctrl Pts',(0.0255542680118797,-0.148279646041953,
1.24092211174296));
#16889=CARTESIAN_POINT('Ctrl Pts',(0.138441506664824,-0.0589391489276913,
1.24886110138027));
#16890=CARTESIAN_POINT('Ctrl Pts',(0.124595033982396,0.0843560996663564,
1.25680009101758));
#16891=CARTESIAN_POINT('Ctrl Pts',(-0.00330965325590636,0.150429120316621,
1.26473908065488));
#16892=CARTESIAN_POINT('Ctrl Pts',(-0.128184579763139,0.0787945908985174,
1.27267807029219));
#16893=CARTESIAN_POINT('Ctrl Pts',(-0.135715308561414,-0.0649709863423027,
1.2806170599295));
#16894=CARTESIAN_POINT('Ctrl Pts',(-0.0190079735469551,-0.149260078337129,
1.2885560495668));
#16895=CARTESIAN_POINT('Ctrl Pts',(0.115099858543875,-0.0969117980795561,
1.29649503920411));
#16896=CARTESIAN_POINT('Ctrl Pts',(0.143841658454547,0.0441525915281748,
1.30443402884141));
#16897=CARTESIAN_POINT('Ctrl Pts',(0.0409062781470196,0.144798309552134,
1.31237301847872));
#16898=CARTESIAN_POINT('Ctrl Pts',(-0.0994759962839106,0.112891098884786,
1.32031200811602));
#16899=CARTESIAN_POINT('Ctrl Pts',(-0.148794813708878,-0.0223601759313527,
1.32825099775333));
#16900=CARTESIAN_POINT('Ctrl Pts',(-0.0619021766503053,-0.13714224202644,
1.33618998739064));
#16901=CARTESIAN_POINT('Ctrl Pts',(0.0816576604940555,-0.126379984705639,
1.34412897702794));
#16902=CARTESIAN_POINT('Ctrl Pts',(0.150465506209006,7.4487583413377E-5,
1.35206796666525));
#16903=CARTESIAN_POINT('Ctrl Pts',(0.0815324923277053,0.126460770918471,
1.36000695630255));
#16904=CARTESIAN_POINT('Ctrl Pts',(-0.062037929094705,0.137080886684378,
1.36794594593986));
#16905=CARTESIAN_POINT('Ctrl Pts',(-0.148816880822527,0.0222128430196456,
1.37588493557716));
#16906=CARTESIAN_POINT('Ctrl Pts',(-0.0993641722043223,-0.112989531455785,
1.38382392521447));
#16907=CARTESIAN_POINT('Ctrl Pts',(0.0410496166270677,-0.144757742348562,
1.39176291485178));
#16908=CARTESIAN_POINT('Ctrl Pts',(0.143885312916173,-0.0440101443352923,
1.39970190448908));
#16909=CARTESIAN_POINT('Ctrl Pts',(0.115003831846793,0.0970256929337524,
1.40764089412639));
#16910=CARTESIAN_POINT('Ctrl Pts',(-0.0191557100743377,0.149241218055048,
1.41557988376369));
#16911=CARTESIAN_POINT('Ctrl Pts',(-0.135779636557791,0.0648365220611291,
1.423518873401));
#16912=CARTESIAN_POINT('Ctrl Pts',(-0.128106375355825,-0.0789213496179777,
1.4314578630383));
#16913=CARTESIAN_POINT('Ctrl Pts',(-0.00316095527563228,-0.150432546011701,
1.43939685267561));
#16914=CARTESIAN_POINT('Ctrl Pts',(0.12467895337041,-0.0842322751882648,
1.44733584231291));
#16915=CARTESIAN_POINT('Ctrl Pts',(0.138382210043398,0.0590753877074232,
1.45527483195022));
#16916=CARTESIAN_POINT('Ctrl Pts',(0.0254091034322018,0.148306397458819,
1.46321382158753));
#16917=CARTESIAN_POINT('Ctrl Pts',(-0.110830116988615,0.101767718932792,
1.47115281122483));
#16918=CARTESIAN_POINT('Ctrl Pts',(-0.145600909330124,-0.0379221829034233,
1.47909180086214));
#16919=CARTESIAN_POINT('Ctrl Pts',(-0.0471050325108872,-0.142916194795756,
1.48703079049945));
#16920=CARTESIAN_POINT('Ctrl Pts',(0.0945521370959566,-0.117043625665234,
1.49496978013675));
#16921=CARTESIAN_POINT('Ctrl Pts',(0.14957741911039,0.0159047428854941,
1.50290876977406));
#16922=CARTESIAN_POINT('Ctrl Pts',(0.0678206238522695,0.134426714629862,
1.51084775941136));
#16923=CARTESIAN_POINT('Ctrl Pts',(-0.0763126473618499,0.129627546381738,
1.51878674904867));
#16924=CARTESIAN_POINT('Ctrl Pts',(-0.125385920115907,0.0477050348167321,
1.52407940880687));
#16925=CARTESIAN_POINT('Ctrl Pts',(-0.127184992207234,0.00540996832206346,
1.52672573868597));
#16926=CARTESIAN_POINT('Ctrl Pts',(0.0684664424539414,-0.095829519891843,
-1.38777878078145E-17));
#16927=CARTESIAN_POINT('Ctrl Pts',(0.100334321247169,-0.0730611673843044,
0.00264632987910189));
#16928=CARTESIAN_POINT('Ctrl Pts',(0.139021564822767,0.00636891437108143,
0.00793898963730573));
#16929=CARTESIAN_POINT('Ctrl Pts',(0.0699018669780613,0.120491966796142,
0.0158779792746114));
#16930=CARTESIAN_POINT('Ctrl Pts',(-0.0632645460347191,0.123954346655885,
0.0238169689119172));
#16931=CARTESIAN_POINT('Ctrl Pts',(-0.138486976988987,0.0141253725679007,
0.0317559585492228));
#16932=CARTESIAN_POINT('Ctrl Pts',(-0.0869496735326521,-0.108728403071097,
0.0396949481865287));
#16933=CARTESIAN_POINT('Ctrl Pts',(0.0441923146003338,-0.131999388615902,
0.0476339378238343));
#16934=CARTESIAN_POINT('Ctrl Pts',(0.134874939024977,-0.034459980695041,
0.0555729274611401));
#16935=CARTESIAN_POINT('Ctrl Pts',(0.102091080224759,0.094638871230671,
0.0635119170984456));
#16936=CARTESIAN_POINT('Ctrl Pts',(-0.0241513666277066,0.137095110112719,
0.0714509067357516));
#16937=CARTESIAN_POINT('Ctrl Pts',(-0.128284260007319,0.0540539703915629,
0.0793898963730571));
#16938=CARTESIAN_POINT('Ctrl Pts',(-0.114982038412656,-0.0784718756714057,
0.0873288860103631));
#16939=CARTESIAN_POINT('Ctrl Pts',(0.00357853460314598,-0.139161043603659,
0.0952678756476685));
#16940=CARTESIAN_POINT('Ctrl Pts',(0.118863112008681,-0.0724583686054966,
0.103206865284975));
#16941=CARTESIAN_POINT('Ctrl Pts',(0.125336705278751,0.0605752693714656,
0.11114585492228));
#16942=CARTESIAN_POINT('Ctrl Pts',(0.0170731091066207,0.138156245709763,
0.119084844559586));
#16943=CARTESIAN_POINT('Ctrl Pts',(-0.106819734848208,0.0892647286947484,
0.127023834196891));
#16944=CARTESIAN_POINT('Ctrl Pts',(-0.132926439498961,-0.0413425724611633,
0.134962823834197));
#16945=CARTESIAN_POINT('Ctrl Pts',(-0.0373480950846616,-0.134103559412242,
0.142901813471503));
#16946=CARTESIAN_POINT('Ctrl Pts',(0.0924198687735613,-0.104101940294199,
0.150840803108809));
#16947=CARTESIAN_POINT('Ctrl Pts',(0.137583777756591,0.0211978768359354,
0.158779792746114));
#16948=CARTESIAN_POINT('Ctrl Pts',(0.0567991668878991,0.127092487218924,
0.16671878238342));
#16949=CARTESIAN_POINT('Ctrl Pts',(-0.075981188277068,0.116642637502503,
0.174657772020726));
#16950=CARTESIAN_POINT('Ctrl Pts',(-0.139205973057234,-0.000585553717998882,
0.182596761658032));
#16951=CARTESIAN_POINT('Ctrl Pts',(-0.0749972298318695,-0.11727771015962,
0.190535751295337));
#16952=CARTESIAN_POINT('Ctrl Pts',(0.0578663373665801,-0.126610160769685,
0.198474740932643));
#16953=CARTESIAN_POINT('Ctrl Pts',(0.13775723856723,-0.0200396862227523,
0.206413730569949));
#16954=CARTESIAN_POINT('Ctrl Pts',(0.091540828968026,0.104875747581476,
0.214352720207254));
#16955=CARTESIAN_POINT('Ctrl Pts',(-0.0384749358425138,0.133784622116252,
0.22229170984456));
#16956=CARTESIAN_POINT('Ctrl Pts',(-0.133269533752038,0.0402228439430644,
0.230230699481866));
#16957=CARTESIAN_POINT('Ctrl Pts',(-0.106065007067505,-0.0901601911982067,
0.238169689119172));
#16958=CARTESIAN_POINT('Ctrl Pts',(0.0182347644767634,-0.138007750384372,
0.246108678756477));
#16959=CARTESIAN_POINT('Ctrl Pts',(0.125841858853055,-0.0595186723796334,
0.254047668393783));
#16960=CARTESIAN_POINT('Ctrl Pts',(0.118249355954961,0.073455671106145,
0.261986658031089));
#16961=CARTESIAN_POINT('Ctrl Pts',(0.00240767183786234,0.139186381940956,
0.269925647668394));
#16962=CARTESIAN_POINT('Ctrl Pts',(-0.115638070838342,0.0775014991741366,
0.277864637305701));
#16963=CARTESIAN_POINT('Ctrl Pts',(-0.12782508485658,-0.0551306945617612,
0.285803626943006));
#16964=CARTESIAN_POINT('Ctrl Pts',(-0.0229969941138309,-0.137294515779738,
0.293742616580312));
#16965=CARTESIAN_POINT('Ctrl Pts',(0.102883268653204,-0.0937746172089793,
0.301681606217617));
#16966=CARTESIAN_POINT('Ctrl Pts',(0.134580950019115,0.0355895166223291,
0.309620595854923));
#16967=CARTESIAN_POINT('Ctrl Pts',(0.0430789950773988,0.13237388709478,
0.317559585492229));
#16968=CARTESIAN_POINT('Ctrl Pts',(-0.0878588274613298,0.107979036106918,
0.325498575129534));
#16969=CARTESIAN_POINT('Ctrl Pts',(-0.1383679148179,-0.0152632221501787,
0.33343756476684));
#16970=CARTESIAN_POINT('Ctrl Pts',(-0.0622106591311991,-0.12453304658572,
0.341376554404146));
#16971=CARTESIAN_POINT('Ctrl Pts',(0.0708961914151981,-0.119801401679107,
0.349315544041452));
#16972=CARTESIAN_POINT('Ctrl Pts',(0.1391024375543,-0.00539978406154301,
0.357254533678757));
#16973=CARTESIAN_POINT('Ctrl Pts',(0.0799699354250877,0.113944965792994,
0.365193523316063));
#16974=CARTESIAN_POINT('Ctrl Pts',(-0.0523695618881846,0.128980908622551,
0.373132512953369));
#16975=CARTESIAN_POINT('Ctrl Pts',(-0.136768314413298,0.0259436692471295,
0.381071502590675));
#16976=CARTESIAN_POINT('Ctrl Pts',(-0.0959650484377783,-0.100843221288265,
0.38901049222798));
#16977=CARTESIAN_POINT('Ctrl Pts',(0.0326876424682324,-0.135315053971568,
0.396949481865287));
#16978=CARTESIAN_POINT('Ctrl Pts',(0.13141703692502,-0.0459152284901983,
0.404888471502591));
#16979=CARTESIAN_POINT('Ctrl Pts',(0.109843140674695,0.0855168418978295,
0.412827461139898));
#16980=CARTESIAN_POINT('Ctrl Pts',(-0.0122846228212416,0.13866410438033,
0.420766450777203));
#16981=CARTESIAN_POINT('Ctrl Pts',(-0.123166656044517,0.0648738825743514,
0.428705440414509));
#16982=CARTESIAN_POINT('Ctrl Pts',(-0.121298056821252,-0.0683039326309071,
0.436644430051815));
#16983=CARTESIAN_POINT('Ctrl Pts',(-0.00838939967687663,-0.138954178686792,
0.44458341968912));
#16984=CARTESIAN_POINT('Ctrl Pts',(0.11219917790857,-0.0824013973067221,
0.452522409326426));
#16985=CARTESIAN_POINT('Ctrl Pts',(0.13007709763057,0.0495842159710775,
0.460461398963732));
#16986=CARTESIAN_POINT('Ctrl Pts',(0.0288783492374893,0.136178877755608,
0.468400388601037));
#16987=CARTESIAN_POINT('Ctrl Pts',(-0.0987565487199846,0.0981111099028881,
0.476339378238344));
#16988=CARTESIAN_POINT('Ctrl Pts',(-0.135986594552616,-0.0297706550724338,
0.484278367875649));
#16989=CARTESIAN_POINT('Ctrl Pts',(-0.0487302328423073,-0.130399425645183,
0.492217357512954));
#16990=CARTESIAN_POINT('Ctrl Pts',(0.0831353173341669,-0.111656458896056,
0.50015634715026));
#16991=CARTESIAN_POINT('Ctrl Pts',(0.13889618212661,0.00930034365552528,
0.508095336787567));
#16992=CARTESIAN_POINT('Ctrl Pts',(0.0675071113591811,0.12174331898465,
0.516034326424871));
#16993=CARTESIAN_POINT('Ctrl Pts',(-0.0656800932930844,0.122738629397884,
0.523973316062178));
#16994=CARTESIAN_POINT('Ctrl Pts',(-0.138741673886299,0.0113751364249866,
0.531912305699483));
#16995=CARTESIAN_POINT('Ctrl Pts',(-0.0847947606245053,-0.110401514355972,
0.539851295336789));
#16996=CARTESIAN_POINT('Ctrl Pts',(0.0467759446245483,-0.131113145053959,
0.547790284974095));
#16997=CARTESIAN_POINT('Ctrl Pts',(0.135526478334676,-0.031799677225719,
0.555729274611401));
#16998=CARTESIAN_POINT('Ctrl Pts',(0.100211809365564,0.0966242157284558,
0.563668264248707));
#16999=CARTESIAN_POINT('Ctrl Pts',(-0.0268399031138932,0.136595261273209,
0.571607253886012));
#17000=CARTESIAN_POINT('Ctrl Pts',(-0.129321523751272,0.0515227066069736,
0.579546243523318));
#17001=CARTESIAN_POINT('Ctrl Pts',(-0.113418152377209,-0.0807153548762533,
0.587485233160623));
#17002=CARTESIAN_POINT('Ctrl Pts',(0.00631176444456456,-0.139064040754811,
0.595424222797929));
#17003=CARTESIAN_POINT('Ctrl Pts',(0.120263693490807,-0.0701091280034811,
0.603363212435234));
#17004=CARTESIAN_POINT('Ctrl Pts',(0.124122453355413,0.0630258865426945,
0.611302202072541));
#17005=CARTESIAN_POINT('Ctrl Pts',(0.0143556138404206,0.138465021405133,
0.619241191709845));
#17006=CARTESIAN_POINT('Ctrl Pts',(-0.108552806291007,0.0871489187988374,
0.627180181347153));
#17007=CARTESIAN_POINT('Ctrl Pts',(-0.132088571872698,-0.043946046262323,
0.635119170984457));
#17008=CARTESIAN_POINT('Ctrl Pts',(-0.0347063025259737,-0.134811417789573,
0.643058160621763));
#17009=CARTESIAN_POINT('Ctrl Pts',(0.0944472082050275,-0.102266175560326,
0.65099715025907));
#17010=CARTESIAN_POINT('Ctrl Pts',(0.137140772714236,0.0238967416356601,
0.658936139896373));
#17011=CARTESIAN_POINT('Ctrl Pts',(0.054291358674537,0.128183829614862,
0.666875129533682));
#17012=CARTESIAN_POINT('Ctrl Pts',(-0.0782580734018908,0.115127406593233,
0.674814119170985));
#17013=CARTESIAN_POINT('Ctrl Pts',(-0.139167602654929,-0.00332026696803425,
0.682753108808293));
#17014=CARTESIAN_POINT('Ctrl Pts',(-0.0726787294560835,-0.118728463672822,
0.690692098445597));
#17015=CARTESIAN_POINT('Ctrl Pts',(0.0603425395611779,-0.125448888878168,
0.698631088082904));
#17016=CARTESIAN_POINT('Ctrl Pts',(0.138124349154501,-0.0173294538893964,
0.706570077720209));
#17017=CARTESIAN_POINT('Ctrl Pts',(0.0894627833767505,0.106653908470079,
0.714509067357515));
#17018=CARTESIAN_POINT('Ctrl Pts',(-0.0410958292974484,0.133002927094911,
0.72244805699482));
#17019=CARTESIAN_POINT('Ctrl Pts',(-0.134034026730954,0.0375968812502473,
0.730387046632127));
#17020=CARTESIAN_POINT('Ctrl Pts',(-0.104273258644039,-0.0922265326964679,
0.738326036269432));
#17021=CARTESIAN_POINT('Ctrl Pts',(0.0209425314183671,-0.137622876656644,
0.746265025906738));
#17022=CARTESIAN_POINT('Ctrl Pts',(0.126986869252672,-0.0570349089493802,
0.754204015544043));
#17023=CARTESIAN_POINT('Ctrl Pts',(0.11678343126468,0.0757646090434518,
0.762143005181349));
#17024=CARTESIAN_POINT('Ctrl Pts',(-0.000327234354877375,0.139206819944772,
0.770081994818654));
#17025=CARTESIAN_POINT('Ctrl Pts',(-0.117138339349379,0.0752147276530931,
0.778020984455961));
#17026=CARTESIAN_POINT('Ctrl Pts',(-0.126717322684213,-0.0576312930030564,
0.785959974093266));
#17027=CARTESIAN_POINT('Ctrl Pts',(-0.0202952816069424,-0.137719814645367,
0.793898963730571));
#17028=CARTESIAN_POINT('Ctrl Pts',(0.104705698854998,-0.0917352845351548,
0.801837953367879));
#17029=CARTESIAN_POINT('Ctrl Pts',(0.133855787965376,0.0382266115373486,
0.809776943005182));
#17030=CARTESIAN_POINT('Ctrl Pts',(0.0404700769297216,0.133194664588195,
0.81771593264249));
#17031=CARTESIAN_POINT('Ctrl Pts',(-0.0899632159395838,0.106232130635072,
0.825654922279794));
#17032=CARTESIAN_POINT('Ctrl Pts',(-0.13804135019805,-0.0179786383510676,
0.833593911917101));
#17033=CARTESIAN_POINT('Ctrl Pts',(-0.059752088941783,-0.125731196083361,
0.841532901554406));
#17034=CARTESIAN_POINT('Ctrl Pts',(0.0732361146625898,-0.118385460722959,
0.849471891191712));
#17035=CARTESIAN_POINT('Ctrl Pts',(0.139181674492094,-0.00266594955618734,
0.857410880829018));
#17036=CARTESIAN_POINT('Ctrl Pts',(0.077715950067195,0.115494055719818,
0.865349870466323));
#17037=CARTESIAN_POINT('Ctrl Pts',(-0.0548934004223171,0.127927168308903,
0.87328886010363));
#17038=CARTESIAN_POINT('Ctrl Pts',(-0.137251604915624,0.0232517257326144,
0.881227849740934));
#17039=CARTESIAN_POINT('Ctrl Pts',(-0.0939653715754795,-0.102709078207047,
0.889166839378241));
#17040=CARTESIAN_POINT('Ctrl Pts',(0.0353397195745277,-0.134646760160997,
0.897105829015547));
#17041=CARTESIAN_POINT('Ctrl Pts',(0.132293719443212,-0.0433245611326863,
0.905044818652852));
#17042=CARTESIAN_POINT('Ctrl Pts',(0.108141885842356,0.0876583043865096,
0.912983808290157));
#17043=CARTESIAN_POINT('Ctrl Pts',(-0.0150064327997127,0.138395999855801,
0.920922797927463));
#17044=CARTESIAN_POINT('Ctrl Pts',(-0.124417390671652,0.0624416423544169,
0.928861787564769));
#17045=CARTESIAN_POINT('Ctrl Pts',(-0.119932754264349,-0.0706737593172073,
0.936800777202075));
#17046=CARTESIAN_POINT('Ctrl Pts',(-0.00565790085648466,-0.139092177922979,
0.944739766839381));
#17047=CARTESIAN_POINT('Ctrl Pts',(0.113796373024222,-0.0801812402497705,
0.952678756476687));
#17048=CARTESIAN_POINT('Ctrl Pts',(0.129077866376032,0.0521301276928276,
0.960617746113992));
#17049=CARTESIAN_POINT('Ctrl Pts',(0.026197419344502,0.13671993644362,0.968556735751298));
#17050=CARTESIAN_POINT('Ctrl Pts',(-0.100664969670515,0.0961520134094621,
0.976495725388603));
#17051=CARTESIAN_POINT('Ctrl Pts',(-0.13537547797311,-0.0324364881732178,
0.98443471502591));
#17052=CARTESIAN_POINT('Ctrl Pts',(-0.0461590140787468,-0.131331607851033,
0.992373704663214));
#17053=CARTESIAN_POINT('Ctrl Pts',(0.0853128637208732,-0.110001641284132,
1.00031269430052));
#17054=CARTESIAN_POINT('Ctrl Pts',(0.138686661656432,0.0120272889735618,
1.00825168393783));
#17055=CARTESIAN_POINT('Ctrl Pts',(0.0651023256631918,0.123046060459907,
1.01619067357513));
#17056=CARTESIAN_POINT('Ctrl Pts',(-0.0680787277209358,0.121424596492465,
1.02412966321244));
#17057=CARTESIAN_POINT('Ctrl Pts',(-0.138938371616466,0.00864723620724691,
1.03206865284975));
#17058=CARTESIAN_POINT('Ctrl Pts',(-0.0826094583655966,-0.112046076191904,
1.04000764248705));
#17059=CARTESIAN_POINT('Ctrl Pts',(0.0493427524230464,-0.130168884856471,
1.04794663212436));
#17060=CARTESIAN_POINT('Ctrl Pts',(0.136125055048066,-0.0291310004912345,
1.05588562176166));
#17061=CARTESIAN_POINT('Ctrl Pts',(0.0982941990358779,0.0985743183458784,
1.06382461139897));
#17062=CARTESIAN_POINT('Ctrl Pts',(-0.0295182596522469,0.136041604476578,
1.07176360103627));
#17063=CARTESIAN_POINT('Ctrl Pts',(-0.130308774647192,0.0489721252490281,
1.07970259067358));
#17064=CARTESIAN_POINT('Ctrl Pts',(-0.111810537096203,-0.0829279783650712,
1.08764158031088));
#17065=CARTESIAN_POINT('Ctrl Pts',(0.00904258428980543,-0.13891320121148,
1.09558056994819));
#17066=CARTESIAN_POINT('Ctrl Pts',(0.121617839487272,-0.067732908692211,
1.1035195595855));
#17067=CARTESIAN_POINT('Ctrl Pts',(0.122860297649024,0.0654522196953821,
1.1114585492228));
#17068=CARTESIAN_POINT('Ctrl Pts',(0.0116325734791967,0.138720326685422,
1.11939753886011));
#17069=CARTESIAN_POINT('Ctrl Pts',(-0.110243974478508,0.0849994817198388,
1.12733652849741));
#17070=CARTESIAN_POINT('Ctrl Pts',(-0.131199719314147,-0.0465325633653302,
1.13527551813472));
#17071=CARTESIAN_POINT('Ctrl Pts',(-0.0320511128216771,-0.13546723577438,
1.14321450777202));
#17072=CARTESIAN_POINT('Ctrl Pts',(0.0964380908528195,-0.100390938007982,
1.15115349740933));
#17073=CARTESIAN_POINT('Ctrl Pts',(0.136644831685568,0.0265863832644056,
1.15909248704664));
#17074=CARTESIAN_POINT('Ctrl Pts',(0.0517625939920979,0.129225692742072,
1.16703147668394));
#17075=CARTESIAN_POINT('Ctrl Pts',(-0.0805047509788913,0.113567736929491,
1.17497046632125));
#17076=CARTESIAN_POINT('Ctrl Pts',(-0.139075513779617,-0.00605369873671642,
1.18290945595855));
#17077=CARTESIAN_POINT('Ctrl Pts',(-0.0703321751825429,-0.12013338809653,
1.19084844559586));
#17078=CARTESIAN_POINT('Ctrl Pts',(0.0627954496153871,-0.124239193932754,
1.19878743523316));
#17079=CARTESIAN_POINT('Ctrl Pts',(0.138438143943654,-0.0146125323915816,
1.20672642487047));
#17080=CARTESIAN_POINT('Ctrl Pts',(0.0873502052771435,0.108390901091839,
1.21466541450777));
#17081=CARTESIAN_POINT('Ctrl Pts',(-0.043700859820065,0.132169893139269,
1.22260440414508));
#17082=CARTESIAN_POINT('Ctrl Pts',(-0.134746782767514,0.0349564062120582,
1.23054339378239));
#17083=CARTESIAN_POINT('Ctrl Pts',(-0.102441260891455,-0.0942572748833364,
1.23848238341969));
#17084=CARTESIAN_POINT('Ctrl Pts',(0.0236422145726536,-0.137184880695923,
1.246421373057));
#17085=CARTESIAN_POINT('Ctrl Pts',(0.128082862902196,-0.0545291301253663,
1.2543603626943));
#17086=CARTESIAN_POINT('Ctrl Pts',(0.115272428336817,0.0780443019497631,
1.26229935233161));
#17087=CARTESIAN_POINT('Ctrl Pts',(-0.00306201423577413,0.139173524314926,
1.27023834196891));
#17088=CARTESIAN_POINT('Ctrl Pts',(-0.118593392628464,0.0728989233548558,
1.27817733160622));
#17089=CARTESIAN_POINT('Ctrl Pts',(-0.125560647806918,-0.06010964584811,
1.28611632124353));
#17090=CARTESIAN_POINT('Ctrl Pts',(-0.0175857351491984,-0.138091953858251,
1.29405531088083));
#17091=CARTESIAN_POINT('Ctrl Pts',(0.106487712804436,-0.089660542174548,
1.30199430051814));
#17092=CARTESIAN_POINT('Ctrl Pts',(0.133078957772855,0.0408489510387311,
1.30993329015544));
#17093=CARTESIAN_POINT('Ctrl Pts',(0.0378455373822902,0.133964029124136,
1.31787227979275));
#17094=CARTESIAN_POINT('Ctrl Pts',(-0.0920328787300654,0.104444219726284,
1.32581126943006));
#17095=CARTESIAN_POINT('Ctrl Pts',(-0.137661501842601,-0.0206871148492911,
1.33375025906736));
#17096=CARTESIAN_POINT('Ctrl Pts',(-0.0572704544775333,-0.126880813469472,
1.34168924870467));
#17097=CARTESIAN_POINT('Ctrl Pts',(0.0755477687720905,-0.116923823242002,
1.34962823834197));
#17098=CARTESIAN_POINT('Ctrl Pts',(0.13920718769651,6.89141801743488E-5,
1.35756722797928));
#17099=CARTESIAN_POINT('Ctrl Pts',(0.0754319660950179,0.116998564767658,
1.36550621761658));
#17100=CARTESIAN_POINT('Ctrl Pts',(-0.0573960494825499,0.126824048933643,
1.37344520725389));
#17101=CARTESIAN_POINT('Ctrl Pts',(-0.13768191782304,0.0205508058651932,
1.38138419689119));
#17102=CARTESIAN_POINT('Ctrl Pts',(-0.0919294216917856,-0.104535287252199,
1.3893231865285));
#17103=CARTESIAN_POINT('Ctrl Pts',(0.0379781508110965,-0.133926497290667,
1.39726217616581));
#17104=CARTESIAN_POINT('Ctrl Pts',(0.133119345865688,-0.0407171622080862,
1.40520116580311));
#17105=CARTESIAN_POINT('Ctrl Pts',(0.106398871137127,0.0897659150453452,
1.41314015544042));
#17106=CARTESIAN_POINT('Ctrl Pts',(-0.0177224175491345,0.138074504763813,
1.42107914507772));
#17107=CARTESIAN_POINT('Ctrl Pts',(-0.125620162573399,0.0599852426217579,
1.42901813471503));
#17108=CARTESIAN_POINT('Ctrl Pts',(-0.118521039729242,-0.0730161975746823,
1.43695712435233));
#17109=CARTESIAN_POINT('Ctrl Pts',(-0.00292444232197888,-0.139176693688359,
1.44489611398964));
#17110=CARTESIAN_POINT('Ctrl Pts',(0.115350068603298,-0.0779297424218237,
1.45283510362695));
#17111=CARTESIAN_POINT('Ctrl Pts',(0.128028003046829,0.0546551750765237,
1.46077409326425));
#17112=CARTESIAN_POINT('Ctrl Pts',(0.0235079116789307,0.137209630484779,
1.46871308290156));
#17113=CARTESIAN_POINT('Ctrl Pts',(-0.102537447198224,0.0941531272373115,
1.47665207253886));
#17114=CARTESIAN_POINT('Ctrl Pts',(-0.134706575776555,-0.0350847218495708,
1.48459106217617));
#17115=CARTESIAN_POINT('Ctrl Pts',(-0.0435804807853106,-0.132222740314769,
1.49253005181348));
#17116=CARTESIAN_POINT('Ctrl Pts',(0.0874774386997331,-0.108286040948335,
1.50046904145078));
#17117=CARTESIAN_POINT('Ctrl Pts',(0.138385550162814,0.0147146982980264,
1.50840803108809));
#17118=CARTESIAN_POINT('Ctrl Pts',(0.0627460642121078,0.124368470664037,
1.51634702072539));
#17119=CARTESIAN_POINT('Ctrl Pts',(-0.0706026869052757,0.119928391791904,
1.5242860103627));
#17120=CARTESIAN_POINT('Ctrl Pts',(-0.116004137797729,0.0441355889673283,
1.5295786701209));
#17121=CARTESIAN_POINT('Ctrl Pts',(-0.117668597464313,0.00500517689812487,
1.532225));
#17122=CARTESIAN_POINT('',(0.0684664424539461,-0.0958295198918396,0.));
#17123=CARTESIAN_POINT('Ctrl Pts',(0.0684664424539414,-0.095829519891843,
-1.38777878078145E-17));
#17124=CARTESIAN_POINT('Ctrl Pts',(0.100334321247169,-0.0730611673843044,
0.00264632987910189));
#17125=CARTESIAN_POINT('Ctrl Pts',(0.139021564822767,0.00636891437108143,
0.00793898963730573));
#17126=CARTESIAN_POINT('Ctrl Pts',(0.0699018669780613,0.120491966796142,
0.0158779792746114));
#17127=CARTESIAN_POINT('Ctrl Pts',(-0.0632645460347191,0.123954346655885,
0.0238169689119172));
#17128=CARTESIAN_POINT('Ctrl Pts',(-0.11596266760442,0.0470121293552651,
0.0293787386625077));
#17129=CARTESIAN_POINT('Ctrl Pts',(-0.117944740497024,0.00404481602818191,
0.0322941785339964));
#17130=CARTESIAN_POINT('Ctrl Pts',(-0.117917485785546,7.60014832213644E-5,
0.0325632885263832));
#17131=CARTESIAN_POINT('Ctrl Pts',(0.0635546915223951,0.132092229195826,
-2.16840434497101E-19));
#17132=CARTESIAN_POINT('Ctrl Pts',(0.0668114782730532,0.13015255741457,
-1.00603861447787E-18));
#17133=CARTESIAN_POINT('Ctrl Pts',(0.0699821360194518,0.12808121947321,
-2.9262196004085E-17));
#17134=CARTESIAN_POINT('Ctrl Pts',(0.0730575207853233,0.125877721325919,
-2.71050543121376E-17));
#17135=CARTESIAN_POINT('Ctrl Pts',(0.0789281193465506,0.121671466161783,
-2.36378102375718E-17));
#17136=CARTESIAN_POINT('Ctrl Pts',(0.0844522091809674,0.11698398814956,
1.43782932504085E-18));
#17137=CARTESIAN_POINT('Ctrl Pts',(0.0895990070394484,0.111875963994554,
9.97465998686664E-18));
#17138=CARTESIAN_POINT('Ctrl Pts',(0.0928865546640729,0.108613183302742,
1.54276111490851E-17));
#17139=CARTESIAN_POINT('Ctrl Pts',(0.0960206821069302,0.105176950779614,
-2.53636710091701E-17));
#17140=CARTESIAN_POINT('Ctrl Pts',(0.098978417360439,0.101599719103904,
-1.56125112837913E-17));
#17141=CARTESIAN_POINT('Ctrl Pts',(0.103148772110026,0.0965558852815647,
-1.86354736740503E-18));
#17142=CARTESIAN_POINT('Ctrl Pts',(0.106976174326278,0.0912251680483688,
1.1337629845105E-17));
#17143=CARTESIAN_POINT('Ctrl Pts',(0.110435561611279,0.0856523061447448,
2.03830008427275E-17));
#17144=CARTESIAN_POINT('Ctrl Pts',(0.112407683932559,0.0824753373788608,
2.55395723911076E-17));
#17145=CARTESIAN_POINT('Ctrl Pts',(0.114261188142284,0.0792174064057451,
2.29308760465575E-17));
#17146=CARTESIAN_POINT('Ctrl Pts',(0.115986535786665,0.0758936579718971,
2.08166817117217E-17));
#17147=CARTESIAN_POINT('Ctrl Pts',(0.120573220307724,0.0670577659456877,
1.51962825639422E-17));
#17148=CARTESIAN_POINT('Ctrl Pts',(0.124235263225439,0.0578042025119142,
2.52358375750583E-18));
#17149=CARTESIAN_POINT('Ctrl Pts',(0.126883306113679,0.0482911783993335,
1.30104260698261E-17));
#17150=CARTESIAN_POINT('Ctrl Pts',(0.128478610866444,0.0425600882242624,
1.93281898253259E-17));
#17151=CARTESIAN_POINT('Ctrl Pts',(0.129704960854084,0.0367345196138549,
-5.78096029915021E-19));
#17152=CARTESIAN_POINT('Ctrl Pts',(0.130533291754837,0.0308494671050701,
0.));
#17153=CARTESIAN_POINT('Ctrl Pts',(0.131003715791213,0.0275072397983871,
3.2831114661813E-19));
#17154=CARTESIAN_POINT('Ctrl Pts',(0.131345346899704,0.0241444941465381,
-1.7128612844445E-18));
#17155=CARTESIAN_POINT('Ctrl Pts',(0.131551728167405,0.0207857616715298,
2.60208521396521E-18));
#17156=CARTESIAN_POINT('Ctrl Pts',(0.131851321606701,0.0159100565018035,
8.86587880453295E-18));
#17157=CARTESIAN_POINT('Ctrl Pts',(0.131867617692795,0.0110341713389591,
-1.68111772803455E-17));
#17158=CARTESIAN_POINT('Ctrl Pts',(0.131586936334964,0.0061777758930637,
-6.93889390390723E-18));
#17159=CARTESIAN_POINT('Ctrl Pts',(0.131099036368572,-0.00226395031615145,
9.98510028643051E-18));
#17160=CARTESIAN_POINT('Ctrl Pts',(0.129715139118287,-0.0106479390144509,
1.03491660509995E-17));
#17161=CARTESIAN_POINT('Ctrl Pts',(0.127493709984164,-0.018859987399606,
1.04083408558608E-17));
#17162=CARTESIAN_POINT('Ctrl Pts',(0.126553994220251,-0.0223338732882013,
1.04333731632617E-17));
#17163=CARTESIAN_POINT('Ctrl Pts',(0.125463061762623,-0.0257782540966497,
1.75224609115742E-17));
#17164=CARTESIAN_POINT('Ctrl Pts',(0.124232565886791,-0.0291638780753137,
1.73472347597681E-17));
#17165=CARTESIAN_POINT('Ctrl Pts',(0.12170396813588,-0.0361211392462112,
1.69871551674183E-17));
#17166=CARTESIAN_POINT('Ctrl Pts',(0.118582485980247,-0.0428512226170345,
-6.45748389186585E-19));
#17167=CARTESIAN_POINT('Ctrl Pts',(0.114911168983798,-0.0492778939609075,
3.46944695195361E-18));
#17168=CARTESIAN_POINT('Ctrl Pts',(0.112347970921096,-0.0537647937721124,
6.34254691478841E-18));
#17169=CARTESIAN_POINT('Ctrl Pts',(0.109516356061708,-0.0581036184196785,
-1.05628593522785E-17));
#17170=CARTESIAN_POINT('Ctrl Pts',(0.106427098863261,-0.0622637901458048,
-1.21430643318376E-17));
#17171=CARTESIAN_POINT('Ctrl Pts',(0.104287070791936,-0.0651456752410043,
-1.32377232732828E-17));
#17172=CARTESIAN_POINT('Ctrl Pts',(0.102021590876101,-0.067943056099314,
-1.03088264066386E-17));
#17173=CARTESIAN_POINT('Ctrl Pts',(0.0996491962474235,-0.0706287444932102,
-1.04083408558608E-17));
#17174=CARTESIAN_POINT('Ctrl Pts',(0.0938611946766418,-0.0771810981592459,
-1.06511292104842E-17));
#17175=CARTESIAN_POINT('Ctrl Pts',(0.0874218747326319,-0.0830961188460978,
9.460259835177E-18));
#17176=CARTESIAN_POINT('Ctrl Pts',(0.0803902102994179,-0.0882260767030795,
2.94902990916057E-17));
#17177=CARTESIAN_POINT('Ctrl Pts',(0.0765868618375105,-0.091000813397402,
4.03243227742548E-17));
#17178=CARTESIAN_POINT('Ctrl Pts',(0.0726097989303321,-0.0935451549285004,
-2.49510848448888E-18));
#17179=CARTESIAN_POINT('Ctrl Pts',(0.0684664424539416,-0.0958295198918429,
0.));
#17180=CARTESIAN_POINT('Ctrl Pts',(-0.00156962371674571,0.146072546381438,
1.50365));
#17181=CARTESIAN_POINT('Ctrl Pts',(0.0218361081466035,0.146362061217761,
1.50238307892777));
#17182=CARTESIAN_POINT('Ctrl Pts',(0.0452966847593804,0.141345883428421,
1.50111615785553));
#17183=CARTESIAN_POINT('Ctrl Pts',(0.0660179268768178,0.130913916311315,
1.4998492367833));
#17184=CARTESIAN_POINT('Ctrl Pts',(0.109300214423576,0.109123745727819,
1.4972029069042));
#17185=CARTESIAN_POINT('Ctrl Pts',(0.140630685714559,0.0637042888941242,
1.49455657702509));
#17186=CARTESIAN_POINT('Ctrl Pts',(0.145752650840527,0.0155206226173656,
1.49191024714599));
#17187=CARTESIAN_POINT('Ctrl Pts',(0.150874615966495,-0.0326630436593903,
1.48926391726689));
#17188=CARTESIAN_POINT('Ctrl Pts',(0.129788074927449,-0.0836109193792113,
1.48661758738779));
#17189=CARTESIAN_POINT('Ctrl Pts',(0.0921021927661857,-0.114042242015571,
1.48397125750869));
#17190=CARTESIAN_POINT('Ctrl Pts',(0.0544163106049216,-0.144473564651931,
1.48132492762959));
#17191=CARTESIAN_POINT('Ctrl Pts',(0.000131087321441313,-0.154388334204831,
1.47867859775048));
#17192=CARTESIAN_POINT('Ctrl Pts',(-0.0458840977328367,-0.139228052523514,
1.47603226787138));
#17193=CARTESIAN_POINT('Ctrl Pts',(-0.0918992827871148,-0.124067770842196,
1.47338593799228));
#17194=CARTESIAN_POINT('Ctrl Pts',(-0.129644429612189,-0.0838324379266627,
1.47073960811318));
#17195=CARTESIAN_POINT('Ctrl Pts',(-0.141854649713415,-0.0369491035797489,
1.46809327823408));
#17196=CARTESIAN_POINT('Ctrl Pts',(-0.14497337938942,-0.0249741805295802,
1.46741735368415));
#17197=CARTESIAN_POINT('Ctrl Pts',(-0.146426231435716,-0.0125655473306973,
1.46674142913422));
#17198=CARTESIAN_POINT('Ctrl Pts',(-0.14631473222987,-0.000131398079681141,
1.46606550458429));
#17199=CARTESIAN_POINT('Origin',(0.,0.,-0.0924367114736175));
#17200=CARTESIAN_POINT('',(-0.0684664424539507,-0.0958295198918364,0.));
#17201=CARTESIAN_POINT('Ctrl Pts',(-0.0686146973663072,-0.0959584553529141,
8.16675286424706E-17));
#17202=CARTESIAN_POINT('Ctrl Pts',(-0.0391968190522335,-0.116741470120209,
0.00244290680874874));
#17203=CARTESIAN_POINT('Ctrl Pts',(0.0436301113039178,-0.130476273073809,
0.0075332029917574));
#17204=CARTESIAN_POINT('Ctrl Pts',(0.134092250525203,-0.0374520209666004,
0.0152708885490261));
#17205=CARTESIAN_POINT('Ctrl Pts',(0.104134301645602,0.0924305194826295,
0.023213056671806));
#17206=CARTESIAN_POINT('Ctrl Pts',(-0.0212379681243542,0.137589894578696,
0.0311552247945861));
#17207=CARTESIAN_POINT('Ctrl Pts',(-0.106685947947232,0.0723488109778776,
0.0375631097285225));
#17208=CARTESIAN_POINT('Ctrl Pts',(-0.117663533972591,0.0165813593984342,
0.041323605288199));
#17209=CARTESIAN_POINT('Ctrl Pts',(-0.117600989619072,5.04992496179954E-5,
0.0424367114736154));
#17210=CARTESIAN_POINT('Origin',(0.,0.,0.));
#17211=CARTESIAN_POINT('Ctrl Pts',(-0.0510216505388318,0.106149619882943,
-0.0164977839420939));
#17212=CARTESIAN_POINT('Ctrl Pts',(-0.0863355867949722,0.0891756983861136,
-0.0138503945678339));
#17213=CARTESIAN_POINT('Ctrl Pts',(-0.13808023131828,0.0175094743621551,
-0.00855561581931395));
#17214=CARTESIAN_POINT('Ctrl Pts',(-0.0894531427980795,-0.106808298616542,
-0.000613447696533924));
#17215=CARTESIAN_POINT('Ctrl Pts',(0.0412394829729132,-0.132934609947913,
0.00732872042624606));
#17216=CARTESIAN_POINT('Ctrl Pts',(0.134092250525203,-0.0374520209666004,
0.0152708885490261));
#17217=CARTESIAN_POINT('Ctrl Pts',(0.104134301645602,0.0924305194826295,
0.023213056671806));
#17218=CARTESIAN_POINT('Ctrl Pts',(-0.0212379681243542,0.137589894578696,
0.0311552247945861));
#17219=CARTESIAN_POINT('Ctrl Pts',(-0.127145335141994,0.0567276974868182,
0.039097392917366));
#17220=CARTESIAN_POINT('Ctrl Pts',(-0.116579117211717,-0.0761160149501382,
0.0470395610401461));
#17221=CARTESIAN_POINT('Ctrl Pts',(0.000787973702835166,-0.139222729671589,
0.054981729162926));
#17222=CARTESIAN_POINT('Ctrl Pts',(0.117431922513572,-0.0747907597173192,
0.0629238972857061));
#17223=CARTESIAN_POINT('Ctrl Pts',(0.126496838785129,0.0581591461343325,
0.070866065408486));
#17224=CARTESIAN_POINT('Ctrl Pts',(0.0196773008918215,0.137828289815661,
0.0788082335312661));
#17225=CARTESIAN_POINT('Ctrl Pts',(-0.105168479521776,0.0912330920368172,
0.0867504016540459));
#17226=CARTESIAN_POINT('Ctrl Pts',(-0.133669226619255,-0.0389412707994331,
0.0946925697768262));
#17227=CARTESIAN_POINT('Ctrl Pts',(-0.0397151780004399,-0.133441281507892,
0.102634737899606));
#17228=CARTESIAN_POINT('Ctrl Pts',(0.0906220264938673,-0.105695447092796,
0.110576906022386));
#17229=CARTESIAN_POINT('Ctrl Pts',(0.137940159127448,0.0188783162799928,
0.118519074145166));
#17230=CARTESIAN_POINT('Ctrl Pts',(0.0588909273047484,0.126157580947307,
0.126461242267946));
#17231=CARTESIAN_POINT('Ctrl Pts',(-0.074108440039672,0.117863552156501,
0.134403410390726));
#17232=CARTESIAN_POINT('Ctrl Pts',(-0.139216864956951,0.00159439502933392,
0.142345578513506));
#17233=CARTESIAN_POINT('Ctrl Pts',(-0.0767883381764272,-0.116135388594389,
0.150287746636286));
#17234=CARTESIAN_POINT('Ctrl Pts',(0.0559861945572589,-0.127473226882309,
0.158229914759066));
#17235=CARTESIAN_POINT('Ctrl Pts',(0.137471621702818,-0.0220324926503626,
0.166172082881846));
#17236=CARTESIAN_POINT('Ctrl Pts',(0.0930189202108026,0.103592267873211,
0.174114251004626));
#17237=CARTESIAN_POINT('Ctrl Pts',(-0.0366486683060043,0.134315868829211,
0.182056419127406));
#17238=CARTESIAN_POINT('Ctrl Pts',(-0.132742311638566,0.0419923350165386,
0.189998587250186));
#17239=CARTESIAN_POINT('Ctrl Pts',(-0.107230360350792,-0.0888004916405464,
0.197940755372966));
#17240=CARTESIAN_POINT('Ctrl Pts',(0.0165156171993534,-0.138242945169174,
0.205882923495746));
#17241=CARTESIAN_POINT('Ctrl Pts',(0.125131592687617,-0.061040658666823,
0.213825091618526));
#17242=CARTESIAN_POINT('Ctrl Pts',(0.119114174013628,0.0720811421096423,
0.221767259741306));
#17243=CARTESIAN_POINT('Ctrl Pts',(0.0039759348809324,0.139169211541763,
0.229709427864086));
#17244=CARTESIAN_POINT('Ctrl Pts',(-0.114804669066963,0.0787639858025777,
0.237651595986866));
#17245=CARTESIAN_POINT('Ctrl Pts',(-0.128412401817242,-0.0537971426620367,
0.245593764109646));
#17246=CARTESIAN_POINT('Ctrl Pts',(-0.024381182195918,-0.137074561658528,
0.253535932232426));
#17247=CARTESIAN_POINT('Ctrl Pts',(0.101985705091022,-0.094777599970642,
0.261478100355206));
#17248=CARTESIAN_POINT('Ctrl Pts',(0.134923209124943,0.0343453801629359,
0.269420268477986));
#17249=CARTESIAN_POINT('Ctrl Pts',(0.0442571924125319,0.132004463632409,
0.277362436600766));
#17250=CARTESIAN_POINT('Ctrl Pts',(-0.0869529592639067,0.108733897080731,
0.285304604723546));
#17251=CARTESIAN_POINT('Ctrl Pts',(-0.138505267237684,-0.0141480898545381,
0.293246772846326));
#17252=CARTESIAN_POINT('Ctrl Pts',(-0.0631725212350128,-0.124068972994571,
0.301188940969106));
#17253=CARTESIAN_POINT('Ctrl Pts',(0.0700327441786229,-0.12032993078169,
0.309131109091886));
#17254=CARTESIAN_POINT('Ctrl Pts',(0.139080821187468,-0.00635631000930847,
0.317073277214666));
#17255=CARTESIAN_POINT('Ctrl Pts',(0.0807165776729536,0.11344034374014,
0.325015445337446));
#17256=CARTESIAN_POINT('Ctrl Pts',(-0.0515923433190751,0.129313988454311,
0.332957613460226));
#17257=CARTESIAN_POINT('Ctrl Pts',(-0.136637377548019,0.026722734813544,
0.340899781583006));
#17258=CARTESIAN_POINT('Ctrl Pts',(-0.0965085366518414,-0.100349289247285,
0.348841949705786));
#17259=CARTESIAN_POINT('Ctrl Pts',(0.0320320385160992,-0.135491055083419,
0.356784117828566));
#17260=CARTESIAN_POINT('Ctrl Pts',(0.131227975626944,-0.0465090949381858,
0.364726285951346));
#17261=CARTESIAN_POINT('Ctrl Pts',(0.110205605501345,0.0850799742312894,
0.372668454074126));
#17262=CARTESIAN_POINT('Ctrl Pts',(-0.0117764211155082,0.138727046407055,
0.380610622196906));
#17263=CARTESIAN_POINT('Ctrl Pts',(-0.122970036152848,0.065285892102983,
0.388552790319686));
#17264=CARTESIAN_POINT('Ctrl Pts',(-0.121510464882371,-0.0679638464419502,
0.396494958442466));
#17265=CARTESIAN_POINT('Ctrl Pts',(-0.00873482453528946,-0.138951719454826,
0.404437126565246));
#17266=CARTESIAN_POINT('Ctrl Pts',(0.112042812448737,-0.0826455423945668,
0.412379294688026));
#17267=CARTESIAN_POINT('Ctrl Pts',(0.130177722634257,0.049372441998279,
0.420321462810806));
#17268=CARTESIAN_POINT('Ctrl Pts',(0.0290564652212241,0.136160197297018,
0.428263630933586));
#17269=CARTESIAN_POINT('Ctrl Pts',(-0.098683499418539,0.098211223603141,
0.436205799056366));
#17270=CARTESIAN_POINT('Ctrl Pts',(-0.136019240449831,-0.0297093205335648,
0.444147967179146));
#17271=CARTESIAN_POINT('Ctrl Pts',(-0.0487473834415776,-0.130413074907061,
0.452090135301926));
#17272=CARTESIAN_POINT('Ctrl Pts',(0.0831820848081396,-0.111645054821459,
0.460032303424706));
#17273=CARTESIAN_POINT('Ctrl Pts',(0.138908217753341,0.00940130521287039,
0.467974471547486));
#17274=CARTESIAN_POINT('Ctrl Pts',(0.0673801526530663,0.121835103839429,
0.475916639670265));
#17275=CARTESIAN_POINT('Ctrl Pts',(-0.0658750545035054,0.12265543075329,
0.483858807793047));
#17276=CARTESIAN_POINT('Ctrl Pts',(-0.138781944133385,0.0111107822259715,
0.491800975915825));
#17277=CARTESIAN_POINT('Ctrl Pts',(-0.084550315326251,-0.110612484274364,
0.499743144038607));
#17278=CARTESIAN_POINT('Ctrl Pts',(0.0471380885036503,-0.131003351527116,
0.507685312161385));
#17279=CARTESIAN_POINT('Ctrl Pts',(0.135643160584381,-0.031381690295376,
0.515627480284167));
#17280=CARTESIAN_POINT('Ctrl Pts',(0.0998851624184703,0.0969888232104648,
0.523569648406945));
#17281=CARTESIAN_POINT('Ctrl Pts',(-0.0273779061153799,0.136507610615132,
0.531511816529727));
#17282=CARTESIAN_POINT('Ctrl Pts',(-0.129560000008381,0.0509714027366644,
0.539453984652505));
#17283=CARTESIAN_POINT('Ctrl Pts',(-0.113051823689188,-0.0812598465397498,
0.547396152775286));
#17284=CARTESIAN_POINT('Ctrl Pts',(0.00702343738442799,-0.139048728244533,
0.555338320898066));
#17285=CARTESIAN_POINT('Ctrl Pts',(0.12066450826877,-0.0694546898587181,
0.563280489020846));
#17286=CARTESIAN_POINT('Ctrl Pts',(0.123764493242992,0.063766979789076,
0.571222657143626));
#17287=CARTESIAN_POINT('Ctrl Pts',(0.0134834875971477,0.13857154491934,
0.579164825266405));
#17288=CARTESIAN_POINT('Ctrl Pts',(-0.109149777898995,0.0864303389077871,
0.587106993389186));
#17289=CARTESIAN_POINT('Ctrl Pts',(-0.131790633456927,-0.0448899368693808,
0.595049161511966));
#17290=CARTESIAN_POINT('Ctrl Pts',(-0.0336977294021144,-0.135086418755761,
0.602991329634746));
#17291=CARTESIAN_POINT('Ctrl Pts',(0.0952657566843092,-0.101529863106778,
0.610933497757526));
#17292=CARTESIAN_POINT('Ctrl Pts',(0.136956022624868,0.025038477707157,
0.618875665880307));
#17293=CARTESIAN_POINT('Ctrl Pts',(0.0531805018142573,0.128669000640787,
0.626817834003085));
#17294=CARTESIAN_POINT('Ctrl Pts',(-0.0793138220987445,0.114425500318782,
0.634760002125867));
#17295=CARTESIAN_POINT('Ctrl Pts',(-0.139148536750765,-0.00464351367351466,
0.642702170248646));
#17296=CARTESIAN_POINT('Ctrl Pts',(-0.0715088964667609,-0.119458592094588,
0.650644338371427));
#17297=CARTESIAN_POINT('Ctrl Pts',(0.0616402393688536,-0.124837327709565,
0.658586506494205));
#17298=CARTESIAN_POINT('Ctrl Pts',(0.138320583400205,-0.0158522461166236,
0.666528674616987));
#17299=CARTESIAN_POINT('Ctrl Pts',(0.0882850628235238,0.107655121482266,
0.674470842739765));
#17300=CARTESIAN_POINT('Ctrl Pts',(-0.0426286451686149,0.132539337972556,
0.682413010862546));
#17301=CARTESIAN_POINT('Ctrl Pts',(-0.13449013477919,0.0360039045964495,
0.690355178985326));
#17302=CARTESIAN_POINT('Ctrl Pts',(-0.103144844235522,-0.0935148042116587,
0.698297347108106));
#17303=CARTESIAN_POINT('Ctrl Pts',(0.022691720100341,-0.137364345221032,
0.706239515230886));
#17304=CARTESIAN_POINT('Ctrl Pts',(0.127740337615313,-0.0553740340325759,
0.714181683353665));
#17305=CARTESIAN_POINT('Ctrl Pts',(0.115765682611161,0.077344581120379,
0.722123851476446));
#17306=CARTESIAN_POINT('Ctrl Pts',(-0.00226223072526165,0.139207614056346,
0.730066019599226));
#17307=CARTESIAN_POINT('Ctrl Pts',(-0.118217708309552,0.0735421711751344,
0.738008187722006));
#17308=CARTESIAN_POINT('Ctrl Pts',(-0.125873620115675,-0.059495455776806,
0.745950355844786));
#17309=CARTESIAN_POINT('Ctrl Pts',(-0.0182163644075178,-0.138029133036789,
0.753892523967566));
#17310=CARTESIAN_POINT('Ctrl Pts',(0.106128952536144,-0.0901139441634624,
0.761834692090347));
#17311=CARTESIAN_POINT('Ctrl Pts',(0.133249245915149,0.0403548753208232,
0.769776860213125));
#17312=CARTESIAN_POINT('Ctrl Pts',(0.0382995408207276,0.133854483197375,
0.777719028335907));
#17313=CARTESIAN_POINT('Ctrl Pts',(-0.0917364783268051,0.104729633071593,
0.785661196458685));
#17314=CARTESIAN_POINT('Ctrl Pts',(-0.137732458880487,-0.0203383202317681,
0.793603364581467));
#17315=CARTESIAN_POINT('Ctrl Pts',(-0.0575513573065257,-0.126774282767806,
0.801545532704245));
#17316=CARTESIAN_POINT('Ctrl Pts',(0.0753527000357912,-0.117071978271622,
0.809487700827026));
#17317=CARTESIAN_POINT('Ctrl Pts',(0.139225942868322,-0.000119714417332432,
0.817429868949805));
#17318=CARTESIAN_POINT('Ctrl Pts',(0.0755539188089132,0.116942220141962,
0.825372037072586));
#17319=CARTESIAN_POINT('Ctrl Pts',(-0.0573332568284509,0.12687306712048,
0.833314205195366));
#17320=CARTESIAN_POINT('Ctrl Pts',(-0.13769727914169,0.0205751504512258,
0.841256373318145));
#17321=CARTESIAN_POINT('Ctrl Pts',(-0.0919164475821765,-0.104571717796869,
0.849198541440926));
#17322=CARTESIAN_POINT('Ctrl Pts',(0.0380692928980519,-0.133920149482284,
0.857140709563706));
#17323=CARTESIAN_POINT('Ctrl Pts',(0.133179650076608,-0.0405839661022353,
0.865082877686486));
#17324=CARTESIAN_POINT('Ctrl Pts',(0.106283765719693,0.0899312995767124,
0.873025045809266));
#17325=CARTESIAN_POINT('Ctrl Pts',(-0.0179789669825735,0.138060255849953,
0.880967213932046));
#17326=CARTESIAN_POINT('Ctrl Pts',(-0.125771118879347,0.0597118342956578,
0.888909382054826));
#17327=CARTESIAN_POINT('Ctrl Pts',(-0.118344004924669,-0.0733387619032726,
0.896851550177606));
#17328=CARTESIAN_POINT('Ctrl Pts',(-0.00250162451743248,-0.139203517821528,
0.904793718300386));
#17329=CARTESIAN_POINT('Ctrl Pts',(0.115632500949424,-0.0775435504945224,
0.912735886423165));
#17330=CARTESIAN_POINT('Ctrl Pts',(0.127835376168433,0.0551542754370876,
0.920678054545947));
#17331=CARTESIAN_POINT('Ctrl Pts',(0.0229279137899797,0.137325118854324,
0.928620222668725));
#17332=CARTESIAN_POINT('Ctrl Pts',(-0.102983873094174,0.0936920454555137,
0.936562390791507));
#17333=CARTESIAN_POINT('Ctrl Pts',(-0.134551852288801,-0.0357725669300891,
0.944504558914285));
#17334=CARTESIAN_POINT('Ctrl Pts',(-0.0428565117498991,-0.132465832952297,
0.952446727037066));
#17335=CARTESIAN_POINT('Ctrl Pts',(0.0880997963686447,-0.107806787258123,
0.960388895159846));
#17336=CARTESIAN_POINT('Ctrl Pts',(0.138347640177547,0.0156143509765511,
0.968331063282625));
#17337=CARTESIAN_POINT('Ctrl Pts',(0.061854832590724,0.124731139593481,
0.976273231405407));
#17338=CARTESIAN_POINT('Ctrl Pts',(-0.0713033562375951,0.119581390225944,
0.984215399528185));
#17339=CARTESIAN_POINT('Ctrl Pts',(-0.139140345480169,0.00488280234845834,
0.992157567650966));
#17340=CARTESIAN_POINT('Ctrl Pts',(-0.0795104838321055,-0.114288934109561,
1.00009973577375));
#17341=CARTESIAN_POINT('Ctrl Pts',(0.0529591494285269,-0.128760265574912,
1.00804190389653));
#17342=CARTESIAN_POINT('Ctrl Pts',(0.136912761112491,-0.0252739657289669,
1.0159840720193));
#17343=CARTESIAN_POINT('Ctrl Pts',(0.0954402180350474,0.101365883217864,
1.02392624014209));
#17344=CARTESIAN_POINT('Ctrl Pts',(-0.0334653697086341,0.135144169424284,
1.03186840826486));
#17345=CARTESIAN_POINT('Ctrl Pts',(-0.131713240771149,0.0451165125500212,
1.03981057638765));
#17346=CARTESIAN_POINT('Ctrl Pts',(-0.109298251871946,-0.0862425048155002,
1.04775274451043));
#17347=CARTESIAN_POINT('Ctrl Pts',(0.0132451643780021,-0.13859452774087,
1.05569491263321));
#17348=CARTESIAN_POINT('Ctrl Pts',(0.123654649330263,-0.0639797248987874,
1.06363708075599));
#17349=CARTESIAN_POINT('Ctrl Pts',(0.120783771971213,0.0692470788374567,
1.07157924887876));
#17350=CARTESIAN_POINT('Ctrl Pts',(0.00726255089817806,0.139036444335888,
1.07952141700155));
#17351=CARTESIAN_POINT('Ctrl Pts',(-0.112911912907791,0.0814541430660127,
1.08746358512433));
#17352=CARTESIAN_POINT('Ctrl Pts',(-0.129647464608677,-0.0507485213543897,
1.09540575324711));
#17353=CARTESIAN_POINT('Ctrl Pts',(-0.0276126195379174,-0.136460326620484,
1.10334792136989));
#17354=CARTESIAN_POINT('Ctrl Pts',(0.0997182217817603,-0.0971604536002107,
1.11129008949267));
#17355=CARTESIAN_POINT('Ctrl Pts',(0.135696927507188,0.0311483765905046,
1.11923225761545));
#17356=CARTESIAN_POINT('Ctrl Pts',(0.0473633069609982,0.130922093830007,
1.12717442573822));
#17357=CARTESIAN_POINT('Ctrl Pts',(-0.0843599685788644,0.110757722983492,
1.13511659386101));
#17358=CARTESIAN_POINT('Ctrl Pts',(-0.138800846271631,-0.0108721006891078,
1.14305876198379));
#17359=CARTESIAN_POINT('Ctrl Pts',(-0.0660858892268601,-0.122541963197144,
1.15100093010657));
#17360=CARTESIAN_POINT('Ctrl Pts',(0.0671705316110708,-0.121950798202395,
1.15894309822935));
#17361=CARTESIAN_POINT('Ctrl Pts',(0.138891844802359,-0.00964017357273747,
1.16688526635212));
#17362=CARTESIAN_POINT('Ctrl Pts',(0.0833739592533277,0.111501840422208,
1.17482743447491));
#17363=CARTESIAN_POINT('Ctrl Pts',(-0.0485230383040216,0.130496713571114,
1.18276960259768));
#17364=CARTESIAN_POINT('Ctrl Pts',(-0.135967947813762,0.0299431906521225,
1.19071177072047));
#17365=CARTESIAN_POINT('Ctrl Pts',(-0.0988522486080867,-0.0980413710850678,
1.19865393884324));
#17366=CARTESIAN_POINT('Ctrl Pts',(0.0288222657999454,-0.136209964735594,
1.20659610696603));
#17367=CARTESIAN_POINT('Ctrl Pts',(0.130092623711363,-0.0495962373069701,
1.21453827508881));
#17368=CARTESIAN_POINT('Ctrl Pts',(0.112184773380136,0.082452738709893,
1.22248044321158));
#17369=CARTESIAN_POINT('Ctrl Pts',(-0.00849585454694533,0.138966535376798,
1.23042261133437));
#17370=CARTESIAN_POINT('Ctrl Pts',(-0.121393406896754,0.0681727090639588,
1.23836477945715));
#17371=CARTESIAN_POINT('Ctrl Pts',(-0.123082127310551,-0.0650743223999996,
1.24630694757992));
#17372=CARTESIAN_POINT('Ctrl Pts',(-0.0120149744006178,-0.138706589206355,
1.25424911570271));
#17373=CARTESIAN_POINT('Ctrl Pts',(0.110059129405696,-0.0852693704304675,
1.26219128382548));
#17374=CARTESIAN_POINT('Ctrl Pts',(0.13130776387206,0.0462833517151888,
1.27013345194827));
#17375=CARTESIAN_POINT('Ctrl Pts',(0.0322649968732001,0.135435768819968,
1.27807562007105));
#17376=CARTESIAN_POINT('Ctrl Pts',(-0.0963358219719167,0.100515107841202,
1.28601778819382));
#17377=CARTESIAN_POINT('Ctrl Pts',(-0.136683130933199,-0.0264877182308561,
1.29395995631661));
#17378=CARTESIAN_POINT('Ctrl Pts',(-0.0518146499729274,-0.129225073214149,
1.30190212443939));
#17379=CARTESIAN_POINT('Ctrl Pts',(0.0805213734929343,-0.11357898534207,
1.30984429256217));
#17380=CARTESIAN_POINT('Ctrl Pts',(0.1390915465469,0.0061171215252809,1.31778646068495));
#17381=CARTESIAN_POINT('Ctrl Pts',(0.0702395735793815,0.120209316621791,
1.32572862880773));
#17382=CARTESIAN_POINT('Ctrl Pts',(-0.0629590648350173,0.124177428154433,
1.33367079693051));
#17383=CARTESIAN_POINT('Ctrl Pts',(-0.138480731711197,0.0143862582011507,
1.34161296505328));
#17384=CARTESIAN_POINT('Ctrl Pts',(-0.0871398218994898,-0.108584202098263,
1.34955513317607));
#17385=CARTESIAN_POINT('Ctrl Pts',(0.0440301174146577,-0.132080378229483,
1.35749730129884));
#17386=CARTESIAN_POINT('Ctrl Pts',(0.13486394497766,-0.0345773583278084,
1.36543946942163));
#17387=CARTESIAN_POINT('Ctrl Pts',(0.102148545386143,0.0946020732301706,
1.3733816375444));
#17388=CARTESIAN_POINT('Ctrl Pts',(-0.0241454188302812,0.137116288461919,
1.38132380566719));
#17389=CARTESIAN_POINT('Ctrl Pts',(-0.128319693277533,0.0540178939468163,
1.38926597378996));
#17390=CARTESIAN_POINT('Ctrl Pts',(-0.114939956470138,-0.0785664351508689,
1.39720814191275));
#17391=CARTESIAN_POINT('Ctrl Pts',(0.00373660876362508,-0.139175849115243,
1.40515031003553));
#17392=CARTESIAN_POINT('Ctrl Pts',(0.118990018389619,-0.0722858665142316,
1.41309247815831));
#17393=CARTESIAN_POINT('Ctrl Pts',(0.125236419206141,0.0608253567263532,
1.42103464628109));
#17394=CARTESIAN_POINT('Ctrl Pts',(0.0167532566496359,0.13821437898841,
1.42897681440387));
#17395=CARTESIAN_POINT('Ctrl Pts',(-0.107077349343502,0.0889846891406984,
1.43691898252665));
#17396=CARTESIAN_POINT('Ctrl Pts',(-0.132814597987359,-0.0417638487589672,
1.44486115064943));
#17397=CARTESIAN_POINT('Ctrl Pts',(-0.0368790902657646,-0.134252921254984,
1.45280331877221));
#17398=CARTESIAN_POINT('Ctrl Pts',(0.0928396680879532,-0.103751556080299,
1.46074548689499));
#17399=CARTESIAN_POINT('Ctrl Pts',(0.137511141307062,0.0217950526079239,
1.46868765501776));
#17400=CARTESIAN_POINT('Ctrl Pts',(0.0562018483347667,0.127378648737854,
1.47662982314055));
#17401=CARTESIAN_POINT('Ctrl Pts',(-0.0765818961642769,0.116263681173923,
1.48457199126332));
#17402=CARTESIAN_POINT('Ctrl Pts',(-0.13923195096087,-0.00134816270381636,
1.49251415938611));
#17403=CARTESIAN_POINT('Ctrl Pts',(-0.0742871760264013,-0.117748889605885,
1.50045632750888));
#17404=CARTESIAN_POINT('Ctrl Pts',(0.0586284551779338,-0.126233948370975,
1.50839849563167));
#17405=CARTESIAN_POINT('Ctrl Pts',(0.137995068118234,-0.019163470063063,
1.51634066375444));
#17406=CARTESIAN_POINT('Ctrl Pts',(0.0906261803825392,0.105639137646141,
1.52428283187723));
#17407=CARTESIAN_POINT('Ctrl Pts',(0.00417072711528833,0.124051375507138,
1.52957761062575));
#17408=CARTESIAN_POINT('Ctrl Pts',(-0.0334019664627544,0.1129391839063,
1.53222500000001));
#17409=CARTESIAN_POINT('Ctrl Pts',(-0.0551480035117261,0.114734422509858,
-0.0109985226280628));
#17410=CARTESIAN_POINT('Ctrl Pts',(-0.093317938433455,0.0963877427684319,
-0.00835113325380276));
#17411=CARTESIAN_POINT('Ctrl Pts',(-0.149247407742026,0.0189255452031589,
-0.00305635450528277));
#17412=CARTESIAN_POINT('Ctrl Pts',(-0.0966876253720675,-0.115446371588928,
0.00488581361749726));
#17413=CARTESIAN_POINT('Ctrl Pts',(0.0445747075563756,-0.143685636564375,
0.0128279817402772));
#17414=CARTESIAN_POINT('Ctrl Pts',(0.144936900801175,-0.0404809362687151,
0.0207701498630572));
#17415=CARTESIAN_POINT('Ctrl Pts',(0.112556116319125,0.0999057960529736,
0.0287123179858373));
#17416=CARTESIAN_POINT('Ctrl Pts',(-0.0229555792165621,0.148717415239805,
0.0366544861086172));
#17417=CARTESIAN_POINT('Ctrl Pts',(-0.137428156769908,0.0613155244327884,
0.0445966542313972));
#17418=CARTESIAN_POINT('Ctrl Pts',(-0.126007400730642,-0.0822718633254329,
0.0525388223541772));
#17419=CARTESIAN_POINT('Ctrl Pts',(0.000851700720621877,-0.150482305134309,
0.0604809904769572));
#17420=CARTESIAN_POINT('Ctrl Pts',(0.126929176276611,-0.0808394286734405,
0.0684231585997372));
#17421=CARTESIAN_POINT('Ctrl Pts',(0.136727213562698,0.0628627408439891,
0.0763653267225173));
#17422=CARTESIAN_POINT('Ctrl Pts',(0.0212686937255662,0.148975090584026,
0.0843074948452972));
#17423=CARTESIAN_POINT('Ctrl Pts',(-0.113673932864549,0.0986115272026031,
0.0922496629680772));
#17424=CARTESIAN_POINT('Ctrl Pts',(-0.144479665027646,-0.0420906285100245,
0.100191831090857));
#17425=CARTESIAN_POINT('Ctrl Pts',(-0.0429271251068198,-0.144233284958223,
0.108133999213637));
#17426=CARTESIAN_POINT('Ctrl Pts',(0.0979510420095061,-0.114243518700172,
0.116076167336417));
#17427=CARTESIAN_POINT('Ctrl Pts',(0.149096007275942,0.0204050915936607,
0.124018335459197));
#17428=CARTESIAN_POINT('Ctrl Pts',(0.0636537044864716,0.136360518400275,
0.131960503581977));
#17429=CARTESIAN_POINT('Ctrl Pts',(-0.0801019266996435,0.127395713772213,
0.139902671704757));
#17430=CARTESIAN_POINT('Ctrl Pts',(-0.15047596611352,0.00172334100814176,
0.147844839827537));
#17431=CARTESIAN_POINT('Ctrl Pts',(-0.0829985603893774,-0.125527785761544,
0.155787007950317));
#17432=CARTESIAN_POINT('Ctrl Pts',(0.0605140527882773,-0.137782566606816,
0.163729176073097));
#17433=CARTESIAN_POINT('Ctrl Pts',(0.148589577098441,-0.0238143605552183,
0.171671344195877));
#17434=CARTESIAN_POINT('Ctrl Pts',(0.100541783424623,0.111970245809892,
0.179613512318657));
#17435=CARTESIAN_POINT('Ctrl Pts',(-0.0396126128240685,0.145178604134651,
0.187555680441437));
#17436=CARTESIAN_POINT('Ctrl Pts',(-0.143477786216001,0.0453884461694337,
0.195497848564217));
#17437=CARTESIAN_POINT('Ctrl Pts',(-0.115902567375552,-0.095982191346566,
0.203440016686997));
#17438=CARTESIAN_POINT('Ctrl Pts',(0.0178513102906219,-0.149423281002214,
0.211382184809777));
#17439=CARTESIAN_POINT('Ctrl Pts',(0.135251553802876,-0.0659772944027704,
0.219324352932557));
#17440=CARTESIAN_POINT('Ctrl Pts',(0.128747479107914,0.07791067196398,0.227266521055337));
#17441=CARTESIAN_POINT('Ctrl Pts',(0.00429748682099232,0.150424458749874,
0.235208689178117));
#17442=CARTESIAN_POINT('Ctrl Pts',(-0.124089444892588,0.0851339876261335,
0.243150857300897));
#17443=CARTESIAN_POINT('Ctrl Pts',(-0.138797696890977,-0.0581479623084488,
0.251093025423677));
#17444=CARTESIAN_POINT('Ctrl Pts',(-0.0263529993083425,-0.148160405002171,
0.259035193546457));
#17445=CARTESIAN_POINT('Ctrl Pts',(0.110233752987369,-0.102442695616748,
0.266977361669237));
#17446=CARTESIAN_POINT('Ctrl Pts',(0.145835062802846,0.0371230472913779,
0.274919529792017));
#17447=CARTESIAN_POINT('Ctrl Pts',(0.0478364728857143,0.142680265085169,
0.282861697914797));
#17448=CARTESIAN_POINT('Ctrl Pts',(-0.0939852406223356,0.117527701960322,
0.290803866037577));
#17449=CARTESIAN_POINT('Ctrl Pts',(-0.14970681824969,-0.01529231023972,
0.298746034160357));
#17450=CARTESIAN_POINT('Ctrl Pts',(-0.0682815703945392,-0.134102995221473,
0.306688202283137));
#17451=CARTESIAN_POINT('Ctrl Pts',(0.0756966107742644,-0.1300615596562,
0.314630370405917));
#17452=CARTESIAN_POINT('Ctrl Pts',(0.150328919865546,-0.00687037371415525,
0.322572538528697));
#17453=CARTESIAN_POINT('Ctrl Pts',(0.0872444944832666,0.122614780370367,
0.330514706651477));
#17454=CARTESIAN_POINT('Ctrl Pts',(-0.0557648508131485,0.139772198940638,
0.338456874774257));
#17455=CARTESIAN_POINT('Ctrl Pts',(-0.147687863823926,0.0288839239377102,
0.346399042897038));
#17456=CARTESIAN_POINT('Ctrl Pts',(-0.104313621021262,-0.10846499275041,
0.354341211019817));
#17457=CARTESIAN_POINT('Ctrl Pts',(0.0346226151823369,-0.146448833047075,
0.362283379142597));
#17458=CARTESIAN_POINT('Ctrl Pts',(0.141840978962514,-0.0502704970123603,
0.370225547265377));
#17459=CARTESIAN_POINT('Ctrl Pts',(0.119118434135606,0.0919607787700563,
0.378167715388157));
#17460=CARTESIAN_POINT('Ctrl Pts',(-0.0127288338612142,0.149946533709345,
0.386109883510937));
#17461=CARTESIAN_POINT('Ctrl Pts',(-0.132915182358376,0.070565859178174,
0.394052051633717));
#17462=CARTESIAN_POINT('Ctrl Pts',(-0.131337568919768,-0.0734603918663599,
0.401994219756497));
#17463=CARTESIAN_POINT('Ctrl Pts',(-0.00944124952954395,-0.150189377088511,
0.409936387879277));
#17464=CARTESIAN_POINT('Ctrl Pts',(0.121104224366159,-0.0893294633566384,
0.417878556002057));
#17465=CARTESIAN_POINT('Ctrl Pts',(0.140705787232781,0.0533654159743681,
0.425820724124838));
#17466=CARTESIAN_POINT('Ctrl Pts',(0.0314063937394313,0.147172091835368,
0.433762892247617));
#17467=CARTESIAN_POINT('Ctrl Pts',(-0.106664482920656,0.106154012011714,
0.441705060370398));
#17468=CARTESIAN_POINT('Ctrl Pts',(-0.147019735166745,-0.032112048430678,
0.449647228493177));
#17469=CARTESIAN_POINT('Ctrl Pts',(-0.052689806088835,-0.14096017351449,
0.457589396615958));
#17470=CARTESIAN_POINT('Ctrl Pts',(0.0899093983958942,-0.120674298270189,
0.465531564738737));
#17471=CARTESIAN_POINT('Ctrl Pts',(0.15014235720654,0.0101616315312987,
0.473473732861518));
#17472=CARTESIAN_POINT('Ctrl Pts',(0.0728294921055832,0.131688462906045,
0.481415900984297));
#17473=CARTESIAN_POINT('Ctrl Pts',(-0.071202669822089,0.132575133389036,
0.489358069107078));
#17474=CARTESIAN_POINT('Ctrl Pts',(-0.150005871264529,0.012009361726732,
0.497300237229857));
#17475=CARTESIAN_POINT('Ctrl Pts',(-0.0913882839399832,-0.119558219045865,
0.505242405352637));
#17476=CARTESIAN_POINT('Ctrl Pts',(0.0509503601487159,-0.141598188489932,
0.513184573475417));
#17477=CARTESIAN_POINT('Ctrl Pts',(0.146613240011817,-0.0339196703426114,
0.521126741598197));
#17478=CARTESIAN_POINT('Ctrl Pts',(0.107963329873666,0.104832750538675,
0.529068909720978));
#17479=CARTESIAN_POINT('Ctrl Pts',(-0.0295920819230583,0.147547602048875,
0.537011077843756));
#17480=CARTESIAN_POINT('Ctrl Pts',(-0.140038106568177,0.055093691941219,
0.544953245966537));
#17481=CARTESIAN_POINT('Ctrl Pts',(-0.122194838935542,-0.0878316999746162,
0.552895414089317));
#17482=CARTESIAN_POINT('Ctrl Pts',(0.00759145471482065,-0.150294231420327,
0.560837582212097));
#17483=CARTESIAN_POINT('Ctrl Pts',(0.130423195946632,-0.0750718065719766,
0.568779750334878));
#17484=CARTESIAN_POINT('Ctrl Pts',(0.133773890807325,0.0689241055160235,
0.576721918457657));
#17485=CARTESIAN_POINT('Ctrl Pts',(0.0145739585745413,0.149778456108953,
0.584664086580438));
#17486=CARTESIAN_POINT('Ctrl Pts',(-0.117977216952174,0.0934203535806499,
0.592606254703216));
#17487=CARTESIAN_POINT('Ctrl Pts',(-0.142449141490696,-0.0485203902651028,
0.600548422825998));
#17488=CARTESIAN_POINT('Ctrl Pts',(-0.036423018067407,-0.146011471938939,
0.608490590948776));
#17489=CARTESIAN_POINT('Ctrl Pts',(0.102970331784443,-0.109741044988262,
0.616432759071558));
#17490=CARTESIAN_POINT('Ctrl Pts',(0.148032279177632,0.0270634532975707,
0.624374927194337));
#17491=CARTESIAN_POINT('Ctrl Pts',(0.0574814509102497,0.139075048028633,
0.632317095317117));
#17492=CARTESIAN_POINT('Ctrl Pts',(-0.0857282916847416,0.123679611042927,
0.640259263439898));
#17493=CARTESIAN_POINT('Ctrl Pts',(-0.150402111894479,-0.00501905574730406,
0.648201431562677));
#17494=CARTESIAN_POINT('Ctrl Pts',(-0.0772921462128499,-0.129119751845818,
0.656143599685457));
#17495=CARTESIAN_POINT('Ctrl Pts',(0.0666253659236285,-0.134933490277457,
0.664085767808237));
#17496=CARTESIAN_POINT('Ctrl Pts',(0.14950719819016,-0.0171342893707992,
0.672027935931017));
#17497=CARTESIAN_POINT('Ctrl Pts',(0.0954250774564579,0.11636168087194,
0.679970104053797));
#17498=CARTESIAN_POINT('Ctrl Pts',(-0.0460762176180427,0.143258397146306,
0.687912272176577));
#17499=CARTESIAN_POINT('Ctrl Pts',(-0.145366963764729,0.0389157041403328,
0.695854440299358));
#17500=CARTESIAN_POINT('Ctrl Pts',(-0.111486636987321,-0.101077771820372,
0.703796608422136));
#17501=CARTESIAN_POINT('Ctrl Pts',(0.02452690272786,-0.148473624679578,
0.711738776544918));
#17502=CARTESIAN_POINT('Ctrl Pts',(0.138071279799868,-0.0598523840572839,
0.719680944667696));
#17503=CARTESIAN_POINT('Ctrl Pts',(0.125128179973684,0.0835997892305201,
0.727623112790477));
#17504=CARTESIAN_POINT('Ctrl Pts',(-0.00244518761474098,0.150465967050502,
0.735565280913257));
#17505=CARTESIAN_POINT('Ctrl Pts',(-0.127778512144395,0.0794898610961098,
0.743507449036036));
#17506=CARTESIAN_POINT('Ctrl Pts',(-0.136053592364468,-0.0643071239260258,
0.751449617158818));
#17507=CARTESIAN_POINT('Ctrl Pts',(-0.019689604662082,-0.149192176910068,
0.759391785281597));
#17508=CARTESIAN_POINT('Ctrl Pts',(0.114712083700712,-0.0974018687498071,
0.767333953404378));
#17509=CARTESIAN_POINT('Ctrl Pts',(0.144025718573537,0.0436185576594447,
0.775276121527157));
#17510=CARTESIAN_POINT('Ctrl Pts',(0.0413969989087525,0.14467990414796,
0.783218289649938));
#17511=CARTESIAN_POINT('Ctrl Pts',(-0.0991556246317344,0.113199594905656,
0.791160457772717));
#17512=CARTESIAN_POINT('Ctrl Pts',(-0.148871509365196,-0.021983172706469,
0.799102625895497));
#17513=CARTESIAN_POINT('Ctrl Pts',(-0.062205797368885,-0.137027095702329,
0.807044794018277));
#17514=CARTESIAN_POINT('Ctrl Pts',(0.081446815661698,-0.126540121706451,
0.814986962141057));
#17515=CARTESIAN_POINT('Ctrl Pts',(0.150485778196879,-0.000129396266831759,
0.822929130263837));
#17516=CARTESIAN_POINT('Ctrl Pts',(0.0816643079123276,0.126399869446589,
0.830871298386618));
#17517=CARTESIAN_POINT('Ctrl Pts',(-0.0619700581130299,0.137133869194964,
0.838813466509397));
#17518=CARTESIAN_POINT('Ctrl Pts',(-0.148833484480893,0.0222391564630926,
0.846755634632177));
#17519=CARTESIAN_POINT('Ctrl Pts',(-0.0993501488194509,-0.113028908304323,
0.854697802754957));
#17520=CARTESIAN_POINT('Ctrl Pts',(0.041148129789194,-0.144750881164039,
0.862639970877736));
#17521=CARTESIAN_POINT('Ctrl Pts',(0.143950494202948,-0.0438661760544617,
0.870582139000517));
#17522=CARTESIAN_POINT('Ctrl Pts',(0.114879417330645,0.0972044528644933,
0.878524307123298));
#17523=CARTESIAN_POINT('Ctrl Pts',(-0.0194330078274841,0.149225816766708,
0.886466475246077));
#17524=CARTESIAN_POINT('Ctrl Pts',(-0.135942801386891,0.0645410019599824,
0.894408643368857));
#17525=CARTESIAN_POINT('Ctrl Pts',(-0.127915022941288,-0.0792700011911429,
0.902350811491637));
#17526=CARTESIAN_POINT('Ctrl Pts',(-0.00270394227186439,-0.150461539534541,
0.910292979614417));
#17527=CARTESIAN_POINT('Ctrl Pts',(0.124984227305131,-0.0838148501630433,
0.918235147737197));
#17528=CARTESIAN_POINT('Ctrl Pts',(0.138174004553101,0.0596148525845174,
0.926177315859977));
#17529=CARTESIAN_POINT('Ctrl Pts',(0.0247821984756025,0.148431225898158,
0.934119483982757));
#17530=CARTESIAN_POINT('Ctrl Pts',(-0.11131264737753,0.101269347369872,
0.942061652105537));
#17531=CARTESIAN_POINT('Ctrl Pts',(-0.145433672650089,-0.0386656571445607,
0.950003820228317));
#17532=CARTESIAN_POINT('Ctrl Pts',(-0.0463225128062989,-0.143178947440692,
0.957945988351097));
#17533=CARTESIAN_POINT('Ctrl Pts',(0.0952248276606132,-0.116525612549003,
0.965888156473877));
#17534=CARTESIAN_POINT('Ctrl Pts',(0.149536443172165,0.0168771545685866,
0.973830324596656));
#17535=CARTESIAN_POINT('Ctrl Pts',(0.0668573142755158,0.134818714245386,
0.981772492719438));
#17536=CARTESIAN_POINT('Ctrl Pts',(-0.0770699830103684,0.129252481220654,
0.989714660842216));
#17537=CARTESIAN_POINT('Ctrl Pts',(-0.15039325815857,0.00527769678589187,
0.997656828964997));
#17538=CARTESIAN_POINT('Ctrl Pts',(-0.0859408583470751,-0.123532000103139,
1.00559899708778));
#17539=CARTESIAN_POINT('Ctrl Pts',(0.0572421967501742,-0.139173693973137,
1.01354116521056));
#17540=CARTESIAN_POINT('Ctrl Pts',(0.147985518909957,-0.0273179863069172,
1.02148333333334));
#17541=CARTESIAN_POINT('Ctrl Pts',(0.103158902618224,0.109563803299803,
1.02942550145612));
#17542=CARTESIAN_POINT('Ctrl Pts',(-0.0361718663885326,0.146073893166727,
1.0373676695789));
#17543=CARTESIAN_POINT('Ctrl Pts',(-0.142365489706367,0.0487652901517079,
1.04530983770168));
#17544=CARTESIAN_POINT('Ctrl Pts',(-0.118137698690712,-0.0932173284908804,
1.05325200582446));
#17545=CARTESIAN_POINT('Ctrl Pts',(0.0143163610725534,-0.149803297655807,
1.06119417394724));
#17546=CARTESIAN_POINT('Ctrl Pts',(0.133655163317704,-0.0691540562905145,
1.06913634207002));
#17547=CARTESIAN_POINT('Ctrl Pts',(0.130552105047211,0.0748474051030229,
1.0770785101928));
#17548=CARTESIAN_POINT('Ctrl Pts',(0.0078499064261323,0.150280954056111,
1.08502067831558));
#17549=CARTESIAN_POINT('Ctrl Pts',(-0.122043612932812,0.0880417101447944,
1.09296284643836));
#17550=CARTESIAN_POINT('Ctrl Pts',(-0.140132644828567,-0.0548527851276936,
1.10090501456114));
#17551=CARTESIAN_POINT('Ctrl Pts',(-0.0298457776877653,-0.147496493982489,
1.10884718268392));
#17552=CARTESIAN_POINT('Ctrl Pts',(0.107782887988268,-0.10501826145877,
1.1167893508067));
#17553=CARTESIAN_POINT('Ctrl Pts',(0.146671355310253,0.033667487497105,
1.12473151892948));
#17554=CARTESIAN_POINT('Ctrl Pts',(0.0511937930472066,0.141510359113225,
1.13267368705226));
#17555=CARTESIAN_POINT('Ctrl Pts',(-0.0911825429852659,0.119715203870077,
1.14061585517504));
#17556=CARTESIAN_POINT('Ctrl Pts',(-0.150026302104679,-0.0117513769282424,
1.14855802329782));
#17557=CARTESIAN_POINT('Ctrl Pts',(-0.0714305557085884,-0.132452489195471,
1.1565001914206));
#17558=CARTESIAN_POINT('Ctrl Pts',(0.0726029180563751,-0.131813513998426,
1.16444235954338));
#17559=CARTESIAN_POINT('Ctrl Pts',(0.150124660100533,-0.010419818262018,
1.17238452766616));
#17560=CARTESIAN_POINT('Ctrl Pts',(0.0901167906002831,0.120519501471002,
1.18032669578894));
#17561=CARTESIAN_POINT('Ctrl Pts',(-0.0524473171394798,0.141050576417769,
1.18826886391172));
#17562=CARTESIAN_POINT('Ctrl Pts',(-0.146964294261872,0.0323648326895764,
1.1962110320345));
#17563=CARTESIAN_POINT('Ctrl Pts',(-0.106846879624786,-0.105970422747861,
1.20415320015727));
#17564=CARTESIAN_POINT('Ctrl Pts',(0.0311532535456026,-0.14722588419309,
1.21209536828006));
#17565=CARTESIAN_POINT('Ctrl Pts',(0.140613805972886,-0.0536073106276968,
1.22003753640283));
#17566=CARTESIAN_POINT('Ctrl Pts',(0.121257666323848,0.0891210667609394,
1.22797970452562));
#17567=CARTESIAN_POINT('Ctrl Pts',(-0.00918295295119051,0.150205391241489,
1.2359218726484));
#17568=CARTESIAN_POINT('Ctrl Pts',(-0.131211043922368,0.0736861461587066,
1.24386404077118));
#17569=CARTESIAN_POINT('Ctrl Pts',(-0.133036338837895,-0.0703371788708997,
1.25180620889396));
#17570=CARTESIAN_POINT('Ctrl Pts',(-0.0129866800356469,-0.149924422041766,
1.25974837701674));
#17571=CARTESIAN_POINT('Ctrl Pts',(0.118960111851797,-0.0921654923014072,
1.26769054513952));
#17572=CARTESIAN_POINT('Ctrl Pts',(0.141927220045961,0.050026496908035,
1.2756327132623));
#17573=CARTESIAN_POINT('Ctrl Pts',(0.0348744139414821,0.146389075532006,
1.28357488138508));
#17574=CARTESIAN_POINT('Ctrl Pts',(-0.104126938119509,0.108644221848311,
1.29151704950786));
#17575=CARTESIAN_POINT('Ctrl Pts',(-0.147737317493493,-0.0286299004949125,
1.29945921763064));
#17576=CARTESIAN_POINT('Ctrl Pts',(-0.0560051364173496,-0.139676092720537,
1.30740138575342));
#17577=CARTESIAN_POINT('Ctrl Pts',(0.0870335032532438,-0.122764634549313,
1.3153435538762));
#17578=CARTESIAN_POINT('Ctrl Pts',(0.150340512633584,0.00661184096937889,
1.32328572199898));
#17579=CARTESIAN_POINT('Ctrl Pts',(0.0759201674095095,0.129931190880528,
1.33122789012176));
#17580=CARTESIAN_POINT('Ctrl Pts',(-0.0680508508044829,0.134220221643466,
1.33917005824454));
#17581=CARTESIAN_POINT('Ctrl Pts',(-0.149680298423566,0.0155497403439283,
1.34711222636732));
#17582=CARTESIAN_POINT('Ctrl Pts',(-0.0941872156892785,-0.117365900463673,
1.3550543944901));
#17583=CARTESIAN_POINT('Ctrl Pts',(0.0475910332998192,-0.142762319241037,
1.36299656261288));
#17584=CARTESIAN_POINT('Ctrl Pts',(0.145771005694385,-0.0373737865856905,
1.37093873073566));
#17585=CARTESIAN_POINT('Ctrl Pts',(0.110409762917901,0.10225297323032,1.37888089885844));
#17586=CARTESIAN_POINT('Ctrl Pts',(-0.0260981686868614,0.148205506441964,
1.38682306698121));
#17587=CARTESIAN_POINT('Ctrl Pts',(-0.138697490589939,0.0583865667538053,
1.394765235104));
#17588=CARTESIAN_POINT('Ctrl Pts',(-0.124235673603468,-0.0849204601545819,
1.40270740322677));
#17589=CARTESIAN_POINT('Ctrl Pts',(0.0040388053119065,-0.150431633134115,
1.41064957134956));
#17590=CARTESIAN_POINT('Ctrl Pts',(0.12861328245382,-0.0781319533624403,
1.41859173947234));
#17591=CARTESIAN_POINT('Ctrl Pts',(0.1353648581188,0.0657445800149866,1.42653390759512));
#17592=CARTESIAN_POINT('Ctrl Pts',(0.0181081687242482,0.149392404544468,
1.43447607571789));
#17593=CARTESIAN_POINT('Ctrl Pts',(-0.115737181672069,0.0961812857364522,
1.44241824384068));
#17594=CARTESIAN_POINT('Ctrl Pts',(-0.143555918690644,-0.0451414811888502,
1.45036041196346));
#17595=CARTESIAN_POINT('Ctrl Pts',(-0.0398616700558823,-0.145110565703753,
1.45830258008624));
#17596=CARTESIAN_POINT('Ctrl Pts',(0.100348034367198,-0.112142416378873,
1.46624474820902));
#17597=CARTESIAN_POINT('Ctrl Pts',(0.14863229283285,0.0235577176564554,
1.4741869163318));
#17598=CARTESIAN_POINT('Ctrl Pts',(0.0607471474677608,0.137680339497592,
1.48212908445458));
#17599=CARTESIAN_POINT('Ctrl Pts',(-0.0827754224726193,0.125666453945577,
1.49007125257736));
#17600=CARTESIAN_POINT('Ctrl Pts',(-0.150492272191201,-0.00145719475437189,
1.49801342070014));
#17601=CARTESIAN_POINT('Ctrl Pts',(-0.0802951178786721,-0.12727177793954,
1.50595558882292));
#17602=CARTESIAN_POINT('Ctrl Pts',(0.0633700050447994,-0.136443062004882,
1.5138977569457));
#17603=CARTESIAN_POINT('Ctrl Pts',(0.149155357006591,-0.0207133070603065,
1.52183992506848));
#17604=CARTESIAN_POINT('Ctrl Pts',(0.0979555318420461,0.114182655252422,
1.52978209319126));
#17605=CARTESIAN_POINT('Ctrl Pts',(0.00450803278943675,0.134083974545181,
1.53507687193978));
#17606=CARTESIAN_POINT('Ctrl Pts',(-0.0361033354337414,0.122073089461022,
1.53772426131404));
#17607=CARTESIAN_POINT('Ctrl Pts',(-0.0592743564846203,0.123319225136773,
-0.00549926131403157));
#17608=CARTESIAN_POINT('Ctrl Pts',(-0.100300290071938,0.10359978715075,
-0.00285187193977157));
#17609=CARTESIAN_POINT('Ctrl Pts',(-0.160414584165772,0.0203416160441626,
0.00244290680874841));
#17610=CARTESIAN_POINT('Ctrl Pts',(-0.103922107946056,-0.124084444561314,
0.0103850749315284));
#17611=CARTESIAN_POINT('Ctrl Pts',(0.0479099321398382,-0.154436663180837,
0.0183272430543084));
#17612=CARTESIAN_POINT('Ctrl Pts',(0.155781551077148,-0.0435098515708298,
0.0262694111770884));
#17613=CARTESIAN_POINT('Ctrl Pts',(0.120977930992648,0.107381072623318,
0.0342115792998684));
#17614=CARTESIAN_POINT('Ctrl Pts',(-0.0246731903087699,0.159844935900913,
0.0421537474226484));
#17615=CARTESIAN_POINT('Ctrl Pts',(-0.147710978397823,0.0659033513787588,
0.0500959155454284));
#17616=CARTESIAN_POINT('Ctrl Pts',(-0.135435684249567,-0.0884277117007276,
0.0580380836682085));
#17617=CARTESIAN_POINT('Ctrl Pts',(0.000915427738408385,-0.16174188059703,
0.0659802517909884));
#17618=CARTESIAN_POINT('Ctrl Pts',(0.13642643003965,-0.0868880976295618,
0.0739224199137684));
#17619=CARTESIAN_POINT('Ctrl Pts',(0.146957588340267,0.0675663355536457,
0.0818645880365484));
#17620=CARTESIAN_POINT('Ctrl Pts',(0.0228600865593111,0.160121891352391,
0.0898067561593285));
#17621=CARTESIAN_POINT('Ctrl Pts',(-0.122179386207322,0.105989962368389,
0.0977489242821083));
#17622=CARTESIAN_POINT('Ctrl Pts',(-0.155290103436038,-0.0452399862206161,
0.105691092404888));
#17623=CARTESIAN_POINT('Ctrl Pts',(-0.0461390722131997,-0.155025288408554,
0.113633260527668));
#17624=CARTESIAN_POINT('Ctrl Pts',(0.105280057525145,-0.122791590307548,
0.121575428650448));
#17625=CARTESIAN_POINT('Ctrl Pts',(0.160251855424436,0.0219318669073289,
0.129517596773229));
#17626=CARTESIAN_POINT('Ctrl Pts',(0.0684164816681947,0.146563455853242,
0.137459764896008));
#17627=CARTESIAN_POINT('Ctrl Pts',(-0.086095413359615,0.136927875387926,
0.145401933018789));
#17628=CARTESIAN_POINT('Ctrl Pts',(-0.16173506727009,0.00185228698694943,
0.153344101141568));
#17629=CARTESIAN_POINT('Ctrl Pts',(-0.0892087826023274,-0.134920182928699,
0.161286269264348));
#17630=CARTESIAN_POINT('Ctrl Pts',(0.0650419110192955,-0.148091906331324,
0.169228437387128));
#17631=CARTESIAN_POINT('Ctrl Pts',(0.159707532494063,-0.025596228460074,
0.177170605509908));
#17632=CARTESIAN_POINT('Ctrl Pts',(0.108064646638443,0.120348223746572,
0.185112773632688));
#17633=CARTESIAN_POINT('Ctrl Pts',(-0.0425765573421325,0.156041339440091,
0.193054941755468));
#17634=CARTESIAN_POINT('Ctrl Pts',(-0.154213260793436,0.0487845573223287,
0.200997109878248));
#17635=CARTESIAN_POINT('Ctrl Pts',(-0.124574774400312,-0.103163891052585,
0.208939278001028));
#17636=CARTESIAN_POINT('Ctrl Pts',(0.0191870033818907,-0.160603616835255,
0.216881446123808));
#17637=CARTESIAN_POINT('Ctrl Pts',(0.145371514918136,-0.0709139301387177,
0.224823614246588));
#17638=CARTESIAN_POINT('Ctrl Pts',(0.138380784202201,0.0837402018183176,
0.232765782369368));
#17639=CARTESIAN_POINT('Ctrl Pts',(0.00461903876105218,0.161679705957985,
0.240707950492149));
#17640=CARTESIAN_POINT('Ctrl Pts',(-0.133374220718213,0.0915039894496894,
0.248650118614928));
#17641=CARTESIAN_POINT('Ctrl Pts',(-0.149182991964712,-0.0624987819548612,
0.256592286737709));
#17642=CARTESIAN_POINT('Ctrl Pts',(-0.0283248164207669,-0.159246248345813,
0.264534454860488));
#17643=CARTESIAN_POINT('Ctrl Pts',(0.118481800883715,-0.110107791262854,
0.272476622983269));
#17644=CARTESIAN_POINT('Ctrl Pts',(0.156746916480749,0.0399007144198201,
0.280418791106048));
#17645=CARTESIAN_POINT('Ctrl Pts',(0.0514157533588968,0.153356066537929,
0.288360959228829));
#17646=CARTESIAN_POINT('Ctrl Pts',(-0.101017521980764,0.126321506839912,
0.296303127351608));
#17647=CARTESIAN_POINT('Ctrl Pts',(-0.160908369261695,-0.0164365306249019,
0.304245295474388));
#17648=CARTESIAN_POINT('Ctrl Pts',(-0.0733906195540655,-0.144137017448375,
0.312187463597168));
#17649=CARTESIAN_POINT('Ctrl Pts',(0.0813604773699057,-0.13979318853071,
0.320129631719948));
#17650=CARTESIAN_POINT('Ctrl Pts',(0.161577018543625,-0.00738443741900211,
0.328071799842729));
#17651=CARTESIAN_POINT('Ctrl Pts',(0.0937724112935796,0.131789217000595,
0.336013967965508));
#17652=CARTESIAN_POINT('Ctrl Pts',(-0.0599373583072218,0.150230409426965,
0.343956136088289));
#17653=CARTESIAN_POINT('Ctrl Pts',(-0.158738350099833,0.0310451130618767,
0.351898304211068));
#17654=CARTESIAN_POINT('Ctrl Pts',(-0.112118705390683,-0.116580696253536,
0.359840472333849));
#17655=CARTESIAN_POINT('Ctrl Pts',(0.0372131918485748,-0.15740661101073,
0.367782640456628));
#17656=CARTESIAN_POINT('Ctrl Pts',(0.152453982298084,-0.0540318990865351,
0.375724808579408));
#17657=CARTESIAN_POINT('Ctrl Pts',(0.128031262769868,0.0988415833088236,
0.383666976702188));
#17658=CARTESIAN_POINT('Ctrl Pts',(-0.0136812466069205,0.161166021011634,
0.391609144824968));
#17659=CARTESIAN_POINT('Ctrl Pts',(-0.142860328563903,0.0758458262533652,
0.399551312947749));
#17660=CARTESIAN_POINT('Ctrl Pts',(-0.141164672957165,-0.0789569372907697,
0.407493481070528));
#17661=CARTESIAN_POINT('Ctrl Pts',(-0.0101476745237983,-0.161427034722196,
0.415435649193308));
#17662=CARTESIAN_POINT('Ctrl Pts',(0.130165636283581,-0.0960133843187101,
0.423377817316089));
#17663=CARTESIAN_POINT('Ctrl Pts',(0.151233851831306,0.0573583899504574,
0.431319985438868));
#17664=CARTESIAN_POINT('Ctrl Pts',(0.0337563222576384,0.158183986373718,
0.439262153561649));
#17665=CARTESIAN_POINT('Ctrl Pts',(-0.114645466422773,0.114096800420287,
0.447204321684428));
#17666=CARTESIAN_POINT('Ctrl Pts',(-0.158020229883659,-0.0345147763277912,
0.455146489807208));
#17667=CARTESIAN_POINT('Ctrl Pts',(-0.0566322287360923,-0.151507272121918,
0.463088657929988));
#17668=CARTESIAN_POINT('Ctrl Pts',(0.0966367119836487,-0.129703541718919,
0.471030826052768));
#17669=CARTESIAN_POINT('Ctrl Pts',(0.161376496659739,0.0109219578497271,
0.478972994175549));
#17670=CARTESIAN_POINT('Ctrl Pts',(0.0782788315581001,0.141541821972661,
0.486915162298328));
#17671=CARTESIAN_POINT('Ctrl Pts',(-0.0765302851406724,0.142494836024782,
0.494857330421108));
#17672=CARTESIAN_POINT('Ctrl Pts',(-0.161229798395673,0.0129079412274925,
0.502799498543889));
#17673=CARTESIAN_POINT('Ctrl Pts',(-0.0982262525537151,-0.128503953817366,
0.510741666666668));
#17674=CARTESIAN_POINT('Ctrl Pts',(0.0547626317937811,-0.152193025452748,
0.518683834789449));
#17675=CARTESIAN_POINT('Ctrl Pts',(0.157583319439253,-0.0364576503898468,
0.526626002912228));
#17676=CARTESIAN_POINT('Ctrl Pts',(0.116041497328862,0.112676677866884,
0.534568171035008));
#17677=CARTESIAN_POINT('Ctrl Pts',(-0.0318062577307366,0.158587593482618,
0.542510339157789));
#17678=CARTESIAN_POINT('Ctrl Pts',(-0.150516213127973,0.0592159811457737,
0.550452507280567));
#17679=CARTESIAN_POINT('Ctrl Pts',(-0.131337854181896,-0.0944035534094825,
0.558394675403349));
#17680=CARTESIAN_POINT('Ctrl Pts',(0.00815947204521347,-0.161539734596121,
0.566336843526128));
#17681=CARTESIAN_POINT('Ctrl Pts',(0.140181883624494,-0.080688923285235,
0.574279011648909));
#17682=CARTESIAN_POINT('Ctrl Pts',(0.143783288371658,0.0740812312429708,
0.582221179771688));
#17683=CARTESIAN_POINT('Ctrl Pts',(0.0156644295519346,0.160985367298567,
0.590163347894469));
#17684=CARTESIAN_POINT('Ctrl Pts',(-0.126804656005353,0.100410368253513,
0.598105516017247));
#17685=CARTESIAN_POINT('Ctrl Pts',(-0.153107649524464,-0.0521508436608248,
0.606047684140029));
#17686=CARTESIAN_POINT('Ctrl Pts',(-0.0391483067326994,-0.156936525122116,
0.613989852262808));
#17687=CARTESIAN_POINT('Ctrl Pts',(0.110674906884577,-0.117952226869747,
0.621932020385589));
#17688=CARTESIAN_POINT('Ctrl Pts',(0.159108535730396,0.0290884288879846,
0.629874188508368));
#17689=CARTESIAN_POINT('Ctrl Pts',(0.061782400006242,0.14948109541648,0.637816356631148));
#17690=CARTESIAN_POINT('Ctrl Pts',(-0.0921427612707386,0.132933721767072,
0.645758524753929));
#17691=CARTESIAN_POINT('Ctrl Pts',(-0.161655687038194,-0.0053945978210935,
0.653700692876707));
#17692=CARTESIAN_POINT('Ctrl Pts',(-0.0830753959589387,-0.138780911597048,
0.661642860999489));
#17693=CARTESIAN_POINT('Ctrl Pts',(0.0716104924784035,-0.145029652845349,
0.669585029122267));
#17694=CARTESIAN_POINT('Ctrl Pts',(0.160693812980115,-0.0184163326249747,
0.677527197245049));
#17695=CARTESIAN_POINT('Ctrl Pts',(0.102565092089392,0.125068240261613,
0.685469365367828));
#17696=CARTESIAN_POINT('Ctrl Pts',(-0.0495237900674707,0.153977456320057,
0.693411533490608));
#17697=CARTESIAN_POINT('Ctrl Pts',(-0.156243792750268,0.0418275036842162,
0.701353701613389));
#17698=CARTESIAN_POINT('Ctrl Pts',(-0.119828429739121,-0.108640739429086,
0.709295869736167));
#17699=CARTESIAN_POINT('Ctrl Pts',(0.0263620853553792,-0.159582904138124,
0.717238037858949));
#17700=CARTESIAN_POINT('Ctrl Pts',(0.148402221984423,-0.0643307340819919,
0.725180205981728));
#17701=CARTESIAN_POINT('Ctrl Pts',(0.134490677336207,0.0898549973406614,
0.733122374104509));
#17702=CARTESIAN_POINT('Ctrl Pts',(-0.00262814450422035,0.161724320044658,
0.741064542227287));
#17703=CARTESIAN_POINT('Ctrl Pts',(-0.137339315979238,0.0854375510170853,
0.749006710350069));
#17704=CARTESIAN_POINT('Ctrl Pts',(-0.146233564613262,-0.0691187920752458,
0.756948878472847));
#17705=CARTESIAN_POINT('Ctrl Pts',(-0.0211628449166461,-0.160355220783347,
0.764891046595629));
#17706=CARTESIAN_POINT('Ctrl Pts',(0.12329521486528,-0.104689793336152,
0.772833214718408));
#17707=CARTESIAN_POINT('Ctrl Pts',(0.154802191231926,0.0468822399980663,
0.780775382841188));
#17708=CARTESIAN_POINT('Ctrl Pts',(0.0444944569967772,0.155505325098544,
0.788717550963968));
#17709=CARTESIAN_POINT('Ctrl Pts',(-0.106574770936664,0.121669556739719,
0.796659719086747));
#17710=CARTESIAN_POINT('Ctrl Pts',(-0.160010559849905,-0.0236280251811701,
0.804601887209529));
#17711=CARTESIAN_POINT('Ctrl Pts',(-0.0668602374312443,-0.147279908636853,
0.812544055332307));
#17712=CARTESIAN_POINT('Ctrl Pts',(0.0875409312876049,-0.13600826514128,
0.820486223455089));
#17713=CARTESIAN_POINT('Ctrl Pts',(0.161745613525436,-0.000139078116330951,
0.828428391577867));
#17714=CARTESIAN_POINT('Ctrl Pts',(0.0877746970157421,0.135857518751215,
0.836370559700649));
#17715=CARTESIAN_POINT('Ctrl Pts',(-0.0666068593976089,0.147394671269449,
0.844312727823428));
#17716=CARTESIAN_POINT('Ctrl Pts',(-0.159969689820096,0.0239031624749592,
0.852254895946208));
#17717=CARTESIAN_POINT('Ctrl Pts',(-0.106783850056725,-0.121486098811777,
0.860197064068988));
#17718=CARTESIAN_POINT('Ctrl Pts',(0.0442269666803361,-0.155581612845794,
0.868139232191768));
#17719=CARTESIAN_POINT('Ctrl Pts',(0.154721338329289,-0.0471483860066884,
0.876081400314548));
#17720=CARTESIAN_POINT('Ctrl Pts',(0.123475068941597,0.104477606152275,
0.884023568437328));
#17721=CARTESIAN_POINT('Ctrl Pts',(-0.0208870486723946,0.160391377683462,
0.891965736560109));
#17722=CARTESIAN_POINT('Ctrl Pts',(-0.146114483894434,0.0693701696243073,
0.899907904682887));
#17723=CARTESIAN_POINT('Ctrl Pts',(-0.137486040957907,-0.0852012404790134,
0.907850072805669));
#17724=CARTESIAN_POINT('Ctrl Pts',(-0.00290626002629624,-0.161719561247554,
0.915792240928448));
#17725=CARTESIAN_POINT('Ctrl Pts',(0.134335953660838,-0.0900861498315643,
0.923734409051229));
#17726=CARTESIAN_POINT('Ctrl Pts',(0.148512632937768,0.0640754297319473,
0.931676577174007));
#17727=CARTESIAN_POINT('Ctrl Pts',(0.0266364831612253,0.159537332941991,
0.939618745296788));
#17728=CARTESIAN_POINT('Ctrl Pts',(-0.119641421660886,0.10884664928423,
0.947560913419568));
#17729=CARTESIAN_POINT('Ctrl Pts',(-0.156315493011378,-0.0415587473590326,
0.955503081542348));
#17730=CARTESIAN_POINT('Ctrl Pts',(-0.0497885138626987,-0.153892061929087,
0.963445249665127));
#17731=CARTESIAN_POINT('Ctrl Pts',(0.102349858952582,-0.125244437839883,
0.971387417787908));
#17732=CARTESIAN_POINT('Ctrl Pts',(0.160725246166783,0.018139958160622,
0.979329585910688));
#17733=CARTESIAN_POINT('Ctrl Pts',(0.0718597959603077,0.14490628889729,
0.987271754033468));
#17734=CARTESIAN_POINT('Ctrl Pts',(-0.0828366097831417,0.138923572215364,
0.995213922156248));
#17735=CARTESIAN_POINT('Ctrl Pts',(-0.161646170836971,0.00567259122332548,
1.00315609027903));
#17736=CARTESIAN_POINT('Ctrl Pts',(-0.0923712328620446,-0.132775066096718,
1.01109825840181));
#17737=CARTESIAN_POINT('Ctrl Pts',(0.0615252440718216,-0.149587122371362,
1.01904042652459));
#17738=CARTESIAN_POINT('Ctrl Pts',(0.159058276707423,-0.0293620068848675,
1.02698259464737));
#17739=CARTESIAN_POINT('Ctrl Pts',(0.1108775872014,0.117761723381742,1.03492476277015));
#17740=CARTESIAN_POINT('Ctrl Pts',(-0.0388783630684312,0.157003616909169,
1.04286693089293));
#17741=CARTESIAN_POINT('Ctrl Pts',(-0.153017738641585,0.0524140677533946,
1.05080909901571));
#17742=CARTESIAN_POINT('Ctrl Pts',(-0.126977145509477,-0.10019215216626,
1.05875126713849));
#17743=CARTESIAN_POINT('Ctrl Pts',(0.0153875577671049,-0.161012067570745,
1.06669343526127));
#17744=CARTESIAN_POINT('Ctrl Pts',(0.143655677305146,-0.0743283876822416,
1.07463560338405));
#17745=CARTESIAN_POINT('Ctrl Pts',(0.140320438123209,0.080447731368589,
1.08257777150683));
#17746=CARTESIAN_POINT('Ctrl Pts',(0.00843726195408678,0.161525463776335,
1.09051993962961));
#17747=CARTESIAN_POINT('Ctrl Pts',(-0.131175312957834,0.094629277223576,
1.09846210775239));
#17748=CARTESIAN_POINT('Ctrl Pts',(-0.150617825048456,-0.0589570489009974,
1.10640427587517));
#17749=CARTESIAN_POINT('Ctrl Pts',(-0.0320789358376135,-0.158532661344495,
1.11434644399795));
#17750=CARTESIAN_POINT('Ctrl Pts',(0.115847554194776,-0.112876069317329,
1.12228861212073));
#17751=CARTESIAN_POINT('Ctrl Pts',(0.157645783113317,0.0361865984037055,
1.13023078024351));
#17752=CARTESIAN_POINT('Ctrl Pts',(0.0550242791334153,0.152098624396442,
1.13817294836629));
#17753=CARTESIAN_POINT('Ctrl Pts',(-0.0980051173916675,0.128672684756662,
1.14611511648907));
#17754=CARTESIAN_POINT('Ctrl Pts',(-0.161251757937727,-0.0126306531673768,
1.15405728461185));
#17755=CARTESIAN_POINT('Ctrl Pts',(-0.0767752221903169,-0.142363015193798,
1.16199945273463));
#17756=CARTESIAN_POINT('Ctrl Pts',(0.0780353045016797,-0.141676229794458,
1.16994162085741));
#17757=CARTESIAN_POINT('Ctrl Pts',(0.161357475398708,-0.0111994629512984,
1.17788378898019));
#17758=CARTESIAN_POINT('Ctrl Pts',(0.0968596219472387,0.129537162519796,
1.18582595710297));
#17759=CARTESIAN_POINT('Ctrl Pts',(-0.0563715959749383,0.151604439264423,
1.19376812522575));
#17760=CARTESIAN_POINT('Ctrl Pts',(-0.157960640709981,0.0347864747270306,
1.20171029334853));
#17761=CARTESIAN_POINT('Ctrl Pts',(-0.114841510641486,-0.113899474410655,
1.20965246147131));
#17762=CARTESIAN_POINT('Ctrl Pts',(0.03348424129126,-0.158241803650584,
1.21759462959409));
#17763=CARTESIAN_POINT('Ctrl Pts',(0.151134988234409,-0.0576183839484237,
1.22553679771687));
#17764=CARTESIAN_POINT('Ctrl Pts',(0.130330559267559,0.0957893948119858,
1.23347896583965));
#17765=CARTESIAN_POINT('Ctrl Pts',(-0.0098700513554357,0.16144424710618,
1.24142113396243));
#17766=CARTESIAN_POINT('Ctrl Pts',(-0.141028680947982,0.0791995832534545,
1.24936330208521));
#17767=CARTESIAN_POINT('Ctrl Pts',(-0.142990550365238,-0.0756000353418,
1.25730547020799));
#17768=CARTESIAN_POINT('Ctrl Pts',(-0.013958385670676,-0.161142254877177,
1.26524763833077));
#17769=CARTESIAN_POINT('Ctrl Pts',(0.127861094297897,-0.0990616141723472,
1.27318980645355));
#17770=CARTESIAN_POINT('Ctrl Pts',(0.152546676219863,0.0537696421008814,
1.28113197457633));
#17771=CARTESIAN_POINT('Ctrl Pts',(0.0374838310097642,0.157342382244044,
1.28907414269911));
#17772=CARTESIAN_POINT('Ctrl Pts',(-0.111918054267102,0.116773335855419,
1.29701631082189));
#17773=CARTESIAN_POINT('Ctrl Pts',(-0.158791504053787,-0.0307720827589687,
1.30495847894467));
#17774=CARTESIAN_POINT('Ctrl Pts',(-0.060195622861772,-0.150127112226926,
1.31290064706745));
#17775=CARTESIAN_POINT('Ctrl Pts',(0.0935456330135535,-0.131950283756556,
1.32084281519023));
#17776=CARTESIAN_POINT('Ctrl Pts',(0.161589478720268,0.00710656041347678,
1.32878498331301));
#17777=CARTESIAN_POINT('Ctrl Pts',(0.0816007612396376,0.139653065139265,
1.33672715143579));
#17778=CARTESIAN_POINT('Ctrl Pts',(-0.0731426367739486,0.144263015132499,
1.34466931955857));
#17779=CARTESIAN_POINT('Ctrl Pts',(-0.160879865135934,0.0167132224867059,
1.35261148768135));
#17780=CARTESIAN_POINT('Ctrl Pts',(-0.101234609479067,-0.126147598829082,
1.36055365580413));
#17781=CARTESIAN_POINT('Ctrl Pts',(0.051151949184981,-0.153444260252591,
1.36849582392691));
#17782=CARTESIAN_POINT('Ctrl Pts',(0.15667806641111,-0.0401702148435725,
1.37643799204969));
#17783=CARTESIAN_POINT('Ctrl Pts',(0.118670980449659,0.10990387323047,1.38438016017247));
#17784=CARTESIAN_POINT('Ctrl Pts',(-0.0280509185434417,0.159294724422008,
1.39232232829525));
#17785=CARTESIAN_POINT('Ctrl Pts',(-0.149075287902345,0.0627552395607943,
1.40026449641803));
#17786=CARTESIAN_POINT('Ctrl Pts',(-0.133531390736797,-0.0912744851582948,
1.40820666454081));
#17787=CARTESIAN_POINT('Ctrl Pts',(0.00434100186018791,-0.161687417152987,
1.41614883266359));
#17788=CARTESIAN_POINT('Ctrl Pts',(0.138236546518021,-0.0839780402106489,
1.42409100078637));
#17789=CARTESIAN_POINT('Ctrl Pts',(0.145493297031458,0.07066380330362,1.43203316890915));
#17790=CARTESIAN_POINT('Ctrl Pts',(0.0194630807988606,0.160570430100525,
1.43997533703193));
#17791=CARTESIAN_POINT('Ctrl Pts',(-0.124397014000637,0.103377882332206,
1.44791750515471));
#17792=CARTESIAN_POINT('Ctrl Pts',(-0.15429723939393,-0.0485191136187331,
1.45585967327749));
#17793=CARTESIAN_POINT('Ctrl Pts',(-0.042844249846,-0.155968210152522,1.46380184140027));
#17794=CARTESIAN_POINT('Ctrl Pts',(0.107856400646442,-0.120533276677448,
1.47174400952305));
#17795=CARTESIAN_POINT('Ctrl Pts',(0.159753444358638,0.0253203827049868,
1.47968617764583));
#17796=CARTESIAN_POINT('Ctrl Pts',(0.0652924466007548,0.147982030257331,
1.48762834576861));
#17797=CARTESIAN_POINT('Ctrl Pts',(-0.0889689487809616,0.13506922671723,
1.49557051389139));
#17798=CARTESIAN_POINT('Ctrl Pts',(-0.161752593421533,-0.00156622680492735,
1.50351268201417));
#17799=CARTESIAN_POINT('Ctrl Pts',(-0.086303059730943,-0.136794666273195,
1.51145485013695));
#17800=CARTESIAN_POINT('Ctrl Pts',(0.0681115549116652,-0.14665217563879,
1.51939701825973));
#17801=CARTESIAN_POINT('Ctrl Pts',(0.160315645894948,-0.02226314405755,
1.52733918638251));
#17802=CARTESIAN_POINT('Ctrl Pts',(0.105284883301553,0.122726172858702,
1.53528135450529));
#17803=CARTESIAN_POINT('Ctrl Pts',(0.00484533846358528,0.144116573583224,
1.54057613325381));
#17804=CARTESIAN_POINT('Ctrl Pts',(-0.0388047044047284,0.131206995015745,
1.54322352262807));
#17805=CARTESIAN_POINT('Ctrl Pts',(-0.0634007094575145,0.131904027763688,
-3.88578058618805E-16));
#17806=CARTESIAN_POINT('Ctrl Pts',(-0.107282641710421,0.110811831533068,
0.00264738937425961));
#17807=CARTESIAN_POINT('Ctrl Pts',(-0.171581760589518,0.0217576868851663,
0.0079421681227796));
#17808=CARTESIAN_POINT('Ctrl Pts',(-0.111156590520044,-0.1327225175337,
0.0158843362455596));
#17809=CARTESIAN_POINT('Ctrl Pts',(0.0512451567233008,-0.165187689797298,
0.0238265043683396));
#17810=CARTESIAN_POINT('Ctrl Pts',(0.16662620135312,-0.0465387668729445,
0.0317686724911196));
#17811=CARTESIAN_POINT('Ctrl Pts',(0.129399745666171,0.114856349193662,
0.0397108406138996));
#17812=CARTESIAN_POINT('Ctrl Pts',(-0.026390801400978,0.170972456562021,
0.0476530087366796));
#17813=CARTESIAN_POINT('Ctrl Pts',(-0.157993800025737,0.070491178324729,
0.0555951768594596));
#17814=CARTESIAN_POINT('Ctrl Pts',(-0.144863967768493,-0.0945835600760224,
0.0635373449822396));
#17815=CARTESIAN_POINT('Ctrl Pts',(0.000979154756195248,-0.17300145605975,
0.0714795131050195));
#17816=CARTESIAN_POINT('Ctrl Pts',(0.145923683802689,-0.0929367665856833,
0.0794216812277997));
#17817=CARTESIAN_POINT('Ctrl Pts',(0.157187963117837,0.0722699302633024,
0.0873638493505794));
#17818=CARTESIAN_POINT('Ctrl Pts',(0.0244514793930555,0.171268692120756,
0.0953060174733598));
#17819=CARTESIAN_POINT('Ctrl Pts',(-0.130684839550095,0.113368397534175,
0.103248185596139));
#17820=CARTESIAN_POINT('Ctrl Pts',(-0.166100541844429,-0.0483893439312075,
0.11119035371892));
#17821=CARTESIAN_POINT('Ctrl Pts',(-0.0493510193195793,-0.165817291858885,
0.119132521841699));
#17822=CARTESIAN_POINT('Ctrl Pts',(0.112609073040783,-0.131339661914923,
0.12707468996448));
#17823=CARTESIAN_POINT('Ctrl Pts',(0.17140770357293,0.0234586422209967,
0.135016858087259));
#17824=CARTESIAN_POINT('Ctrl Pts',(0.0731792588499177,0.156766393306209,
0.14295902621004));
#17825=CARTESIAN_POINT('Ctrl Pts',(-0.0920889000195865,0.146460037003638,
0.150901194332819));
#17826=CARTESIAN_POINT('Ctrl Pts',(-0.172994168426659,0.00198123296575728,
0.1588433624556));
#17827=CARTESIAN_POINT('Ctrl Pts',(-0.0954190048152776,-0.144312580095855,
0.16678553057838));
#17828=CARTESIAN_POINT('Ctrl Pts',(0.0695697692503139,-0.158401246055831,
0.17472769870116));
#17829=CARTESIAN_POINT('Ctrl Pts',(0.170825487889685,-0.0273780963649298,
0.18266986682394));
#17830=CARTESIAN_POINT('Ctrl Pts',(0.115587509852263,0.128726201683253,
0.19061203494672));
#17831=CARTESIAN_POINT('Ctrl Pts',(-0.0455405018601966,0.16690407474553,
0.198554203069499));
#17832=CARTESIAN_POINT('Ctrl Pts',(-0.164948735370872,0.0521806684752238,
0.20649637119228));
#17833=CARTESIAN_POINT('Ctrl Pts',(-0.133246981425072,-0.110345590758605,
0.214438539315059));
#17834=CARTESIAN_POINT('Ctrl Pts',(0.0205226964731592,-0.171783952668295,
0.22238070743784));
#17835=CARTESIAN_POINT('Ctrl Pts',(0.155491476033395,-0.0758505658746651,
0.230322875560619));
#17836=CARTESIAN_POINT('Ctrl Pts',(0.148014089296488,0.0895697316726553,
0.2382650436834));
#17837=CARTESIAN_POINT('Ctrl Pts',(0.00494059070111224,0.172934953166096,
0.24620721180618));
#17838=CARTESIAN_POINT('Ctrl Pts',(-0.142658996543838,0.0978739912732451,
0.25414937992896));
#17839=CARTESIAN_POINT('Ctrl Pts',(-0.159568287038446,-0.0668496016012732,
0.262091548051739));
#17840=CARTESIAN_POINT('Ctrl Pts',(-0.0302966335331915,-0.170332091689456,
0.27003371617452));
#17841=CARTESIAN_POINT('Ctrl Pts',(0.126729848780061,-0.11777288690896,
0.2779758842973));
#17842=CARTESIAN_POINT('Ctrl Pts',(0.167658770158652,0.0426783815482623,
0.28591805242008));
#17843=CARTESIAN_POINT('Ctrl Pts',(0.0549950338320791,0.164031867990689,
0.293860220542859));
#17844=CARTESIAN_POINT('Ctrl Pts',(-0.108049803339193,0.135115311719503,
0.30180238866564));
#17845=CARTESIAN_POINT('Ctrl Pts',(-0.1721099202737,-0.0175807510100837,
0.309744556788419));
#17846=CARTESIAN_POINT('Ctrl Pts',(-0.0784996687135917,-0.154171039675278,
0.3176867249112));
#17847=CARTESIAN_POINT('Ctrl Pts',(0.087024343965547,-0.14952481740522,
0.325628893033979));
#17848=CARTESIAN_POINT('Ctrl Pts',(0.172825117221703,-0.00789850112384905,
0.33357106115676));
#17849=CARTESIAN_POINT('Ctrl Pts',(0.100300328103893,0.140963653630822,
0.341513229279539));
#17850=CARTESIAN_POINT('Ctrl Pts',(-0.0641098658012952,0.160688619913292,
0.349455397402319));
#17851=CARTESIAN_POINT('Ctrl Pts',(-0.16978883637574,0.033206302186043,
0.357397565525099));
#17852=CARTESIAN_POINT('Ctrl Pts',(-0.119923789760104,-0.124696399756661,
0.36533973364788));
#17853=CARTESIAN_POINT('Ctrl Pts',(0.0398037685148125,-0.168364388974385,
0.373281901770659));
#17854=CARTESIAN_POINT('Ctrl Pts',(0.163066985633654,-0.0577933011607096,
0.38122406989344));
#17855=CARTESIAN_POINT('Ctrl Pts',(0.136944091404129,0.10572238784759,0.38916623801622));
#17856=CARTESIAN_POINT('Ctrl Pts',(-0.0146336593526265,0.172385508313924,
0.397108406138999));
#17857=CARTESIAN_POINT('Ctrl Pts',(-0.152805474769431,0.0811257933285562,
0.40505057426178));
#17858=CARTESIAN_POINT('Ctrl Pts',(-0.150991776994562,-0.0844534827151793,
0.412992742384559));
#17859=CARTESIAN_POINT('Ctrl Pts',(-0.0108540995180527,-0.172664692355881,
0.42093491050734));
#17860=CARTESIAN_POINT('Ctrl Pts',(0.139227048201004,-0.102697305280782,
0.428877078630119));
#17861=CARTESIAN_POINT('Ctrl Pts',(0.16176191642983,0.0613513639265466,
0.4368192467529));
#17862=CARTESIAN_POINT('Ctrl Pts',(0.0361062507758455,0.169195880912067,
0.444761414875679));
#17863=CARTESIAN_POINT('Ctrl Pts',(-0.12262644992489,0.12203958882886,0.45270358299846));
#17864=CARTESIAN_POINT('Ctrl Pts',(-0.169020724600573,-0.0369175042249048,
0.460645751121239));
#17865=CARTESIAN_POINT('Ctrl Pts',(-0.0605746513833496,-0.162054370729346,
0.468587919244019));
#17866=CARTESIAN_POINT('Ctrl Pts',(0.103364025571403,-0.138732785167649,
0.4765300873668));
#17867=CARTESIAN_POINT('Ctrl Pts',(0.172610636112938,0.0116822841681558,
0.484472255489579));
#17868=CARTESIAN_POINT('Ctrl Pts',(0.083728171010617,0.151395181039277,
0.49241442361236));
#17869=CARTESIAN_POINT('Ctrl Pts',(-0.081857900459256,0.152414538660527,
0.500356591735139));
#17870=CARTESIAN_POINT('Ctrl Pts',(-0.172453725526818,0.0138065207282529,
0.50829875985792));
#17871=CARTESIAN_POINT('Ctrl Pts',(-0.105064221167447,-0.137449688588867,
0.516240927980699));
#17872=CARTESIAN_POINT('Ctrl Pts',(0.0585749034388466,-0.162787862415564,
0.52418309610348));
#17873=CARTESIAN_POINT('Ctrl Pts',(0.168553398866689,-0.0389956304370821,
0.532125264226259));
#17874=CARTESIAN_POINT('Ctrl Pts',(0.124119664784058,0.120520605195094,
0.54006743234904));
#17875=CARTESIAN_POINT('Ctrl Pts',(-0.0340204335384149,0.16962758491636,
0.548009600471819));
#17876=CARTESIAN_POINT('Ctrl Pts',(-0.160994319687769,0.0633382703503284,
0.5559517685946));
#17877=CARTESIAN_POINT('Ctrl Pts',(-0.14048086942825,-0.100975406844349,
0.563893936717379));
#17878=CARTESIAN_POINT('Ctrl Pts',(0.00872748937560605,-0.172785237771916,
0.57183610484016));
#17879=CARTESIAN_POINT('Ctrl Pts',(0.149940571302356,-0.0863060399984934,
0.579778272962939));
#17880=CARTESIAN_POINT('Ctrl Pts',(0.153792685935992,0.0792383569699183,
0.58772044108572));
#17881=CARTESIAN_POINT('Ctrl Pts',(0.0167549005293281,0.17219227848818,
0.595662609208499));
#17882=CARTESIAN_POINT('Ctrl Pts',(-0.135632095058532,0.107400382926376,
0.60360477733128));
#17883=CARTESIAN_POINT('Ctrl Pts',(-0.163766157558233,-0.0557812970565469,
0.611546945454059));
#17884=CARTESIAN_POINT('Ctrl Pts',(-0.0418735953979919,-0.167861578305293,
0.61948911357684));
#17885=CARTESIAN_POINT('Ctrl Pts',(0.118379481984711,-0.126163408751231,
0.627431281699619));
#17886=CARTESIAN_POINT('Ctrl Pts',(0.17018479228316,0.0311134044783985,
0.6353734498224));
#17887=CARTESIAN_POINT('Ctrl Pts',(0.0660833491022344,0.159887142804326,
0.643315617945179));
#17888=CARTESIAN_POINT('Ctrl Pts',(-0.0985572308567358,0.142187832491218,
0.651257786067961));
#17889=CARTESIAN_POINT('Ctrl Pts',(-0.172909262181909,-0.00577013989488307,
0.659199954190738));
#17890=CARTESIAN_POINT('Ctrl Pts',(-0.0888586457050277,-0.148442071348278,
0.667142122313521));
#17891=CARTESIAN_POINT('Ctrl Pts',(0.0765956190331784,-0.155125815413241,
0.675084290436298));
#17892=CARTESIAN_POINT('Ctrl Pts',(0.171880427770071,-0.0196983758791502,
0.683026458559081));
#17893=CARTESIAN_POINT('Ctrl Pts',(0.109705106722326,0.133774799651286,
0.690968626681858));
#17894=CARTESIAN_POINT('Ctrl Pts',(-0.0529713625168984,0.164696515493808,
0.698910794804641));
#17895=CARTESIAN_POINT('Ctrl Pts',(-0.167120621735807,0.0447393032280997,
0.706852962927418));
#17896=CARTESIAN_POINT('Ctrl Pts',(-0.12817022249092,-0.116203707037801,
0.7147951310502));
#17897=CARTESIAN_POINT('Ctrl Pts',(0.0281972679828983,-0.17069218359667,
0.722737299172979));
#17898=CARTESIAN_POINT('Ctrl Pts',(0.158733164168978,-0.0688090841067,0.73067946729576));
#17899=CARTESIAN_POINT('Ctrl Pts',(0.14385317469873,0.0961102054508026,
0.738621635418538));
#17900=CARTESIAN_POINT('Ctrl Pts',(-0.00281110139369983,0.172982673038814,
0.746563803541321));
#17901=CARTESIAN_POINT('Ctrl Pts',(-0.146900119814081,0.0913852409380608,
0.754505971664098));
#17902=CARTESIAN_POINT('Ctrl Pts',(-0.156413536862055,-0.0739304602244656,
0.762448139786881));
#17903=CARTESIAN_POINT('Ctrl Pts',(-0.0226360851712103,-0.171518264656626,
0.770390307909658));
#17904=CARTESIAN_POINT('Ctrl Pts',(0.131878346029848,-0.111977717922496,
0.778332476032441));
#17905=CARTESIAN_POINT('Ctrl Pts',(0.165578663890314,0.0501459223366878,
0.786274644155218));
#17906=CARTESIAN_POINT('Ctrl Pts',(0.047591915084802,0.166330746049129,
0.794216812278001));
#17907=CARTESIAN_POINT('Ctrl Pts',(-0.113993917241593,0.130139518573781,
0.802158980400778));
#17908=CARTESIAN_POINT('Ctrl Pts',(-0.171149610334614,-0.0252728776558711,
0.81010114852356));
#17909=CARTESIAN_POINT('Ctrl Pts',(-0.0715146774936035,-0.157532721571376,
0.818043316646339));
#17910=CARTESIAN_POINT('Ctrl Pts',(0.0936350469135118,-0.14547640857611,
0.825985484769119));
#17911=CARTESIAN_POINT('Ctrl Pts',(0.173005448853992,-0.000148759965830227,
0.8339276528919));
#17912=CARTESIAN_POINT('Ctrl Pts',(0.0938850861191564,0.145315168055841,
0.841869821014678));
#17913=CARTESIAN_POINT('Ctrl Pts',(-0.0712436606821878,0.157655473343934,
0.849811989137461));
#17914=CARTESIAN_POINT('Ctrl Pts',(-0.171105895159299,0.0255671684868261,
0.857754157260238));
#17915=CARTESIAN_POINT('Ctrl Pts',(-0.114217551294,-0.129943289319231,0.86569632538302));
#17916=CARTESIAN_POINT('Ctrl Pts',(0.0473058035714782,-0.166412344527548,
0.873638493505798));
#17917=CARTESIAN_POINT('Ctrl Pts',(0.16549218245563,-0.0504305959589149,
0.88158066162858));
#17918=CARTESIAN_POINT('Ctrl Pts',(0.132070720552549,0.111750759440056,
0.889522829751358));
#17919=CARTESIAN_POINT('Ctrl Pts',(-0.022341089517305,0.171556938600217,
0.89746499787414));
#17920=CARTESIAN_POINT('Ctrl Pts',(-0.156286166401977,0.074199337288632,
0.905407165996919));
#17921=CARTESIAN_POINT('Ctrl Pts',(-0.147057058974526,-0.0911324797668838,
0.913349334119699));
#17922=CARTESIAN_POINT('Ctrl Pts',(-0.00310857778072832,-0.172977582960567,
0.92129150224248));
#17923=CARTESIAN_POINT('Ctrl Pts',(0.143687680016546,-0.0963574495000853,
0.929233670365259));
#17924=CARTESIAN_POINT('Ctrl Pts',(0.158851261322436,0.0685360068793772,
0.93717583848804));
#17925=CARTESIAN_POINT('Ctrl Pts',(0.0284907678468484,0.170643439985825,
0.945118006610819));
#17926=CARTESIAN_POINT('Ctrl Pts',(-0.127970195944242,0.116423951198588,
0.9530601747336));
#17927=CARTESIAN_POINT('Ctrl Pts',(-0.167197313372666,-0.0444518375735043,
0.961002342856378));
#17928=CARTESIAN_POINT('Ctrl Pts',(-0.0532545149190986,-0.164605176417482,
0.96894451097916));
#17929=CARTESIAN_POINT('Ctrl Pts',(0.10947489024455,-0.133963263130763,
0.976886679101939));
#17930=CARTESIAN_POINT('Ctrl Pts',(0.1719140491614,0.0194027617526574,0.984828847224719));
#17931=CARTESIAN_POINT('Ctrl Pts',(0.0768622776450996,0.154993863549195,
0.992771015347499));
#17932=CARTESIAN_POINT('Ctrl Pts',(-0.088603236555915,0.148594663210074,
1.00071318347028));
#17933=CARTESIAN_POINT('Ctrl Pts',(-0.172899083515371,0.00606748566075909,
1.00865535159306));
#17934=CARTESIAN_POINT('Ctrl Pts',(-0.0988016073770141,-0.142018132090297,
1.01659751971584));
#17935=CARTESIAN_POINT('Ctrl Pts',(0.0658082913934689,-0.160000550769587,
1.02453968783862));
#17936=CARTESIAN_POINT('Ctrl Pts',(0.170131034504888,-0.0314060274628177,
1.0324818559614));
#17937=CARTESIAN_POINT('Ctrl Pts',(0.118596271784576,0.125959643463681,
1.04042402408418));
#17938=CARTESIAN_POINT('Ctrl Pts',(-0.0415848597483297,0.167933340651612,
1.04836619220696));
#17939=CARTESIAN_POINT('Ctrl Pts',(-0.163669987576804,0.0560628453550813,
1.05630836032974));
#17940=CARTESIAN_POINT('Ctrl Pts',(-0.135816592328243,-0.107166975841641,
1.06425052845252));
#17941=CARTESIAN_POINT('Ctrl Pts',(0.0164587544616562,-0.172220837485682,
1.0721926965753));
#17942=CARTESIAN_POINT('Ctrl Pts',(0.153656191292587,-0.0795027190739688,
1.08013486469808));
#17943=CARTESIAN_POINT('Ctrl Pts',(0.150088771199207,0.0860480576341552,
1.08807703282086));
#17944=CARTESIAN_POINT('Ctrl Pts',(0.00902461748204118,0.172769973496559,
1.09601920094364));
#17945=CARTESIAN_POINT('Ctrl Pts',(-0.140307012982855,0.101216844302358,
1.10396136906642));
#17946=CARTESIAN_POINT('Ctrl Pts',(-0.161103005268346,-0.0630613126743013,
1.1119035371892));
#17947=CARTESIAN_POINT('Ctrl Pts',(-0.0343120939874615,-0.1695688287065,
1.11984570531198));
#17948=CARTESIAN_POINT('Ctrl Pts',(0.123912220401285,-0.120733877175888,
1.12778787343476));
#17949=CARTESIAN_POINT('Ctrl Pts',(0.168620210916381,0.0387057093103061,
1.13573004155754));
#17950=CARTESIAN_POINT('Ctrl Pts',(0.0588547652196237,0.162686889679659,
1.14367220968032));
#17951=CARTESIAN_POINT('Ctrl Pts',(-0.104827691798069,0.137630165643247,
1.1516143778031));
#17952=CARTESIAN_POINT('Ctrl Pts',(-0.172477213770776,-0.0135099294065116,
1.15955654592588));
#17953=CARTESIAN_POINT('Ctrl Pts',(-0.0821198886720452,-0.152273541192125,
1.16749871404866));
#17954=CARTESIAN_POINT('Ctrl Pts',(0.083467690946984,-0.15153894559049,
1.17544088217144));
#17955=CARTESIAN_POINT('Ctrl Pts',(0.172590290696882,-0.0119791076405788,
1.18338305029422));
#17956=CARTESIAN_POINT('Ctrl Pts',(0.103602453294194,0.13855482356859,1.191325218417));
#17957=CARTESIAN_POINT('Ctrl Pts',(-0.0602958748103966,0.162158302111078,
1.19926738653978));
#17958=CARTESIAN_POINT('Ctrl Pts',(-0.168956987158091,0.0372081167644847,
1.20720955466256));
#17959=CARTESIAN_POINT('Ctrl Pts',(-0.122836141658186,-0.121828526073448,
1.21515172278534));
#17960=CARTESIAN_POINT('Ctrl Pts',(0.0358152290369173,-0.169257723108079,
1.22309389090812));
#17961=CARTESIAN_POINT('Ctrl Pts',(0.161656170495932,-0.0616294572691503,
1.2310360590309));
#17962=CARTESIAN_POINT('Ctrl Pts',(0.13940345221127,0.102457722863032,1.23897822715368));
#17963=CARTESIAN_POINT('Ctrl Pts',(-0.0105571497596809,0.172683102970871,
1.24692039527646));
#17964=CARTESIAN_POINT('Ctrl Pts',(-0.150846317973597,0.0847130203482025,
1.25486256339924));
#17965=CARTESIAN_POINT('Ctrl Pts',(-0.152944761892581,-0.0808628918127005,
1.26280473152202));
#17966=CARTESIAN_POINT('Ctrl Pts',(-0.0149300913057054,-0.172360087712588,
1.2707468996448));
#17967=CARTESIAN_POINT('Ctrl Pts',(0.136762076743997,-0.105957736043287,
1.27868906776758));
#17968=CARTESIAN_POINT('Ctrl Pts',(0.163166132393764,0.0575127872937276,
1.28663123589036));
#17969=CARTESIAN_POINT('Ctrl Pts',(0.0400932480780463,0.168295688956082,
1.29457340401314));
#17970=CARTESIAN_POINT('Ctrl Pts',(-0.119709170414695,0.124902449862528,
1.30251557213592));
#17971=CARTESIAN_POINT('Ctrl Pts',(-0.169845690614082,-0.0329142650230248,
1.3104577402587));
#17972=CARTESIAN_POINT('Ctrl Pts',(-0.0643861093061943,-0.160578131733314,
1.31839990838148));
#17973=CARTESIAN_POINT('Ctrl Pts',(0.100057762773863,-0.141135932963798,
1.32634207650426));
#17974=CARTESIAN_POINT('Ctrl Pts',(0.172838444806952,0.00760127985757451,
1.33428424462704));
#17975=CARTESIAN_POINT('Ctrl Pts',(0.0872813550697656,0.149374939398002,
1.34222641274982));
#17976=CARTESIAN_POINT('Ctrl Pts',(-0.0782344227434143,0.154305808621531,
1.3501685808726));
#17977=CARTESIAN_POINT('Ctrl Pts',(-0.172079431848303,0.0178767046294837,
1.35811074899538));
#17978=CARTESIAN_POINT('Ctrl Pts',(-0.108282003268856,-0.134929297194493,
1.36605291711816));
#17979=CARTESIAN_POINT('Ctrl Pts',(0.0547128650701426,-0.164126201264144,
1.37399508524094));
#17980=CARTESIAN_POINT('Ctrl Pts',(0.167585127127835,-0.0429666431014547,
1.38193725336372));
#17981=CARTESIAN_POINT('Ctrl Pts',(0.126932197981417,0.117554773230619,
1.3898794214865));
#17982=CARTESIAN_POINT('Ctrl Pts',(-0.0300036684000219,0.170383942402052,
1.39782158960928));
#17983=CARTESIAN_POINT('Ctrl Pts',(-0.159453085214751,0.0671239123677834,
1.40576375773206));
#17984=CARTESIAN_POINT('Ctrl Pts',(-0.142827107870127,-0.0976285101620078,
1.41370592585484));
#17985=CARTESIAN_POINT('Ctrl Pts',(0.00464319840846943,-0.172943201171859,
1.42164809397762));
#17986=CARTESIAN_POINT('Ctrl Pts',(0.147859810582222,-0.0898241270588577,
1.4295902621004));
#17987=CARTESIAN_POINT('Ctrl Pts',(0.155621735944117,0.0755830265922534,
1.43753243022318));
#17988=CARTESIAN_POINT('Ctrl Pts',(0.0208179928734729,0.171748455656582,
1.44547459834596));
#17989=CARTESIAN_POINT('Ctrl Pts',(-0.133056846329205,0.11057447892796,
1.45341676646874));
#17990=CARTESIAN_POINT('Ctrl Pts',(-0.165038560097216,-0.0518967460486161,
1.46135893459152));
#17991=CARTESIAN_POINT('Ctrl Pts',(-0.0458268296361176,-0.166825854601292,
1.4693011027143));
#17992=CARTESIAN_POINT('Ctrl Pts',(0.115364766925686,-0.128924136976022,
1.47724327083708));
#17993=CARTESIAN_POINT('Ctrl Pts',(0.170874595884426,0.0270830477535184,
1.48518543895986));
#17994=CARTESIAN_POINT('Ctrl Pts',(0.0698377457337486,0.158283721017069,
1.49312760708264));
#17995=CARTESIAN_POINT('Ctrl Pts',(-0.0951624750893037,0.144471999488883,
1.50106977520542));
#17996=CARTESIAN_POINT('Ctrl Pts',(-0.173012914651864,-0.00167525885548286,
1.5090119433282));
#17997=CARTESIAN_POINT('Ctrl Pts',(-0.092311001583214,-0.14631755460685,
1.51695411145098));
#17998=CARTESIAN_POINT('Ctrl Pts',(0.072853104778531,-0.156861289272697,
1.52489627957376));
#17999=CARTESIAN_POINT('Ctrl Pts',(0.171475934783304,-0.0238129810547936,
1.53283844769654));
#18000=CARTESIAN_POINT('Ctrl Pts',(0.11261423476106,0.131269690464983,1.54078061581932));
#18001=CARTESIAN_POINT('Ctrl Pts',(0.00518264413773371,0.154149172621267,
1.54607539456784));
#18002=CARTESIAN_POINT('Ctrl Pts',(-0.0415060733757155,0.140340900570467,
1.5487227839421));
#18003=CARTESIAN_POINT('Ctrl Pts',(-0.146248097568756,-0.000123763188177425,
1.45893449541571));
#18004=CARTESIAN_POINT('Ctrl Pts',(-0.146367493381718,-0.0150081347743067,
1.45974264180765));
#18005=CARTESIAN_POINT('Ctrl Pts',(-0.144277648885518,-0.0298597803798721,
1.46055078819958));
#18006=CARTESIAN_POINT('Ctrl Pts',(-0.139839652725699,-0.043973059977961,
1.46135893459152));
#18007=CARTESIAN_POINT('Ctrl Pts',(-0.125301316610186,-0.0902064488995044,
1.46400632396578));
#18008=CARTESIAN_POINT('Ctrl Pts',(-0.08556407312315,-0.1285161517504,1.46665371334004));
#18009=CARTESIAN_POINT('Ctrl Pts',(-0.0388301852859989,-0.141354050238301,
1.4693011027143));
#18010=CARTESIAN_POINT('Ctrl Pts',(0.00790370255115092,-0.154191948726202,
1.47194849208856));
#18011=CARTESIAN_POINT('Ctrl Pts',(0.0616342347384179,-0.141558042851112,
1.47459588146282));
#18012=CARTESIAN_POINT('Ctrl Pts',(0.0977511389918415,-0.109239892458645,
1.47724327083708));
#18013=CARTESIAN_POINT('Ctrl Pts',(0.133868043245265,-0.0769217420661769,
1.47989066021134));
#18014=CARTESIAN_POINT('Ctrl Pts',(0.152371319564846,-0.024919347156331,
1.4825380495856));
#18015=CARTESIAN_POINT('Ctrl Pts',(0.144783482699524,0.0229486291758506,
1.48518543895986));
#18016=CARTESIAN_POINT('Ctrl Pts',(0.137195645834202,0.0708166055080336,
1.48783282833412));
#18017=CARTESIAN_POINT('Ctrl Pts',(0.103516695783975,0.114550163262552,
1.49048021770838));
#18018=CARTESIAN_POINT('Ctrl Pts',(0.0591771839550196,0.13411498855178,
1.49312760708264));
#18019=CARTESIAN_POINT('Ctrl Pts',(0.014837672126065,0.153679813841007,
1.4957749964569));
#18020=CARTESIAN_POINT('Ctrl Pts',(-0.0401624014816186,0.149075906664945,
1.49842238583116));
#18021=CARTESIAN_POINT('Ctrl Pts',(-0.0806375115458872,0.122416076686187,
1.50106977520542));
#18022=CARTESIAN_POINT('Ctrl Pts',(-0.0937869288003098,0.113754921033589,
1.50192985013695));
#18023=CARTESIAN_POINT('Ctrl Pts',(-0.105403311347291,0.102765876910903,
1.50278992506847));
#18024=CARTESIAN_POINT('Ctrl Pts',(-0.115078604842433,0.0902138214954038,
1.50365));
#18025=CARTESIAN_POINT('Ctrl Pts',(-0.0686146973663081,-0.0959584553529135,
1.07336015076065E-17));
#18026=CARTESIAN_POINT('Ctrl Pts',(-0.0712979561985307,-0.0944995001033786,
9.02613639135873E-18));
#18027=CARTESIAN_POINT('Ctrl Pts',(-0.0739152333025289,-0.0929325179580126,
1.64107321374712E-17));
#18028=CARTESIAN_POINT('Ctrl Pts',(-0.0764591723283171,-0.0912589988675934,
1.6154612370034E-17));
#18029=CARTESIAN_POINT('Ctrl Pts',(-0.0824897891353913,-0.0872917841461184,
1.52077426268717E-17));
#18030=CARTESIAN_POINT('Ctrl Pts',(-0.0881090519769445,-0.0827275518978924,
1.30971627060498E-17));
#18031=CARTESIAN_POINT('Ctrl Pts',(-0.0932912133381108,-0.0776621329443405,
1.43114686768087E-17));
#18032=CARTESIAN_POINT('Ctrl Pts',(-0.0960634919631888,-0.074952307504085,
1.49610807310118E-17));
#18033=CARTESIAN_POINT('Ctrl Pts',(-0.0987043519497191,-0.0721043812799658,
1.74993329480528E-17));
#18034=CARTESIAN_POINT('Ctrl Pts',(-0.101206237074718,-0.0691378820326018,
9.97465998686664E-18));
#18035=CARTESIAN_POINT('Ctrl Pts',(-0.105823426721714,-0.0636632543305198,
-3.91200561030858E-18));
#18036=CARTESIAN_POINT('Ctrl Pts',(-0.109972666997065,-0.0577811896139199,
2.24798207762934E-18));
#18037=CARTESIAN_POINT('Ctrl Pts',(-0.113625452403263,-0.0515741981665521,
9.54097911787244E-18));
#18038=CARTESIAN_POINT('Ctrl Pts',(-0.115386295340069,-0.0485820878086944,
1.30566037435822E-17));
#18039=CARTESIAN_POINT('Ctrl Pts',(-0.117027309103105,-0.0455212415157476,
-2.79521757168051E-18));
#18040=CARTESIAN_POINT('Ctrl Pts',(-0.118543833519887,-0.0424058589801268,
-3.46944695195361E-18));
#18041=CARTESIAN_POINT('Ctrl Pts',(-0.122700941917732,-0.0338659484069709,
-5.31764971597768E-18));
#18042=CARTESIAN_POINT('Ctrl Pts',(-0.125931492798984,-0.0249085743588085,
-1.15219401683824E-18));
#18043=CARTESIAN_POINT('Ctrl Pts',(-0.128167520083254,-0.0157105262534848,
9.54097911787244E-18));
#18044=CARTESIAN_POINT('Ctrl Pts',(-0.128992166906242,-0.0123182862745252,
1.3484621181291E-17));
#18045=CARTESIAN_POINT('Ctrl Pts',(-0.129681150280034,-0.00889298553317688,
1.10989611676181E-17));
#18046=CARTESIAN_POINT('Ctrl Pts',(-0.130229483957028,-0.00544263935519351,
9.54097911787244E-18));
#18047=CARTESIAN_POINT('Ctrl Pts',(-0.130761899349706,-0.00209245771889707,
8.02822573502553E-18));
#18048=CARTESIAN_POINT('Ctrl Pts',(-0.131160261982709,0.00127366115726457,
1.11791151702242E-17));
#18049=CARTESIAN_POINT('Ctrl Pts',(-0.131420990891747,0.00464012593483382,
8.67361737988404E-18));
#18050=CARTESIAN_POINT('Ctrl Pts',(-0.131728666658755,0.00861275649723166,
5.71697955546795E-18));
#18051=CARTESIAN_POINT('Ctrl Pts',(-0.131845259942619,0.0125891451047215,
-9.26473565962443E-18));
#18052=CARTESIAN_POINT('Ctrl Pts',(-0.131765781147177,0.0165567997877194,
-1.04083408558608E-17));
#18053=CARTESIAN_POINT('Ctrl Pts',(-0.131635692412819,0.0230509492424239,
-1.21888544026837E-17));
#18054=CARTESIAN_POINT('Ctrl Pts',(-0.13098103789945,0.0295216962360144,
-2.67049856555875E-17));
#18055=CARTESIAN_POINT('Ctrl Pts',(-0.129839098367345,0.0359278479980343,
-3.46944695195361E-17));
#18056=CARTESIAN_POINT('Ctrl Pts',(-0.129254890951344,0.0392051855997028,
-3.87818275556788E-17));
#18057=CARTESIAN_POINT('Ctrl Pts',(-0.128542951403208,0.0424656461998481,
-3.10678831811161E-17));
#18058=CARTESIAN_POINT('Ctrl Pts',(-0.1277070993652,0.0457037274559979,
-3.29597460435593E-17));
#18059=CARTESIAN_POINT('Ctrl Pts',(-0.126886363095037,0.0488832504000222,
-3.48173959609792E-17));
#18060=CARTESIAN_POINT('Ctrl Pts',(-0.125948031872817,0.0520333657183593,
-3.53366201082739E-17));
#18061=CARTESIAN_POINT('Ctrl Pts',(-0.124899042599898,0.0551436241923499,
-3.46944695195361E-17));
#18062=CARTESIAN_POINT('Ctrl Pts',(-0.122234979928128,0.0630425834229368,
-3.30636335736642E-17));
#18063=CARTESIAN_POINT('Ctrl Pts',(-0.118856305871375,0.070695441500891,
-2.1366080483524E-17));
#18064=CARTESIAN_POINT('Ctrl Pts',(-0.114834854776346,0.078019637496205,
-1.73472347597681E-17));
#18065=CARTESIAN_POINT('Ctrl Pts',(-0.11215901866562,0.0828930893082948,
-1.46731322388254E-17));
#18066=CARTESIAN_POINT('Ctrl Pts',(-0.109198005187061,0.0876211033078822,
8.28606628989234E-18));
#18067=CARTESIAN_POINT('Ctrl Pts',(-0.105966883726074,0.0921780034666525,
8.67361737988404E-18));
#18068=CARTESIAN_POINT('Ctrl Pts',(-0.104137243112614,0.094758373688769,
8.89307035390601E-18));
#18069=CARTESIAN_POINT('Ctrl Pts',(-0.102221042121924,0.0972831505018574,
-2.31209379389524E-17));
#18070=CARTESIAN_POINT('Ctrl Pts',(-0.100229777791505,0.0997373632832089,
-2.08166817117217E-17));
#18071=CARTESIAN_POINT('Ctrl Pts',(-0.0937202782075859,0.107760254486057,
-1.32840027382311E-17));
#18072=CARTESIAN_POINT('Ctrl Pts',(-0.0863914655699752,0.115060936709644,
5.4842312373535E-18));
#18073=CARTESIAN_POINT('Ctrl Pts',(-0.0783508402622743,0.121487309774744,
1.38777878078145E-17));
#18074=CARTESIAN_POINT('Ctrl Pts',(-0.073610711791116,0.125275800441382,
1.8825977152717E-17));
#18075=CARTESIAN_POINT('Ctrl Pts',(-0.068622257850438,0.128760167547443,
-9.09579695168528E-18));
#18076=CARTESIAN_POINT('Ctrl Pts',(-0.0634007094575209,0.131904027763685,
-6.93889390390723E-18));
#18077=CARTESIAN_POINT('Origin',(0.,0.,0.));
#18078=CARTESIAN_POINT('Origin',(-0.0721687836487033,-0.125,-0.3));
#18079=CARTESIAN_POINT('',(-0.0721687836487033,-0.125,-0.3));
#18080=CARTESIAN_POINT('',(0.0721687836487032,-0.125,-0.3));
#18081=CARTESIAN_POINT('',(-0.0360843918243517,-0.125,-0.3));
#18082=CARTESIAN_POINT('',(-0.0721687836487033,-0.125,-0.15));
#18083=CARTESIAN_POINT('',(-0.0721687836487033,-0.125,-0.3));
#18084=CARTESIAN_POINT('',(0.0721687836487032,-0.125,-0.15));
#18085=CARTESIAN_POINT('',(-0.0721687836487033,-0.125,-0.15));
#18086=CARTESIAN_POINT('',(0.0721687836487032,-0.125,-0.3));
#18087=CARTESIAN_POINT('Origin',(-0.144337567297406,1.76762539787485E-17,
-0.3));
#18088=CARTESIAN_POINT('',(-0.144337567297406,1.76762539787485E-17,-0.3));
#18089=CARTESIAN_POINT('',(-0.126295371385231,-0.03125,-0.3));
#18090=CARTESIAN_POINT('',(-0.144337567297406,2.77555756156289E-17,-0.15));
#18091=CARTESIAN_POINT('',(-0.144337567297406,1.76762539787485E-17,-0.3));
#18092=CARTESIAN_POINT('',(-0.144337567297406,1.76762539787485E-17,-0.15));
#18093=CARTESIAN_POINT('Origin',(-0.0721687836487032,0.125,-0.3));
#18094=CARTESIAN_POINT('',(-0.0721687836487032,0.125,-0.3));
#18095=CARTESIAN_POINT('',(-0.090210979560879,0.09375,-0.3));
#18096=CARTESIAN_POINT('',(-0.0721687836487032,0.125,-0.15));
#18097=CARTESIAN_POINT('',(-0.0721687836487032,0.125,-0.3));
#18098=CARTESIAN_POINT('',(-0.0721687836487032,0.125,-0.15));
#18099=CARTESIAN_POINT('Origin',(0.0721687836487032,0.125,-0.3));
#18100=CARTESIAN_POINT('',(0.0721687836487032,0.125,-0.3));
#18101=CARTESIAN_POINT('',(0.0360843918243516,0.125,-0.3));
#18102=CARTESIAN_POINT('',(0.0721687836487032,0.125,-0.15));
#18103=CARTESIAN_POINT('',(0.0721687836487032,0.125,-0.3));
#18104=CARTESIAN_POINT('',(0.0721687836487032,0.125,-0.15));
#18105=CARTESIAN_POINT('Origin',(0.144337567297406,0.,-0.3));
#18106=CARTESIAN_POINT('',(0.144337567297406,0.,-0.3));
#18107=CARTESIAN_POINT('',(0.126295371385231,0.03125,-0.3));
#18108=CARTESIAN_POINT('',(0.144337567297406,0.,-0.15));
#18109=CARTESIAN_POINT('',(0.144337567297406,0.,-0.3));
#18110=CARTESIAN_POINT('',(0.144337567297406,0.,-0.15));
#18111=CARTESIAN_POINT('Origin',(0.0721687836487032,-0.125,-0.3));
#18112=CARTESIAN_POINT('',(0.0902109795608791,-0.09375,-0.3));
#18113=CARTESIAN_POINT('',(0.0721687836487032,-0.125,-0.15));
#18114=CARTESIAN_POINT('Origin',(0.,0.,-0.15));
#18115=CARTESIAN_POINT('Origin',(0.,0.,0.));
#18116=CARTESIAN_POINT('',(-0.275,-3.36777869765522E-17,0.));
#18117=CARTESIAN_POINT('Origin',(0.,0.,0.));
#18118=CARTESIAN_POINT('Origin',(0.,0.,-0.3));
#18119=CARTESIAN_POINT('',(-0.275,-3.36777869765522E-17,-0.3));
#18120=CARTESIAN_POINT('',(-0.275,-3.36777869765522E-17,-0.3));
#18121=CARTESIAN_POINT('Origin',(0.,0.,-0.3));
#18122=CARTESIAN_POINT('Origin',(0.,0.,-0.3));
#18123=CARTESIAN_POINT('Origin',(0.,0.,1.6));
#19074=UNCERTAINTY_MEASURE_WITH_UNIT(LENGTH_MEASURE(0.001),#19091,
'DISTANCE_ACCURACY_VALUE',
'Maximum model space distance between geometric entities at asserted c
onnectivities');
#19077=UNCERTAINTY_MEASURE_WITH_UNIT(LENGTH_MEASURE(0.001),#19091,
'DISTANCE_ACCURACY_VALUE',
'Maximum model space distance between geometric entities at asserted c
onnectivities');
#19087=(
GEOMETRIC_REPRESENTATION_CONTEXT(3)
GLOBAL_UNCERTAINTY_ASSIGNED_CONTEXT((#19074))
GLOBAL_UNIT_ASSIGNED_CONTEXT((#19091,#19093,#19094))
REPRESENTATION_CONTEXT('','3D')
);
#19090=(
GEOMETRIC_REPRESENTATION_CONTEXT(3)
GLOBAL_UNCERTAINTY_ASSIGNED_CONTEXT((#19077))
GLOBAL_UNIT_ASSIGNED_CONTEXT((#19091,#19093,#19094))
REPRESENTATION_CONTEXT('','3D')
);
#19091=(
LENGTH_UNIT()
NAMED_UNIT(*)
SI_UNIT(.CENTI.,.METRE.)
);
#19093=(
NAMED_UNIT(*)
PLANE_ANGLE_UNIT()
SI_UNIT($,.RADIAN.)
);
#19094=(
NAMED_UNIT(*)
SI_UNIT($,.STERADIAN.)
SOLID_ANGLE_UNIT()
);
#19104=SHAPE_DEFINITION_REPRESENTATION(#19116,#19144);
#19116=PRODUCT_DEFINITION_SHAPE('',$,#19157);
#19144=SHAPE_REPRESENTATION('',(#7304),#19087);
#19147=PRODUCT_DEFINITION_CONTEXT('part definition',#19185,'design');
#19157=PRODUCT_DEFINITION('2026-11-10-05-09-19-266',
'Socket head cap screw M3x16',#19169,#19147);
#19169=PRODUCT_DEFINITION_FORMATION('',$,#19196);
#19185=APPLICATION_CONTEXT(
'Core Data for Automotive Mechanical Design Process');
#19186=PRODUCT_CONTEXT('part definition',#19185,'mechanical');
#19196=PRODUCT('2026-11-10-05-09-19-266','Socket head cap screw M3x16',
$,(#19186));
#19202=PRESENTATION_STYLE_ASSIGNMENT((#19210));
#19210=SURFACE_STYLE_USAGE(.BOTH.,#19218);
#19218=SURFACE_SIDE_STYLE('',(#19226));
#19226=SURFACE_STYLE_FILL_AREA(#19234);
#19234=FILL_AREA_STYLE('Dark gray',(#19242));
#19242=FILL_AREA_STYLE_COLOUR('Dark gray',#19250);
#19250=COLOUR_RGB('Dark gray',0.250980392156863,0.282352941176471,0.32156862745098);
ENDSEC;
END-ISO-10303-21;
